ISO-10303-21;
HEADER;
FILE_DESCRIPTION((''),'2;1');
FILE_NAME('Pan_Head_Phillips_Screw.step','2026-10-09T10:33:02-07:00',(''),(''),'','','');
FILE_SCHEMA (('AUTOMOTIVE_DESIGN { 1 0 10303 214 3 1 1 }'));
ENDSEC;
DATA;
#10=MECHANICAL_DESIGN_GEOMETRIC_PRESENTATION_REPRESENTATION('',(#847),#86330);
#121=SPHERICAL_SURFACE('',#36434,4.225) ;
#468=TOROIDAL_SURFACE('',#36429,2.55,0.449999999999999) ;
#469=TOROIDAL_SURFACE('',#36456,2.55,0.45) ;
#758=(
BOUNDED_SURFACE()
B_SPLINE_SURFACE(1,2,((#84487,#84488,#84489,#84490,#84491,#84492,#84493,
#84494,#84495,#84496,#84497,#84498,#84499,#84500,#84501,#84502,#84503,#84504,
#84505,#84506,#84507,#84508,#84509,#84510,#84511,#84512,#84513,#84514,#84515,
#84516,#84517,#84518,#84519,#84520,#84521,#84522,#84523,#84524,#84525,#84526,
#84527,#84528,#84529,#84530,#84531,#84532,#84533,#84534,#84535,#84536,#84537,
#84538,#84539,#84540,#84541,#84542,#84543,#84544,#84545,#84546,#84547,#84548,
#84549,#84550,#84551,#84552,#84553,#84554,#84555,#84556,#84557,#84558,#84559,
#84560,#84561,#84562,#84563,#84564,#84565,#84566,#84567,#84568,#84569,#84570,
#84571,#84572,#84573,#84574,#84575,#84576,#84577,#84578,#84579,#84580,#84581,
#84582,#84583,#84584,#84585,#84586,#84587,#84588,#84589,#84590,#84591,#84592,
#84593,#84594,#84595,#84596,#84597,#84598,#84599,#84600,#84601,#84602,#84603,
#84604,#84605,#84606,#84607,#84608,#84609,#84610,#84611,#84612,#84613,#84614,
#84615,#84616,#84617,#84618,#84619,#84620,#84621,#84622,#84623,#84624,#84625,
#84626,#84627,#84628,#84629,#84630,#84631,#84632,#84633,#84634,#84635,#84636,
#84637,#84638,#84639,#84640,#84641,#84642,#84643,#84644,#84645,#84646,#84647,
#84648,#84649,#84650,#84651,#84652,#84653,#84654,#84655,#84656,#84657,#84658,
#84659,#84660,#84661,#84662,#84663,#84664,#84665,#84666,#84667,#84668,#84669,
#84670,#84671,#84672,#84673,#84674,#84675,#84676,#84677,#84678,#84679,#84680,
#84681,#84682,#84683,#84684,#84685,#84686,#84687,#84688,#84689,#84690,#84691,
#84692,#84693,#84694,#84695,#84696,#84697,#84698,#84699,#84700,#84701,#84702,
#84703),(#84704,#84705,#84706,#84707,#84708,#84709,#84710,#84711,#84712,
#84713,#84714,#84715,#84716,#84717,#84718,#84719,#84720,#84721,#84722,#84723,
#84724,#84725,#84726,#84727,#84728,#84729,#84730,#84731,#84732,#84733,#84734,
#84735,#84736,#84737,#84738,#84739,#84740,#84741,#84742,#84743,#84744,#84745,
#84746,#84747,#84748,#84749,#84750,#84751,#84752,#84753,#84754,#84755,#84756,
#84757,#84758,#84759,#84760,#84761,#84762,#84763,#84764,#84765,#84766,#84767,
#84768,#84769,#84770,#84771,#84772,#84773,#84774,#84775,#84776,#84777,#84778,
#84779,#84780,#84781,#84782,#84783,#84784,#84785,#84786,#84787,#84788,#84789,
#84790,#84791,#84792,#84793,#84794,#84795,#84796,#84797,#84798,#84799,#84800,
#84801,#84802,#84803,#84804,#84805,#84806,#84807,#84808,#84809,#84810,#84811,
#84812,#84813,#84814,#84815,#84816,#84817,#84818,#84819,#84820,#84821,#84822,
#84823,#84824,#84825,#84826,#84827,#84828,#84829,#84830,#84831,#84832,#84833,
#84834,#84835,#84836,#84837,#84838,#84839,#84840,#84841,#84842,#84843,#84844,
#84845,#84846,#84847,#84848,#84849,#84850,#84851,#84852,#84853,#84854,#84855,
#84856,#84857,#84858,#84859,#84860,#84861,#84862,#84863,#84864,#84865,#84866,
#84867,#84868,#84869,#84870,#84871,#84872,#84873,#84874,#84875,#84876,#84877,
#84878,#84879,#84880,#84881,#84882,#84883,#84884,#84885,#84886,#84887,#84888,
#84889,#84890,#84891,#84892,#84893,#84894,#84895,#84896,#84897,#84898,#84899,
#84900,#84901,#84902,#84903,#84904,#84905,#84906,#84907,#84908,#84909,#84910,
#84911,#84912,#84913,#84914,#84915,#84916,#84917,#84918,#84919,#84920)),
 .UNSPECIFIED.,.F.,.F.,.F.)
B_SPLINE_SURFACE_WITH_KNOTS((2,2),(3,2,2,2,2,2,2,2,2,2,2,2,2,2,2,2,2,2,
2,2,2,2,2,2,2,2,2,2,2,2,2,2,2,2,2,2,2,2,2,2,2,2,2,2,2,2,2,2,2,2,2,2,2,2,
2,2,2,2,2,2,2,2,2,2,2,2,2,2,2,2,2,2,2,2,2,2,2,2,2,2,2,2,2,2,2,2,2,2,2,2,
2,2,2,2,2,2,2,2,2,2,2,2,2,2,2,2,2,2,3),(-3.28672302357595E-5,1.),(-2.52038739293362E-5,
0.00925925925925926,0.0185185185185185,0.0277777777777778,0.037037037037037,
0.0462962962962963,0.0555555555555556,0.0648148148148148,0.0740740740740741,
0.0833333333333333,0.0925925925925926,0.101851851851852,0.111111111111111,
0.12037037037037,0.12962962962963,0.138888888888889,0.148148148148148,0.157407407407407,
0.166666666666667,0.175925925925926,0.185185185185185,0.194444444444444,
0.203703703703704,0.212962962962963,0.222222222222222,0.231481481481481,
0.240740740740741,0.25,0.259259259259259,0.268518518518519,0.277777777777778,
0.287037037037037,0.296296296296296,0.305555555555556,0.314814814814815,
0.324074074074074,0.333333333333333,0.342592592592593,0.351851851851852,
0.361111111111111,0.37037037037037,0.37962962962963,0.388888888888889,0.398148148148148,
0.407407407407407,0.416666666666667,0.425925925925926,0.435185185185185,
0.444444444444444,0.453703703703704,0.462962962962963,0.472222222222222,
0.481481481481481,0.490740740740741,0.5,0.509259259259259,0.518518518518518,
0.527777777777778,0.537037037037037,0.546296296296296,0.555555555555556,
0.564814814814815,0.574074074074074,0.583333333333333,0.592592592592593,
0.601851851851852,0.611111111111111,0.62037037037037,0.62962962962963,0.638888888888889,
0.648148148148148,0.657407407407407,0.666666666666667,0.675925925925926,
0.685185185185185,0.694444444444444,0.703703703703704,0.712962962962963,
0.722222222222222,0.731481481481482,0.740740740740741,0.75,0.759259259259259,
0.768518518518518,0.777777777777778,0.787037037037037,0.796296296296296,
0.805555555555556,0.814814814814815,0.824074074074074,0.833333333333333,
0.842592592592593,0.851851851851852,0.861111111111111,0.87037037037037,
0.87962962962963,0.888888888888889,0.898148148148148,0.907407407407407,
0.916666666666667,0.925925925925926,0.935185185185185,0.944444444444444,
0.953703703703704,0.962962962962963,0.972222222222222,0.981481481481482,
0.990740740740741,1.),.UNSPECIFIED.)
GEOMETRIC_REPRESENTATION_ITEM()
RATIONAL_B_SPLINE_SURFACE(((1.00073134796636,0.865660722470502,1.,0.866025403784439,
1.,0.866025403784439,1.,0.866025403784439,1.,0.866025403784439,1.,0.866025403784439,
1.,0.866025403784439,1.,0.866025403784439,1.,0.866025403784439,1.,0.866025403784439,
1.,0.866025403784439,1.,0.866025403784439,1.,0.866025403784439,1.,0.866025403784439,
1.,0.866025403784439,1.,0.866025403784439,1.,0.866025403784439,1.,0.866025403784439,
1.,0.866025403784439,1.,0.866025403784439,1.,0.866025403784439,1.,0.866025403784439,
1.,0.866025403784439,1.,0.866025403784439,1.,0.866025403784439,1.,0.866025403784439,
1.,0.866025403784439,1.,0.866025403784439,1.,0.866025403784439,1.,0.866025403784439,
1.,0.866025403784439,1.,0.866025403784439,1.,0.866025403784439,1.,0.866025403784439,
1.,0.866025403784439,1.,0.866025403784439,1.,0.866025403784439,1.,0.866025403784439,
1.,0.866025403784439,1.,0.866025403784439,1.,0.866025403784439,1.,0.866025403784439,
1.,0.866025403784439,1.,0.866025403784439,1.,0.866025403784439,1.,0.866025403784439,
1.,0.866025403784439,1.,0.866025403784439,1.,0.866025403784439,1.,0.866025403784439,
1.,0.866025403784439,1.,0.866025403784439,1.,0.866025403784439,1.,0.866025403784439,
1.,0.866025403784439,1.,0.866025403784439,1.,0.866025403784439,1.,0.866025403784439,
1.,0.866025403784439,1.,0.866025403784439,1.,0.866025403784439,1.,0.866025403784439,
1.,0.866025403784439,1.,0.866025403784439,1.,0.866025403784439,1.,0.866025403784439,
1.,0.866025403784439,1.,0.866025403784439,1.,0.866025403784439,1.,0.866025403784439,
1.,0.866025403784439,1.,0.866025403784439,1.,0.866025403784439,1.,0.866025403784439,
1.,0.866025403784439,1.,0.866025403784439,1.,0.866025403784439,1.,0.866025403784439,
1.,0.866025403784439,1.,0.866025403784439,1.,0.866025403784439,1.,0.866025403784439,
1.,0.866025403784439,1.,0.866025403784439,1.,0.866025403784439,1.,0.866025403784439,
1.,0.866025403784439,1.,0.866025403784439,1.,0.866025403784439,1.,0.866025403784439,
1.,0.866025403784439,1.,0.866025403784439,1.,0.866025403784439,1.,0.866025403784439,
1.,0.866025403784439,1.,0.866025403784439,1.,0.866025403784439,1.,0.866025403784439,
1.,0.866025403784439,1.,0.866025403784439,1.,0.866025403784439,1.,0.866025403784439,
1.,0.866025403784439,1.,0.866025403784439,1.,0.866025403784439,1.,0.866025403784439,
1.,0.866025403784439,1.,0.866025403784439,1.),(1.00073134796636,0.865660722470502,
1.,0.866025403784439,1.,0.866025403784439,1.,0.866025403784439,1.,0.866025403784439,
1.,0.866025403784439,1.,0.866025403784439,1.,0.866025403784439,1.,0.866025403784439,
1.,0.866025403784439,1.,0.866025403784439,1.,0.866025403784439,1.,0.866025403784439,
1.,0.866025403784439,1.,0.866025403784439,1.,0.866025403784439,1.,0.866025403784439,
1.,0.866025403784439,1.,0.866025403784439,1.,0.866025403784439,1.,0.866025403784439,
1.,0.866025403784439,1.,0.866025403784439,1.,0.866025403784439,1.,0.866025403784439,
1.,0.866025403784439,1.,0.866025403784439,1.,0.866025403784439,1.,0.866025403784439,
1.,0.866025403784439,1.,0.866025403784439,1.,0.866025403784439,1.,0.866025403784439,
1.,0.866025403784439,1.,0.866025403784439,1.,0.866025403784439,1.,0.866025403784439,
1.,0.866025403784439,1.,0.866025403784439,1.,0.866025403784439,1.,0.866025403784439,
1.,0.866025403784439,1.,0.866025403784439,1.,0.866025403784439,1.,0.866025403784439,
1.,0.866025403784439,1.,0.866025403784439,1.,0.866025403784439,1.,0.866025403784439,
1.,0.866025403784439,1.,0.866025403784439,1.,0.866025403784439,1.,0.866025403784439,
1.,0.866025403784439,1.,0.866025403784439,1.,0.866025403784439,1.,0.866025403784439,
1.,0.866025403784439,1.,0.866025403784439,1.,0.866025403784439,1.,0.866025403784439,
1.,0.866025403784439,1.,0.866025403784439,1.,0.866025403784439,1.,0.866025403784439,
1.,0.866025403784439,1.,0.866025403784439,1.,0.866025403784439,1.,0.866025403784439,
1.,0.866025403784439,1.,0.866025403784439,1.,0.866025403784439,1.,0.866025403784439,
1.,0.866025403784439,1.,0.866025403784439,1.,0.866025403784439,1.,0.866025403784439,
1.,0.866025403784439,1.,0.866025403784439,1.,0.866025403784439,1.,0.866025403784439,
1.,0.866025403784439,1.,0.866025403784439,1.,0.866025403784439,1.,0.866025403784439,
1.,0.866025403784439,1.,0.866025403784439,1.,0.866025403784439,1.,0.866025403784439,
1.,0.866025403784439,1.,0.866025403784439,1.,0.866025403784439,1.,0.866025403784439,
1.,0.866025403784439,1.,0.866025403784439,1.,0.866025403784439,1.,0.866025403784439,
1.,0.866025403784439,1.,0.866025403784439,1.,0.866025403784439,1.,0.866025403784439,
1.,0.866025403784439,1.,0.866025403784439,1.,0.866025403784439,1.,0.866025403784439,
1.,0.866025403784439,1.,0.866025403784439,1.,0.866025403784439,1.)))
REPRESENTATION_ITEM('')
SURFACE()
) ;
#759=(
BOUNDED_SURFACE()
B_SPLINE_SURFACE(1,2,((#84922,#84923,#84924,#84925,#84926,#84927,#84928,
#84929,#84930,#84931,#84932,#84933,#84934,#84935,#84936,#84937,#84938,#84939,
#84940,#84941,#84942,#84943,#84944,#84945,#84946,#84947,#84948,#84949,#84950,
#84951,#84952,#84953,#84954,#84955,#84956,#84957,#84958,#84959,#84960,#84961,
#84962,#84963,#84964,#84965,#84966,#84967,#84968,#84969,#84970,#84971,#84972,
#84973,#84974,#84975,#84976,#84977,#84978,#84979,#84980,#84981,#84982,#84983,
#84984,#84985,#84986,#84987,#84988,#84989,#84990,#84991,#84992,#84993,#84994,
#84995,#84996,#84997,#84998,#84999,#85000,#85001,#85002,#85003,#85004,#85005,
#85006,#85007,#85008,#85009,#85010,#85011,#85012,#85013,#85014,#85015,#85016,
#85017,#85018,#85019,#85020,#85021,#85022,#85023,#85024,#85025,#85026,#85027,
#85028,#85029,#85030,#85031,#85032,#85033,#85034,#85035,#85036,#85037,#85038,
#85039,#85040,#85041,#85042,#85043,#85044,#85045,#85046,#85047,#85048,#85049,
#85050,#85051,#85052,#85053,#85054,#85055,#85056,#85057,#85058,#85059,#85060,
#85061,#85062,#85063,#85064,#85065,#85066,#85067,#85068,#85069,#85070,#85071,
#85072,#85073,#85074,#85075,#85076,#85077,#85078,#85079,#85080,#85081,#85082,
#85083,#85084,#85085,#85086,#85087,#85088,#85089,#85090,#85091,#85092,#85093,
#85094,#85095,#85096,#85097,#85098,#85099,#85100,#85101,#85102,#85103,#85104,
#85105,#85106,#85107,#85108,#85109,#85110,#85111,#85112,#85113,#85114,#85115,
#85116,#85117,#85118,#85119,#85120,#85121,#85122,#85123,#85124,#85125,#85126,
#85127,#85128,#85129,#85130,#85131,#85132,#85133,#85134,#85135,#85136,#85137,
#85138),(#85139,#85140,#85141,#85142,#85143,#85144,#85145,#85146,#85147,
#85148,#85149,#85150,#85151,#85152,#85153,#85154,#85155,#85156,#85157,#85158,
#85159,#85160,#85161,#85162,#85163,#85164,#85165,#85166,#85167,#85168,#85169,
#85170,#85171,#85172,#85173,#85174,#85175,#85176,#85177,#85178,#85179,#85180,
#85181,#85182,#85183,#85184,#85185,#85186,#85187,#85188,#85189,#85190,#85191,
#85192,#85193,#85194,#85195,#85196,#85197,#85198,#85199,#85200,#85201,#85202,
#85203,#85204,#85205,#85206,#85207,#85208,#85209,#85210,#85211,#85212,#85213,
#85214,#85215,#85216,#85217,#85218,#85219,#85220,#85221,#85222,#85223,#85224,
#85225,#85226,#85227,#85228,#85229,#85230,#85231,#85232,#85233,#85234,#85235,
#85236,#85237,#85238,#85239,#85240,#85241,#85242,#85243,#85244,#85245,#85246,
#85247,#85248,#85249,#85250,#85251,#85252,#85253,#85254,#85255,#85256,#85257,
#85258,#85259,#85260,#85261,#85262,#85263,#85264,#85265,#85266,#85267,#85268,
#85269,#85270,#85271,#85272,#85273,#85274,#85275,#85276,#85277,#85278,#85279,
#85280,#85281,#85282,#85283,#85284,#85285,#85286,#85287,#85288,#85289,#85290,
#85291,#85292,#85293,#85294,#85295,#85296,#85297,#85298,#85299,#85300,#85301,
#85302,#85303,#85304,#85305,#85306,#85307,#85308,#85309,#85310,#85311,#85312,
#85313,#85314,#85315,#85316,#85317,#85318,#85319,#85320,#85321,#85322,#85323,
#85324,#85325,#85326,#85327,#85328,#85329,#85330,#85331,#85332,#85333,#85334,
#85335,#85336,#85337,#85338,#85339,#85340,#85341,#85342,#85343,#85344,#85345,
#85346,#85347,#85348,#85349,#85350,#85351,#85352,#85353,#85354,#85355)),
 .UNSPECIFIED.,.F.,.F.,.F.)
B_SPLINE_SURFACE_WITH_KNOTS((2,2),(3,2,2,2,2,2,2,2,2,2,2,2,2,2,2,2,2,2,
2,2,2,2,2,2,2,2,2,2,2,2,2,2,2,2,2,2,2,2,2,2,2,2,2,2,2,2,2,2,2,2,2,2,2,2,
2,2,2,2,2,2,2,2,2,2,2,2,2,2,2,2,2,2,2,2,2,2,2,2,2,2,2,2,2,2,2,2,2,2,2,2,
2,2,2,2,2,2,2,2,2,2,2,2,2,2,2,2,2,2,3),(0.,1.),(0.,0.00925925925925926,
0.0185185185185185,0.0277777777777778,0.037037037037037,0.0462962962962963,
0.0555555555555556,0.0648148148148148,0.0740740740740741,0.0833333333333333,
0.0925925925925926,0.101851851851852,0.111111111111111,0.12037037037037,
0.12962962962963,0.138888888888889,0.148148148148148,0.157407407407407,
0.166666666666667,0.175925925925926,0.185185185185185,0.194444444444444,
0.203703703703704,0.212962962962963,0.222222222222222,0.231481481481481,
0.240740740740741,0.25,0.259259259259259,0.268518518518519,0.277777777777778,
0.287037037037037,0.296296296296296,0.305555555555556,0.314814814814815,
0.324074074074074,0.333333333333333,0.342592592592593,0.351851851851852,
0.361111111111111,0.37037037037037,0.37962962962963,0.388888888888889,0.398148148148148,
0.407407407407407,0.416666666666667,0.425925925925926,0.435185185185185,
0.444444444444444,0.453703703703704,0.462962962962963,0.472222222222222,
0.481481481481481,0.490740740740741,0.5,0.509259259259259,0.518518518518518,
0.527777777777778,0.537037037037037,0.546296296296296,0.555555555555556,
0.564814814814815,0.574074074074074,0.583333333333333,0.592592592592593,
0.601851851851852,0.611111111111111,0.62037037037037,0.62962962962963,0.638888888888889,
0.648148148148148,0.657407407407407,0.666666666666667,0.675925925925926,
0.685185185185185,0.694444444444444,0.703703703703704,0.712962962962963,
0.722222222222222,0.731481481481482,0.740740740740741,0.75,0.759259259259259,
0.768518518518518,0.777777777777778,0.787037037037037,0.796296296296296,
0.805555555555556,0.814814814814815,0.824074074074074,0.833333333333333,
0.842592592592593,0.851851851851852,0.861111111111111,0.87037037037037,
0.87962962962963,0.888888888888889,0.898148148148148,0.907407407407407,
0.916666666666667,0.925925925925926,0.935185185185185,0.944444444444444,
0.953703703703704,0.962962962962963,0.972222222222222,0.981481481481482,
0.990740740740741,1.),.UNSPECIFIED.)
GEOMETRIC_REPRESENTATION_ITEM()
RATIONAL_B_SPLINE_SURFACE(((1.,0.866025403784439,1.,0.866025403784439,1.,
0.866025403784439,1.,0.866025403784439,1.,0.866025403784439,1.,0.866025403784439,
1.,0.866025403784439,1.,0.866025403784439,1.,0.866025403784439,1.,0.866025403784439,
1.,0.866025403784439,1.,0.866025403784439,1.,0.866025403784439,1.,0.866025403784439,
1.,0.866025403784439,1.,0.866025403784439,1.,0.866025403784439,1.,0.866025403784439,
1.,0.866025403784439,1.,0.866025403784439,1.,0.866025403784439,1.,0.866025403784439,
1.,0.866025403784439,1.,0.866025403784439,1.,0.866025403784439,1.,0.866025403784439,
1.,0.866025403784439,1.,0.866025403784439,1.,0.866025403784439,1.,0.866025403784439,
1.,0.866025403784439,1.,0.866025403784439,1.,0.866025403784439,1.,0.866025403784439,
1.,0.866025403784439,1.,0.866025403784439,1.,0.866025403784439,1.,0.866025403784439,
1.,0.866025403784439,1.,0.866025403784439,1.,0.866025403784439,1.,0.866025403784439,
1.,0.866025403784439,1.,0.866025403784439,1.,0.866025403784439,1.,0.866025403784439,
1.,0.866025403784439,1.,0.866025403784439,1.,0.866025403784439,1.,0.866025403784439,
1.,0.866025403784439,1.,0.866025403784439,1.,0.866025403784439,1.,0.866025403784439,
1.,0.866025403784439,1.,0.866025403784439,1.,0.866025403784439,1.,0.866025403784439,
1.,0.866025403784439,1.,0.866025403784439,1.,0.866025403784439,1.,0.866025403784439,
1.,0.866025403784439,1.,0.866025403784439,1.,0.866025403784439,1.,0.866025403784439,
1.,0.866025403784439,1.,0.866025403784439,1.,0.866025403784439,1.,0.866025403784439,
1.,0.866025403784439,1.,0.866025403784439,1.,0.866025403784439,1.,0.866025403784439,
1.,0.866025403784439,1.,0.866025403784439,1.,0.866025403784439,1.,0.866025403784439,
1.,0.866025403784439,1.,0.866025403784439,1.,0.866025403784439,1.,0.866025403784439,
1.,0.866025403784439,1.,0.866025403784439,1.,0.866025403784439,1.,0.866025403784439,
1.,0.866025403784439,1.,0.866025403784439,1.,0.866025403784439,1.,0.866025403784439,
1.,0.866025403784439,1.,0.866025403784439,1.,0.866025403784439,1.,0.866025403784439,
1.,0.866025403784439,1.,0.866025403784439,1.,0.866025403784439,1.,0.866025403784439,
1.,0.866025403784439,1.,0.866025403784439,1.,0.866025403784439,1.,0.866025403784439,
1.,0.866025403784439,1.,0.866025403784439,1.,0.866025403784439,1.,0.866025403784439,
1.,0.866025403784439,1.,0.866025403784439,1.),(1.,0.866025403784439,1.,
0.866025403784439,1.,0.866025403784439,1.,0.866025403784439,1.,0.866025403784439,
1.,0.866025403784439,1.,0.866025403784439,1.,0.866025403784439,1.,0.866025403784439,
1.,0.866025403784439,1.,0.866025403784439,1.,0.866025403784439,1.,0.866025403784439,
1.,0.866025403784439,1.,0.866025403784439,1.,0.866025403784439,1.,0.866025403784439,
1.,0.866025403784439,1.,0.866025403784439,1.,0.866025403784439,1.,0.866025403784439,
1.,0.866025403784439,1.,0.866025403784439,1.,0.866025403784439,1.,0.866025403784439,
1.,0.866025403784439,1.,0.866025403784439,1.,0.866025403784439,1.,0.866025403784439,
1.,0.866025403784439,1.,0.866025403784439,1.,0.866025403784439,1.,0.866025403784439,
1.,0.866025403784439,1.,0.866025403784439,1.,0.866025403784439,1.,0.866025403784439,
1.,0.866025403784439,1.,0.866025403784439,1.,0.866025403784439,1.,0.866025403784439,
1.,0.866025403784439,1.,0.866025403784439,1.,0.866025403784439,1.,0.866025403784439,
1.,0.866025403784439,1.,0.866025403784439,1.,0.866025403784439,1.,0.866025403784439,
1.,0.866025403784439,1.,0.866025403784439,1.,0.866025403784439,1.,0.866025403784439,
1.,0.866025403784439,1.,0.866025403784439,1.,0.866025403784439,1.,0.866025403784439,
1.,0.866025403784439,1.,0.866025403784439,1.,0.866025403784439,1.,0.866025403784439,
1.,0.866025403784439,1.,0.866025403784439,1.,0.866025403784439,1.,0.866025403784439,
1.,0.866025403784439,1.,0.866025403784439,1.,0.866025403784439,1.,0.866025403784439,
1.,0.866025403784439,1.,0.866025403784439,1.,0.866025403784439,1.,0.866025403784439,
1.,0.866025403784439,1.,0.866025403784439,1.,0.866025403784439,1.,0.866025403784439,
1.,0.866025403784439,1.,0.866025403784439,1.,0.866025403784439,1.,0.866025403784439,
1.,0.866025403784439,1.,0.866025403784439,1.,0.866025403784439,1.,0.866025403784439,
1.,0.866025403784439,1.,0.866025403784439,1.,0.866025403784439,1.,0.866025403784439,
1.,0.866025403784439,1.,0.866025403784439,1.,0.866025403784439,1.,0.866025403784439,
1.,0.866025403784439,1.,0.866025403784439,1.,0.866025403784439,1.,0.866025403784439,
1.,0.866025403784439,1.,0.866025403784439,1.,0.866025403784439,1.,0.866025403784439,
1.,0.866025403784439,1.,0.866025403784439,1.,0.866025403784439,1.,0.866025403784439,
1.,0.866025403784439,1.,0.866025403784439,1.,0.866025403784439,1.)))
REPRESENTATION_ITEM('')
SURFACE()
) ;
#760=(
BOUNDED_SURFACE()
B_SPLINE_SURFACE(1,2,((#85356,#85357,#85358,#85359,#85360,#85361,#85362,
#85363,#85364,#85365,#85366,#85367,#85368),(#85369,#85370,#85371,#85372,
#85373,#85374,#85375,#85376,#85377,#85378,#85379,#85380,#85381)),
 .UNSPECIFIED.,.F.,.F.,.F.)
B_SPLINE_SURFACE_WITH_KNOTS((2,2),(3,2,2,2,2,2,3),(0.,1.),(-2.070897694853E-5,
0.166666666666667,0.333333333333333,0.5,0.666666666666667,0.833333333333333,
1.),.UNSPECIFIED.)
GEOMETRIC_REPRESENTATION_ITEM()
RATIONAL_B_SPLINE_SURFACE(((1.00003329785877,0.866008756923491,1.,0.866025403784439,
1.,0.866025403784439,1.,0.866025403784439,1.,0.866025403784439,1.,0.866025403784439,
1.),(1.00003329785877,0.866008756923491,1.,0.866025403784439,1.,0.866025403784439,
1.,0.866025403784439,1.,0.866025403784439,1.,0.866025403784439,1.)))
REPRESENTATION_ITEM('')
SURFACE()
) ;
#805=(
BOUNDED_CURVE()
B_SPLINE_CURVE(2,(#84380,#84381,#84382),.UNSPECIFIED.,.F.,.F.)
B_SPLINE_CURVE_WITH_KNOTS((3,3),(0.144622167450292,0.333975502520127),
 .UNSPECIFIED.)
CURVE()
GEOMETRIC_REPRESENTATION_ITEM()
RATIONAL_B_SPLINE_CURVE((1.05123113411618,1.06704736773796,1.03645650657006))
REPRESENTATION_ITEM('')
) ;
#806=(
BOUNDED_CURVE()
B_SPLINE_CURVE(2,(#84385,#84386,#84387),.UNSPECIFIED.,.F.,.F.)
B_SPLINE_CURVE_WITH_KNOTS((3,3),(-0.273691078067528,-0.0843377429954669),
 .UNSPECIFIED.)
CURVE()
GEOMETRIC_REPRESENTATION_ITEM()
RATIONAL_B_SPLINE_CURVE((1.05123113407425,1.06704736768547,1.03645650654287))
REPRESENTATION_ITEM('')
) ;
#807=(
BOUNDED_CURVE()
B_SPLINE_CURVE(2,(#84393,#84394,#84395),.UNSPECIFIED.,.F.,.F.)
B_SPLINE_CURVE_WITH_KNOTS((3,3),(0.14462216745017,0.333975502519992),
 .UNSPECIFIED.)
CURVE()
GEOMETRIC_REPRESENTATION_ITEM()
RATIONAL_B_SPLINE_CURVE((1.05123113411541,1.06704736773698,1.03645650656957))
REPRESENTATION_ITEM('')
) ;
#808=(
BOUNDED_CURVE()
B_SPLINE_CURVE(2,(#84398,#84399,#84400),.UNSPECIFIED.,.F.,.F.)
B_SPLINE_CURVE_WITH_KNOTS((3,3),(-0.273691078054969,-0.0843377429828408),
 .UNSPECIFIED.)
CURVE()
GEOMETRIC_REPRESENTATION_ITEM()
RATIONAL_B_SPLINE_CURVE((1.0512311341411,1.06704736776924,1.03645650658487))
REPRESENTATION_ITEM('')
) ;
#809=(
BOUNDED_CURVE()
B_SPLINE_CURVE(2,(#85385,#85386,#85387),.UNSPECIFIED.,.F.,.F.)
B_SPLINE_CURVE_WITH_KNOTS((3,3),(-0.273691078066784,-0.0843377429945845),
 .UNSPECIFIED.)
CURVE()
GEOMETRIC_REPRESENTATION_ITEM()
RATIONAL_B_SPLINE_CURVE((1.05123113407905,1.06704736769164,1.03645650654597))
REPRESENTATION_ITEM('')
) ;
#810=(
BOUNDED_CURVE()
B_SPLINE_CURVE(2,(#85390,#85391,#85392),.UNSPECIFIED.,.F.,.F.)
B_SPLINE_CURVE_WITH_KNOTS((3,3),(0.144622167447006,0.333975502516735),
 .UNSPECIFIED.)
CURVE()
GEOMETRIC_REPRESENTATION_ITEM()
RATIONAL_B_SPLINE_CURVE((1.05123113409603,1.06704736771258,1.03645650655733))
REPRESENTATION_ITEM('')
) ;
#811=(
BOUNDED_CURVE()
B_SPLINE_CURVE(2,(#85446,#85447,#85448),.UNSPECIFIED.,.F.,.F.)
B_SPLINE_CURVE_WITH_KNOTS((3,3),(0.144622167449308,0.333975502519229),
 .UNSPECIFIED.)
CURVE()
GEOMETRIC_REPRESENTATION_ITEM()
RATIONAL_B_SPLINE_CURVE((1.05123113411181,1.06704736773254,1.03645650656736))
REPRESENTATION_ITEM('')
) ;
#812=(
BOUNDED_CURVE()
B_SPLINE_CURVE(2,(#85450,#85451,#85452),.UNSPECIFIED.,.F.,.F.)
B_SPLINE_CURVE_WITH_KNOTS((3,3),(0.14462216745368,0.333975502523465),
 .UNSPECIFIED.)
CURVE()
GEOMETRIC_REPRESENTATION_ITEM()
RATIONAL_B_SPLINE_CURVE((1.05123113413176,1.06704736775736,1.03645650657979))
REPRESENTATION_ITEM('')
) ;
#823=SHAPE_REPRESENTATION_RELATIONSHIP('SRR','None',#86473,#835) ;
#835=ADVANCED_BREP_SHAPE_REPRESENTATION('',(#859),#86327) ;
#847=STYLED_ITEM('',(#86582),#859) ;
#859=MANIFOLD_SOLID_BREP('Body1',#32646) ;
#897=CONICAL_SURFACE('',#36415,4.35024047358084,0.785398163397443) ;
#898=CONICAL_SURFACE('',#36417,4.35024047358084,0.785398163397443) ;
#899=CONICAL_SURFACE('',#36423,1.5,0.26179938779915) ;
#900=CONICAL_SURFACE('',#36426,1.5,0.26179938779915) ;
#901=CONICAL_SURFACE('',#36461,1.5,0.26179938779915) ;
#902=CONICAL_SURFACE('',#36477,1.5,0.26179938779915) ;
#1185=FACE_BOUND('',#6193,.T.) ;
#1186=FACE_BOUND('',#6197,.T.) ;
#1630=B_SPLINE_CURVE_WITH_KNOTS('',3,(#81802,#81803,#81804,#81805,#81806,
#81807,#81808,#81809,#81810,#81811,#81812,#81813,#81814,#81815,#81816,#81817,
#81818,#81819,#81820,#81821,#81822,#81823,#81824,#81825),.UNSPECIFIED.,
 .F.,.F.,(4,2,2,2,2,2,2,2,2,2,2,4),(13.8867005186057,13.9350474908693,13.9924855972126,
14.0524156344104,14.1100718512641,14.16910817166,14.2282720252749,14.2852973565917,
14.3449598229184,14.4034785115834,14.4576795870239,14.5137172238172),
 .UNSPECIFIED.) ;
#1631=B_SPLINE_CURVE_WITH_KNOTS('',3,(#81828,#81829,#81830,#81831,#81832,
#81833,#81834,#81835,#81836,#81837,#81838,#81839,#81840,#81841,#81842,#81843,
#81844,#81845,#81846,#81847,#81848,#81849),.UNSPECIFIED.,.F.,.F.,(4,2,2,
2,2,2,2,2,2,2,4),(9.99999999983386E-7,0.0304626053349231,0.0610090759544533,
0.120167775309188,0.177705880467965,0.237495432414644,0.295507829943808,
0.353719522676528,0.41351508898739,0.47065222200038,0.508205581620669),
 .UNSPECIFIED.) ;
#1632=B_SPLINE_CURVE_WITH_KNOTS('',3,(#81854,#81855,#81856,#81857,#81858,
#81859,#81860,#81861,#81862,#81863,#81864,#81865,#81866,#81867,#81868,#81869,
#81870,#81871,#81872,#81873,#81874,#81875,#81876,#81877,#81878,#81879,#81880,
#81881,#81882,#81883,#81884,#81885,#81886,#81887,#81888,#81889),
 .UNSPECIFIED.,.F.,.F.,(4,2,2,2,2,2,2,2,2,2,2,2,2,2,2,2,2,4),(12.9412330053418,
12.998236214922,13.0563572589213,13.1159524118842,13.1733090635897,13.2329612974308,
13.2917792811559,13.3487577815587,13.4084196690731,13.4665880264056,13.5243074655242,
13.584060767217,13.6415584764723,13.7011457577954,13.7601194030082,13.8170733726563,
13.8767213491233,13.8867005186057),.UNSPECIFIED.) ;
#1633=B_SPLINE_CURVE_WITH_KNOTS('',3,(#81890,#81891,#81892,#81893,#81894,
#81895,#81896,#81897,#81898,#81899,#81900,#81901,#81902,#81903,#81904,#81905,
#81906,#81907,#81908,#81909,#81910,#81911,#81912,#81913,#81914,#81915,#81916,
#81917,#81918,#81919,#81920,#81921,#81922,#81923,#81924,#81925),
 .UNSPECIFIED.,.F.,.F.,(4,2,2,2,2,2,2,2,2,2,2,2,2,2,2,2,2,4),(0.508205581620669,
0.529516158689829,0.589294709689451,0.64670174785647,0.706343830502454,
0.764822728260175,0.822910164017873,0.883310219729821,0.940608465203719,
0.999371393345501,1.0591764292834,1.11640397895033,1.17581182275485,1.23468547612338,
1.29256543862931,1.35273576560654,1.41016590071693,1.45610265637391),
 .UNSPECIFIED.) ;
#1634=B_SPLINE_CURVE_WITH_KNOTS('',3,(#81930,#81931,#81932,#81933,#81934,
#81935,#81936,#81937,#81938,#81939,#81940,#81941,#81942,#81943,#81944,#81945,
#81946,#81947,#81948,#81949,#81950,#81951,#81952,#81953,#81954,#81955,#81956,
#81957,#81958,#81959,#81960,#81961,#81962,#81963,#81964,#81965,#81966,#81967),
 .UNSPECIFIED.,.F.,.F.,(4,2,2,2,2,2,2,2,2,2,2,2,2,2,2,2,2,2,4),(11.9961952508726,
12.0042837462161,12.0618845196288,12.1208623533056,12.1799693778926,12.2369397423948,
12.2965444576751,12.3550069487343,12.4121989388398,12.4722827355704,12.5300739275151,
12.5885939955338,12.6479201143845,12.7050601300443,12.7647104833383,12.8233948532171,
12.880498390127,12.9402044488287,12.9412330053418),.UNSPECIFIED.) ;
#1635=B_SPLINE_CURVE_WITH_KNOTS('',3,(#81968,#81969,#81970,#81971,#81972,
#81973,#81974,#81975,#81976,#81977,#81978,#81979,#81980,#81981,#81982,#81983,
#81984,#81985,#81986,#81987,#81988,#81989,#81990,#81991,#81992,#81993,#81994,
#81995,#81996,#81997,#81998,#81999,#82000,#82001,#82002,#82003),
 .UNSPECIFIED.,.F.,.F.,(4,2,2,2,2,2,2,2,2,2,2,2,2,2,2,2,2,4),(1.45610265637391,
1.46871800860693,1.52849061803271,1.58558862544678,1.64478817475386,1.70416297781245,
1.76186476207488,1.82183697097415,1.879497358742,1.93787034129416,1.99764047850571,
2.0547078195011,2.11373042452122,2.17368686543178,2.23124440123845,2.29105539109935,
2.34902981745396,2.40334819810103),.UNSPECIFIED.) ;
#1636=B_SPLINE_CURVE_WITH_KNOTS('',3,(#82008,#82009,#82010,#82011,#82012,
#82013,#82014,#82015,#82016,#82017,#82018,#82019,#82020,#82021,#82022,#82023,
#82024,#82025,#82026,#82027,#82028,#82029,#82030,#82031,#82032,#82033,#82034,
#82035,#82036,#82037,#82038,#82039,#82040,#82041,#82042,#82043),
 .UNSPECIFIED.,.F.,.F.,(4,2,2,2,2,2,2,2,2,2,2,2,2,2,2,2,2,4),(11.0517238864306,
11.0681655496399,11.1254856558836,11.1856249155873,11.2443861394716,11.3013091538836,
11.3609130535846,11.4190252875331,11.4766878949276,11.5363835817554,11.593825824283,
11.6533537955196,11.7122706230244,11.769169357543,11.8287594281516,11.8870294631155,
11.9444113071521,11.9961952508726),.UNSPECIFIED.) ;
#1637=B_SPLINE_CURVE_WITH_KNOTS('',3,(#82044,#82045,#82046,#82047,#82048,
#82049,#82050,#82051,#82052,#82053,#82054,#82055,#82056,#82057,#82058,#82059,
#82060,#82061,#82062,#82063,#82064,#82065,#82066,#82067,#82068,#82069,#82070,
#82071,#82072,#82073,#82074,#82075,#82076,#82077,#82078,#82079,#82080,#82081),
 .UNSPECIFIED.,.F.,.F.,(4,2,2,2,2,2,2,2,2,2,2,2,2,2,2,2,2,2,4),(2.40334819810103,
2.4072605468042,2.46705591833339,2.52418455061912,2.58306722119116,2.64284703329508,
2.7002709712672,2.75993178087289,2.81835849049791,2.87646189303058,2.93688032948389,
2.99415810892388,3.05293740878363,3.11273682802953,3.16997581814349,3.22939954900085,
3.28820658472353,3.34609923977367,3.35114202110295),.UNSPECIFIED.) ;
#1638=B_SPLINE_CURVE_WITH_KNOTS('',3,(#82086,#82087,#82088,#82089,#82090,
#82091,#82092,#82093,#82094,#82095,#82096,#82097,#82098,#82099,#82100,#82101,
#82102,#82103,#82104,#82105,#82106,#82107,#82108,#82109,#82110,#82111,#82112,
#82113,#82114,#82115,#82116,#82117,#82118,#82119,#82120,#82121),
 .UNSPECIFIED.,.F.,.F.,(4,2,2,2,2,2,2,2,2,2,2,2,2,2,2,2,2,4),(10.1061328943984,
10.1319344713036,10.1889836828643,10.248657015031,10.3072111047501,10.3644467073206,
10.4246264128683,10.4825080245906,10.5410374571557,10.6004592838386,10.6576583140244,
10.7172803345211,10.7759257359241,10.8329561804325,10.8926005512979,10.9505943726261,
11.0086070054143,11.0517238864306),.UNSPECIFIED.) ;
#1639=B_SPLINE_CURVE_WITH_KNOTS('',3,(#82122,#82123,#82124,#82125,#82126,
#82127,#82128,#82129,#82130,#82131,#82132,#82133,#82134,#82135,#82136,#82137,
#82138,#82139,#82140,#82141,#82142,#82143,#82144,#82145,#82146,#82147,#82148,
#82149,#82150,#82151,#82152,#82153,#82154,#82155,#82156,#82157),
 .UNSPECIFIED.,.F.,.F.,(4,2,2,2,2,2,2,2,2,2,2,2,2,2,2,2,2,4),(3.35114202110295,
3.40628444731813,3.46368137332275,3.52224634036856,3.58200944812486,3.63910679195477,
3.6983187890776,3.75761489908632,3.81532554132471,3.87530847359802,3.93292407555114,
3.99130574702326,4.05106281670436,4.10811742404662,4.16714832201972,4.22701774069037,
4.28457972163558,4.2982223769055),.UNSPECIFIED.) ;
#1640=B_SPLINE_CURVE_WITH_KNOTS('',3,(#82162,#82163,#82164,#82165,#82166,
#82167,#82168,#82169,#82170,#82171,#82172,#82173,#82174,#82175,#82176,#82177,
#82178,#82179,#82180,#82181,#82182,#82183,#82184,#82185,#82186,#82187,#82188,
#82189,#82190,#82191,#82192,#82193,#82194,#82195,#82196,#82197),
 .UNSPECIFIED.,.F.,.F.,(4,2,2,2,2,2,2,2,2,2,2,2,2,2,2,2,2,4),(9.16068336219022,
9.19538360180203,9.25235946726598,9.31202418801378,9.37021833087523,9.4279003321042,
9.48768220706314,9.54520591189467,9.60471899739655,9.66372331785842,9.72068736339293,
9.78034198576824,9.83869910931437,9.89611140398129,9.95607523366671,10.013762247429,
10.0727354918934,10.1061328943984),.UNSPECIFIED.) ;
#1641=B_SPLINE_CURVE_WITH_KNOTS('',3,(#82198,#82199,#82200,#82201,#82202,
#82203,#82204,#82205,#82206,#82207,#82208,#82209,#82210,#82211,#82212,#82213,
#82214,#82215,#82216,#82217,#82218,#82219,#82220,#82221,#82222,#82223,#82224,
#82225,#82226,#82227,#82228,#82229,#82230,#82231,#82232,#82233),
 .UNSPECIFIED.,.F.,.F.,(4,2,2,2,2,2,2,2,2,2,2,2,2,2,2,2,2,4),(4.2982223769055,
4.34439663186739,4.40231707582145,4.46055170597777,4.52033067706177,4.57743592485621,
4.63632205749593,4.69608715005503,4.75351317167067,4.81317737256235,4.87153538562735,
4.92963978294915,4.99006111696204,5.04730335700837,5.10608391044735,5.16586145253212,
5.22309807562595,5.2457892592979),.UNSPECIFIED.) ;
#1642=B_SPLINE_CURVE_WITH_KNOTS('',3,(#82238,#82239,#82240,#82241,#82242,
#82243,#82244,#82245,#82246,#82247,#82248,#82249,#82250,#82251,#82252,#82253,
#82254,#82255,#82256,#82257,#82258,#82259,#82260,#82261,#82262,#82263,#82264,
#82265,#82266,#82267,#82268,#82269,#82270,#82271,#82272,#82273),
 .UNSPECIFIED.,.F.,.F.,(4,2,2,2,2,2,2,2,2,2,2,2,2,2,2,2,2,4),(8.21436505857019,
8.25733956019176,8.31460502469798,8.37486191077879,8.43281602299387,8.4913430031965,
8.55084190230918,8.60811398753954,8.66779474291512,8.72651665970665,8.78358981574751,
8.84329151668778,8.90136153830009,8.9593861037039,9.01902504997052,9.07642130387137,
9.13654008132794,9.16068336219022),.UNSPECIFIED.) ;
#1643=B_SPLINE_CURVE_WITH_KNOTS('',3,(#82274,#82275,#82276,#82277,#82278,
#82279,#82280,#82281,#82282,#82283,#82284,#82285,#82286,#82287,#82288,#82289,
#82290,#82291,#82292,#82293,#82294,#82295,#82296,#82297,#82298,#82299,#82300,
#82301,#82302,#82303,#82304,#82305,#82306,#82307,#82308,#82309),
 .UNSPECIFIED.,.F.,.F.,(4,2,2,2,2,2,2,2,2,2,2,2,2,2,2,2,2,4),(5.2457892592979,
5.28252236343818,5.34124533948901,5.39913569519271,5.45932029051008,5.51666828733251,
5.57523098093596,5.63496811679614,5.69205059527559,5.75125970307787,5.8104586001455,
5.86816306502341,5.92814118700423,5.98569549667876,6.04407067666668,6.10379801346566,
6.16082506805814,6.19252875602354),.UNSPECIFIED.) ;
#1644=B_SPLINE_CURVE_WITH_KNOTS('',3,(#82314,#82315,#82316,#82317,#82318,
#82319,#82320,#82321,#82322,#82323,#82324,#82325,#82326,#82327,#82328,#82329,
#82330,#82331,#82332,#82333,#82334,#82335,#82336,#82337,#82338,#82339,#82340,
#82341,#82342,#82343,#82344,#82345,#82346,#82347,#82348,#82349),
 .UNSPECIFIED.,.F.,.F.,(4,2,2,2,2,2,2,2,2,2,2,2,2,2,2,2,2,4),(7.26810373508885,
7.31959226080252,7.37728070535416,7.43713087514446,7.49471888210049,7.55420561942568,
7.61327955037669,7.67029385961975,7.72999626093379,7.78842276307307,7.84585231980428,
7.90588921391058,7.96364491307247,8.02260214152301,8.08187479149579,8.13898700097499,
8.19871197935205,8.21436505857019),.UNSPECIFIED.) ;
#1645=B_SPLINE_CURVE_WITH_KNOTS('',3,(#82350,#82351,#82352,#82353,#82354,
#82355,#82356,#82357,#82358,#82359,#82360,#82361,#82362,#82363,#82364,#82365,
#82366,#82367,#82368,#82369,#82370,#82371,#82372,#82373,#82374,#82375,#82376,
#82377,#82378,#82379,#82380,#82381,#82382,#82383,#82384,#82385),
 .UNSPECIFIED.,.F.,.F.,(4,2,2,2,2,2,2,2,2,2,2,2,2,2,2,2,2,4),(6.19252875602354,
6.21984888247365,6.2796116781406,6.33716298617571,6.39697019465541,6.45481923300649,
6.51304248460271,6.57278820928456,6.62985451075959,6.68872863482653,6.74846230883204,
6.80587530622558,6.86552729196779,6.92379822165874,6.98188832681,7.04229679654806,
7.09948736675755,7.13949123074078),.UNSPECIFIED.) ;
#1646=B_SPLINE_CURVE_WITH_KNOTS('',3,(#82390,#82391,#82392,#82393,#82394,
#82395,#82396,#82397,#82398,#82399,#82400,#82401,#82402,#82403,#82404,#82405,
#82406,#82407,#82408,#82409,#82410,#82411,#82412,#82413,#82414,#82415,#82416,
#82417,#82418,#82419,#82420,#82421,#82422,#82423,#82424,#82425,#82426,#82427),
 .UNSPECIFIED.,.F.,.F.,(4,2,2,2,2,2,2,2,2,2,2,2,2,2,2,2,2,2,4),(6.32170606963374,
6.32400468955437,6.38370211924148,6.44076735369172,6.4994918136059,6.55916879534269,
6.61644284739015,6.67594418833338,6.73444756181926,6.79240320162889,6.85266228462122,
6.90991547332821,6.9685446550446,7.02826345535349,7.08537458801367,7.14464864112866,
7.20357745851197,7.26133349550517,7.26810373508885),.UNSPECIFIED.) ;
#1647=B_SPLINE_CURVE_WITH_KNOTS('',3,(#82428,#82429,#82430,#82431,#82432,
#82433,#82434,#82435,#82436,#82437,#82438,#82439,#82440,#82441,#82442,#82443,
#82444,#82445,#82446,#82447,#82448,#82449,#82450,#82451,#82452,#82453,#82454,
#82455,#82456,#82457,#82458,#82459,#82460,#82461,#82462,#82463),
 .UNSPECIFIED.,.F.,.F.,(4,2,2,2,2,2,2,2,2,2,2,2,2,2,2,2,2,4),(7.13949123074078,
7.15825374460888,7.2179922538912,7.27521247887906,7.33403878159532,7.39109870458423,
7.45082647635778,7.50900171095632,7.56689066611655,7.62664565486306,7.68414864972785,
7.7440004506624,7.80296907884385,7.85997329598635,7.9196775938442,7.9779974472315,
8.03557740903284,8.08585791009537),.UNSPECIFIED.) ;
#1648=B_SPLINE_CURVE_WITH_KNOTS('',3,(#82468,#82469,#82470,#82471,#82472,
#82473,#82474,#82475,#82476,#82477,#82478,#82479,#82480,#82481,#82482,#82483,
#82484,#82485,#82486,#82487,#82488,#82489,#82490,#82491,#82492,#82493,#82494,
#82495,#82496,#82497,#82498,#82499,#82500,#82501,#82502,#82503),
 .UNSPECIFIED.,.F.,.F.,(4,2,2,2,2,2,2,2,2,2,2,2,2,2,2,2,2,4),(5.37622687183942,
5.38702250960326,5.44667528576275,5.50363907047652,5.56264942463801,5.62213453916844,
5.67966286689129,5.73945005988841,5.79711619501117,5.85531485867278,5.91497648508351,
5.97194790610636,6.03079582310035,6.09088439256072,6.14828357290543,6.20792599150807,
6.26593197674811,6.32170606963374),.UNSPECIFIED.) ;
#1649=B_SPLINE_CURVE_WITH_KNOTS('',3,(#82504,#82505,#82506,#82507,#82508,
#82509,#82510,#82511,#82512,#82513,#82514,#82515,#82516,#82517,#82518,#82519,
#82520,#82521,#82522,#82523,#82524,#82525,#82526,#82527,#82528,#82529,#82530,
#82531,#82532,#82533,#82534,#82535,#82536,#82537,#82538,#82539),
 .UNSPECIFIED.,.F.,.F.,(4,2,2,2,2,2,2,2,2,2,2,2,2,2,2,2,2,4),(8.08585791009537,
8.09549597218786,8.15314538334764,8.21242039989169,8.27156797612537,8.32860911320981,
8.38831773648552,8.44681872385912,8.50417468441307,8.56429334890911,8.62212277167029,
8.68090338297569,8.74026085247203,8.79743772848003,8.85718076728487,8.91589420882259,
8.97312504989025,9.032439876577),.UNSPECIFIED.) ;
#1650=B_SPLINE_CURVE_WITH_KNOTS('',3,(#82544,#82545,#82546,#82547,#82548,
#82549,#82550,#82551,#82552,#82553,#82554,#82555,#82556,#82557,#82558,#82559,
#82560,#82561,#82562,#82563,#82564,#82565,#82566,#82567,#82568,#82569,#82570,
#82571,#82572,#82573,#82574,#82575,#82576,#82577,#82578,#82579),
 .UNSPECIFIED.,.F.,.F.,(4,2,2,2,2,2,2,2,2,2,2,2,2,2,2,2,2,4),(4.43047895939197,
4.45007522884968,4.50969926510265,4.5669061270457,4.62633650352384,4.68484659374169,
4.74273561983522,4.80292366691765,4.86015173224413,4.9187133717519,4.97838620834566,
5.03543961578679,5.09464600810578,5.15359503132235,5.21128816879447,5.27125894855187,
5.3286592324085,5.37622687183942),.UNSPECIFIED.) ;
#1651=B_SPLINE_CURVE_WITH_KNOTS('',3,(#82580,#82581,#82582,#82583,#82584,
#82585,#82586,#82587,#82588,#82589,#82590,#82591,#82592,#82593,#82594,#82595,
#82596,#82597,#82598,#82599,#82600,#82601,#82602,#82603,#82604,#82605,#82606,
#82607,#82608,#82609,#82610,#82611,#82612,#82613,#82614,#82615,#82616,#82617),
 .UNSPECIFIED.,.F.,.F.,(4,2,2,2,2,2,2,2,2,2,2,2,2,2,2,2,2,2,4),(9.032439876577,
9.03347505180903,9.09151345897655,9.1499072073473,9.20950017382282,9.26685935009706,
9.32657952091107,9.38539515694615,9.44247136996037,9.50220784047952,9.56037205525028,
9.61830724947866,9.67804902641785,9.73554052963516,9.79547082649963,9.85442397084414,
9.91143409586645,9.97114381916621,9.97904550765146),.UNSPECIFIED.) ;
#1652=B_SPLINE_CURVE_WITH_KNOTS('',3,(#82622,#82623,#82624,#82625,#82626,
#82627,#82628,#82629,#82630,#82631,#82632,#82633,#82634,#82635,#82636,#82637,
#82638,#82639,#82640,#82641,#82642,#82643,#82644,#82645,#82646,#82647,#82648,
#82649,#82650,#82651,#82652,#82653,#82654,#82655,#82656,#82657),
 .UNSPECIFIED.,.F.,.F.,(4,2,2,2,2,2,2,2,2,2,2,2,2,2,2,2,2,4),(3.48575023797641,
3.51399594028383,3.5734997701978,3.63095276691785,3.69066016886127,3.74831136852578,
3.80643429791633,3.86604096895959,3.92296464805189,3.98173649994462,4.04184951588525,
4.09917852154368,4.15874676311374,4.21674528680338,4.27474780856614,4.33439370231729,
4.39142122162925,4.43047895939197),.UNSPECIFIED.) ;
#1653=B_SPLINE_CURVE_WITH_KNOTS('',3,(#82658,#82659,#82660,#82661,#82662,
#82663,#82664,#82665,#82666,#82667,#82668,#82669,#82670,#82671,#82672,#82673,
#82674,#82675,#82676,#82677,#82678,#82679,#82680,#82681,#82682,#82683,#82684,
#82685,#82686,#82687,#82688,#82689,#82690,#82691,#82692,#82693),
 .UNSPECIFIED.,.F.,.F.,(4,2,2,2,2,2,2,2,2,2,2,2,2,2,2,2,2,4),(9.97904550765146,
10.0294478805367,10.0870653156411,10.1469658748943,10.2045993921111,10.2639450069181,
10.3230729369084,10.3801081197963,10.4398186669585,10.4982996881472,10.5556817539635,
10.6157782501837,10.6735879401908,10.7324274869952,10.7917618523947,10.8489207802873,
10.908661926968,10.9254729108197),.UNSPECIFIED.) ;
#1654=B_SPLINE_CURVE_WITH_KNOTS('',3,(#82698,#82699,#82700,#82701,#82702,
#82703,#82704,#82705,#82706,#82707,#82708,#82709,#82710,#82711,#82712,#82713,
#82714,#82715,#82716,#82717,#82718,#82719,#82720,#82721,#82722,#82723,#82724,
#82725,#82726,#82727,#82728,#82729,#82730,#82731,#82732,#82733),
 .UNSPECIFIED.,.F.,.F.,(4,2,2,2,2,2,2,2,2,2,2,2,2,2,2,2,2,4),(2.5410263785329,
2.57866932478977,2.63717406289675,2.69497909645909,2.75507795688919,2.81226721150962,
2.87074374700886,2.93035398974217,2.98733419714063,3.04645519099512,3.10541264329701,
3.16302582590397,3.22291178102946,3.28028618337226,3.33856871206754,3.39816287801024,
3.45506667880724,3.48575023797641),.UNSPECIFIED.) ;
#1655=B_SPLINE_CURVE_WITH_KNOTS('',3,(#82734,#82735,#82736,#82737,#82738,
#82739,#82740,#82741,#82742,#82743,#82744,#82745,#82746,#82747,#82748,#82749,
#82750,#82751,#82752,#82753,#82754,#82755,#82756,#82757,#82758,#82759,#82760,
#82761,#82762,#82763,#82764,#82765,#82766,#82767,#82768,#82769),
 .UNSPECIFIED.,.F.,.F.,(4,2,2,2,2,2,2,2,2,2,2,2,2,2,2,2,2,4),(10.9254729108197,
10.9673518741525,11.0245962962134,11.0849206118767,11.1429360001134,11.2013745918176,
11.2609415930954,11.3182768845568,11.3779883710219,11.436778174129,11.4938561844441,
11.5535855030256,11.6117237029001,11.6696898328819,11.7294030058459,11.7868681658494,
11.846860602723,11.8722070730006),.UNSPECIFIED.) ;
#1656=B_SPLINE_CURVE_WITH_KNOTS('',3,(#82774,#82775,#82776,#82777,#82778,
#82779,#82780,#82781,#82782,#82783,#82784,#82785,#82786,#82787,#82788,#82789,
#82790,#82791,#82792,#82793,#82794,#82795,#82796,#82797,#82798,#82799,#82800,
#82801,#82802,#82803,#82804,#82805,#82806,#82807,#82808,#82809),
 .UNSPECIFIED.,.F.,.F.,(4,2,2,2,2,2,2,2,2,2,2,2,2,2,2,2,2,4),(1.59524381008426,
1.64219928555692,1.69995479960911,1.75811654543929,1.81778735648274,1.87477859220045,
1.93359025056505,1.99385447979138,2.05122669579738,2.1108385062818,2.16894963367187,
2.22699679299248,2.2867105859981,2.34381635052473,2.40251607132118,2.46217352123779,
2.51932796376252,2.5410263785329),.UNSPECIFIED.) ;
#1657=B_SPLINE_CURVE_WITH_KNOTS('',3,(#82810,#82811,#82812,#82813,#82814,
#82815,#82816,#82817,#82818,#82819,#82820,#82821,#82822,#82823,#82824,#82825,
#82826,#82827,#82828,#82829,#82830,#82831,#82832,#82833,#82834,#82835,#82836,
#82837,#82838,#82839,#82840,#82841,#82842,#82843,#82844,#82845),
 .UNSPECIFIED.,.F.,.F.,(4,2,2,2,2,2,2,2,2,2,2,2,2,2,2,2,2,4),(11.8722070730006,
11.9057830423993,11.9627849572883,12.0224843188238,12.080757543489,12.1383977592506,
12.1982648617393,12.2558675785037,12.3152681844023,12.3743611588062,12.4313765000627,
12.4910732525112,12.5495191814863,12.6069130219924,12.6669718088517,12.7247467828119,
12.783630310924,12.8183169223007),.UNSPECIFIED.) ;
#1658=B_SPLINE_CURVE_WITH_KNOTS('',3,(#82850,#82851,#82852,#82853,#82854,
#82855,#82856,#82857,#82858,#82859,#82860,#82861,#82862,#82863,#82864,#82865,
#82866,#82867,#82868,#82869,#82870,#82871,#82872,#82873,#82874,#82875,#82876,
#82877,#82878,#82879,#82880,#82881,#82882,#82883,#82884,#82885),
 .UNSPECIFIED.,.F.,.F.,(4,2,2,2,2,2,2,2,2,2,2,2,2,2,2,2,2,4),(0.649736777376371,
0.705689678240313,0.762957073707775,0.821462804205472,0.88112900735365,
0.938149594548792,0.9973007844438,1.0563910421508,1.11403726413225,1.17395573242052,
1.23142244431764,1.28973859070027,1.34939294812008,1.40635125485932,1.46531509515816,
1.52496337930765,1.58245418488598,1.59524381008426),.UNSPECIFIED.) ;
#1659=B_SPLINE_CURVE_WITH_KNOTS('',3,(#82886,#82887,#82888,#82889,#82890,
#82891,#82892,#82893,#82894,#82895,#82896,#82897,#82898,#82899,#82900,#82901,
#82902,#82903,#82904,#82905,#82906,#82907,#82908,#82909,#82910,#82911,#82912,
#82913,#82914,#82915,#82916,#82917,#82918,#82919,#82920,#82921),
 .UNSPECIFIED.,.F.,.F.,(4,2,2,2,2,2,2,2,2,2,2,2,2,2,2,2,2,4),(12.8183169223007,
12.8429261623028,12.9000532843054,12.9597768932427,13.0184281247438,13.0756720407192,
13.1359550292795,13.1939323314564,13.2524012731139,13.3119268030521,13.3692232666448,
13.4289104836939,13.4876590852451,13.5447247490731,13.6044312671098,13.6625282462393,
13.7205109861668,13.764829475703),.UNSPECIFIED.) ;
#1660=B_SPLINE_CURVE_WITH_KNOTS('',3,(#82927,#82928,#82929,#82930,#82931,
#82932,#82933,#82934,#82935,#82936,#82937,#82938,#82939,#82940,#82941,#82942,
#82943,#82944,#82945,#82946,#82947,#82948,#82949,#82950,#82951,#82952,#82953,
#82954,#82955,#82956,#82957,#82958),.UNSPECIFIED.,.F.,.F.,(4,2,2,2,2,2,
2,2,2,2,2,2,2,2,2,4),(-0.604482102223105,-0.604472052630673,-0.558816604903575,
-0.512995341988544,-0.466125939830108,-0.421016120560909,-0.374090744720571,
-0.327859265800465,-0.283024906762521,-0.23608761475075,-0.190362394357742,
-0.144876688170418,-0.0979214349660129,-0.0527340847053595,-0.0268491614321842,
-9.99999981043942E-7),.UNSPECIFIED.) ;
#1661=B_SPLINE_CURVE_WITH_KNOTS('',3,(#82962,#82963,#82964,#82965,#82966,
#82967,#82968,#82969,#82970,#82971,#82972,#82973,#82974,#82975,#82976,#82977,
#82978,#82979,#82980,#82981,#82982,#82983,#82984,#82985,#82986,#82987,#82988,
#82989,#82990,#82991,#82992,#82993,#82994,#82995,#82996,#82997,#82998,#82999,
#83000,#83001,#83002,#83003,#83004,#83005,#83006,#83007,#83008,#83009,#83010,
#83011,#83012,#83013,#83014,#83015,#83016,#83017,#83018,#83019,#83020,#83021,
#83022,#83023,#83024,#83025,#83026,#83027,#83028,#83029,#83030,#83031,#83032,
#83033,#83034,#83035,#83036,#83037,#83038,#83039,#83040,#83041,#83042,#83043,
#83044,#83045,#83046,#83047,#83048,#83049,#83050,#83051,#83052,#83053,#83054,
#83055,#83056,#83057,#83058),.UNSPECIFIED.,.F.,.F.,(4,3,3,3,3,3,3,3,3,3,
3,3,3,3,3,3,3,3,3,3,3,3,3,3,3,3,3,3,3,3,3,3,4),(0.,0.0325197560323793,0.0361754347737445,
0.0545181792551618,0.0665073209256394,0.0701985195194899,0.0715839281444508,
0.0766179496429377,0.0876742174549116,0.0986799106067661,0.109623686050927,
0.117049763338473,0.128531172361757,0.151540610100312,0.160999394201887,
0.165201627662936,0.175477096788014,0.185820644734618,0.196164192681223,
0.200180615978208,0.204045205104025,0.206337708125956,0.208347839550571,
0.224387966023407,0.244962280061539,0.253570253824267,0.257129272275443,
0.282960548052419,0.285773414391098,0.289578563004044,0.292679154477924,
0.309399625992716,0.323847468004356),.UNSPECIFIED.) ;
#1662=B_SPLINE_CURVE_WITH_KNOTS('',3,(#83059,#83060,#83061,#83062,#83063,
#83064,#83065,#83066,#83067,#83068,#83069,#83070),.UNSPECIFIED.,.F.,.F.,
(4,2,2,2,2,4),(-11.5393310976055,-11.5013731957114,-11.4621334340822,-11.4153480751354,
-11.370429899528,-11.3541155477015),.UNSPECIFIED.) ;
#1663=B_SPLINE_CURVE_WITH_KNOTS('',3,(#83075,#83076,#83077,#83078,#83079,
#83080,#83081,#83082,#83083,#83084,#83085,#83086,#83087,#83088,#83089,#83090,
#83091,#83092,#83093,#83094,#83095,#83096,#83097,#83098,#83099,#83100,#83101,
#83102,#83103,#83104,#83105,#83106,#83107,#83108,#83109,#83110),
 .UNSPECIFIED.,.F.,.F.,(4,2,2,2,2,2,2,2,2,2,2,2,2,2,2,2,2,4),(-1.34731169092089,
-1.3412018153619,-1.29589168841991,-1.24955082083875,-1.20306965837919,
-1.15826389470243,-1.11138171165322,-1.06538584417928,-1.02039676291541,
-0.973136021319122,-0.927670180887149,-0.881634272236604,-0.834974620519227,
-0.790022224945155,-0.743078246417081,-0.696892986888225,-0.651937532555577,
-0.604482102223105),.UNSPECIFIED.) ;
#1664=B_SPLINE_CURVE_WITH_KNOTS('',3,(#83111,#83112,#83113,#83114,#83115,
#83116,#83117,#83118,#83119,#83120,#83121,#83122,#83123,#83124,#83125,#83126,
#83127,#83128,#83129,#83130,#83131,#83132,#83133,#83134,#83135,#83136,#83137,
#83138,#83139,#83140,#83141,#83142,#83143,#83144,#83145,#83146),
 .UNSPECIFIED.,.F.,.F.,(4,2,2,2,2,2,2,2,2,2,2,2,2,2,2,2,2,4),(-11.3541155477015,
-11.3237621770439,-11.2778677119073,-11.2323992784145,-11.1851333428345,
-11.1402220975301,-11.0942245020397,-11.0473852179779,-11.002595542972,
-10.9561167440097,-10.9099470224542,-10.8646457619258,-10.8175607661819,
-10.7725610586643,-10.7267296728004,-10.6799275400698,-10.6352322960093,
-10.6125286589702),.UNSPECIFIED.) ;
#1665=B_SPLINE_CURVE_WITH_KNOTS('',3,(#83151,#83152,#83153,#83154,#83155,
#83156,#83157,#83158,#83159,#83160,#83161,#83162,#83163,#83164,#83165,#83166,
#83167,#83168,#83169,#83170,#83171,#83172,#83173,#83174,#83175,#83176,#83177,
#83178,#83179,#83180,#83181,#83182,#83183,#83184,#83185,#83186),
 .UNSPECIFIED.,.F.,.F.,(4,2,2,2,2,2,2,2,2,2,2,2,2,2,2,2,2,4),(-2.08931556787976,
-2.07717317487852,-2.03206502854522,-1.98490565151034,-1.93867897462963,
-1.89393154733524,-1.8470655465658,-1.8013407535219,-1.75604490428414,-1.70908360063356,
-1.66389336498396,-1.61717126675813,-1.57083532596603,-1.5260973037643,
-1.47924023671116,-1.43339866758495,-1.38829377159172,-1.34731169092089),
 .UNSPECIFIED.) ;
#1666=B_SPLINE_CURVE_WITH_KNOTS('',3,(#83187,#83188,#83189,#83190,#83191,
#83192,#83193,#83194,#83195,#83196,#83197,#83198,#83199,#83200,#83201,#83202,
#83203,#83204,#83205,#83206,#83207,#83208,#83209,#83210,#83211,#83212,#83213,
#83214,#83215,#83216,#83217,#83218,#83219,#83220,#83221,#83222),
 .UNSPECIFIED.,.F.,.F.,(4,2,2,2,2,2,2,2,2,2,2,2,2,2,2,2,2,4),(-10.6125286589702,
-10.5889100367047,-10.5423832940755,-10.4972140874325,-10.4502727021239,
-10.4051066814913,-10.3594048645256,-10.3126050385905,-10.267925831595,
-10.2217251541091,-10.174778107769,-10.1297038549222,-10.0828665268164,
-10.0374670241972,-9.99185573135441,-9.94502566253314,-9.9002901133366,
-9.87140270043892),.UNSPECIFIED.) ;
#1667=B_SPLINE_CURVE_WITH_KNOTS('',3,(#83227,#83228,#83229,#83230,#83231,
#83232,#83233,#83234,#83235,#83236,#83237,#83238,#83239,#83240,#83241,#83242,
#83243,#83244,#83245,#83246,#83247,#83248,#83249,#83250,#83251,#83252,#83253,
#83254,#83255,#83256,#83257,#83258,#83259,#83260,#83261,#83262),
 .UNSPECIFIED.,.F.,.F.,(4,2,2,2,2,2,2,2,2,2,2,2,2,2,2,2,2,4),(-2.83245463856665,
-2.81370343304387,-2.76880307515479,-2.72186916108506,-2.67574833193176,
-2.63076864197808,-2.58337370011299,-2.53778287170268,-2.49186092435614,
-2.44506390373703,-2.40002203430969,-2.35312926746393,-2.30697313780473,
-2.26214711373248,-2.21524024196913,-2.16959241343306,-2.12404413386628,
-2.08931556787976),.UNSPECIFIED.) ;
#1668=B_SPLINE_CURVE_WITH_KNOTS('',3,(#83263,#83264,#83265,#83266,#83267,
#83268,#83269,#83270,#83271,#83272,#83273,#83274,#83275,#83276,#83277,#83278,
#83279,#83280,#83281,#83282,#83283,#83284,#83285,#83286,#83287,#83288,#83289,
#83290,#83291,#83292,#83293,#83294,#83295,#83296,#83297,#83298),
 .UNSPECIFIED.,.F.,.F.,(4,2,2,2,2,2,2,2,2,2,2,2,2,2,2,2,2,4),(-9.87140270043892,
-9.85417324171317,-9.80735552697951,-9.76235647797716,-9.71560253017239,
-9.66986064457499,-9.62431652276782,-9.57696752511082,-9.53210483846283,
-9.48603207223652,-9.43919136581251,-9.39434694969904,-9.34779975847588,
-9.30183561623833,-9.25647793175298,-9.20933024089469,-9.16442679755697,
-9.12966134408518),.UNSPECIFIED.) ;
#1669=B_SPLINE_CURVE_WITH_KNOTS('',3,(#83303,#83304,#83305,#83306,#83307,
#83308,#83309,#83310,#83311,#83312,#83313,#83314,#83315,#83316,#83317,#83318,
#83319,#83320,#83321,#83322,#83323,#83324,#83325,#83326,#83327,#83328,#83329,
#83330,#83331,#83332,#83333,#83334,#83335,#83336,#83337,#83338),
 .UNSPECIFIED.,.F.,.F.,(4,2,2,2,2,2,2,2,2,2,2,2,2,2,2,2,2,4),(-3.57487681123277,
-3.54968647514162,-3.50493349970735,-3.45805565860227,-3.41224821672189,
-3.36705025131333,-3.31999785751033,-3.27472319297991,-3.22820685407033,
-3.18177117344887,-3.13698401394248,-3.09009589679917,-3.04414982511993,
-2.9991008402324,-2.95189561122699,-2.90648023451509,-2.86030375025126,
-2.83245463856665),.UNSPECIFIED.) ;
#1670=B_SPLINE_CURVE_WITH_KNOTS('',3,(#83339,#83340,#83341,#83342,#83343,
#83344,#83345,#83346,#83347,#83348,#83349,#83350,#83351,#83352,#83353,#83354,
#83355,#83356,#83357,#83358,#83359,#83360,#83361,#83362,#83363,#83364,#83365,
#83366,#83367,#83368,#83369,#83370,#83371,#83372,#83373,#83374),
 .UNSPECIFIED.,.F.,.F.,(4,2,2,2,2,2,2,2,2,2,2,2,2,2,2,2,2,4),(-9.12966134408518,
-9.11854010652168,-9.07175780388743,-9.02705303938877,-8.98068119937531,
-8.93440550666307,-8.88920021314424,-8.8422177708298,-8.79719195681835,
-8.75145611879147,-8.70469585620383,-8.66005189617882,-8.61382199987997,
-8.56716018383391,-8.52207136168262,-8.47521592007197,-8.42999357961432,
-8.38917606320042),.UNSPECIFIED.) ;
#1671=B_SPLINE_CURVE_WITH_KNOTS('',3,(#83379,#83380,#83381,#83382,#83383,
#83384,#83385,#83386,#83387,#83388,#83389,#83390,#83391,#83392,#83393,#83394,
#83395,#83396,#83397,#83398,#83399,#83400,#83401,#83402,#83403,#83404,#83405,
#83406,#83407,#83408,#83409,#83410,#83411,#83412,#83413,#83414),
 .UNSPECIFIED.,.F.,.F.,(4,2,2,2,2,2,2,2,2,2,2,2,2,2,2,2,2,4),(-4.31766659413976,
-4.28659846302871,-4.24170055646562,-4.19474588369237,-4.1490979597056,
-4.10340702113605,-4.0565409612618,-4.01143575579773,-3.96405683387488,
-3.91784449462356,-3.87305125486111,-3.82615059506103,-3.78044321036394,
-3.73502561909169,-3.68808695293045,-3.64291630589686,-3.59599189048964,
-3.57487681123277),.UNSPECIFIED.) ;
#1672=B_SPLINE_CURVE_WITH_KNOTS('',3,(#83415,#83416,#83417,#83418,#83419,
#83420,#83421,#83422,#83423,#83424,#83425,#83426,#83427,#83428,#83429,#83430,
#83431,#83432,#83433,#83434,#83435,#83436,#83437,#83438,#83439,#83440,#83441,
#83442,#83443,#83444,#83445,#83446,#83447,#83448,#83449,#83450,#83451,#83452),
 .UNSPECIFIED.,.F.,.F.,(4,2,2,2,2,2,2,2,2,2,2,2,2,2,2,2,2,2,4),(-8.38917606320042,
-8.38437093820375,-8.33759893938715,-8.29293925621511,-8.24681517513577,
-8.199713215607,-8.15470298046625,-8.10793414450284,-8.06245545585829,-8.01690611295866,
-7.97009066411063,-7.92534712298602,-7.87929000553699,-7.83248902005484,
-7.78754258654849,-7.74084506106679,-7.69498578432255,-7.64949066614786,
-7.64797087659483),.UNSPECIFIED.) ;
#1673=B_SPLINE_CURVE_WITH_KNOTS('',3,(#83457,#83458,#83459,#83460,#83461,
#83462,#83463,#83464,#83465,#83466,#83467,#83468,#83469,#83470,#83471,#83472,
#83473,#83474,#83475,#83476,#83477,#83478,#83479,#83480,#83481,#83482,#83483,
#83484,#83485,#83486,#83487,#83488,#83489,#83490,#83491,#83492),
 .UNSPECIFIED.,.F.,.F.,(4,2,2,2,2,2,2,2,2,2,2,2,2,2,2,2,2,4),(-5.06189018830862,
-5.0246914476009,-4.97950438607291,-4.93227395428298,-4.88683167766163,
-4.8404383466902,-4.79381815898027,-4.74888605317594,-4.70188421904935,
-4.65574875023561,-4.61066410116121,-4.56325818761082,-4.51765389759663,
-4.47155159378806,-4.424747023233,-4.3796963332284,-4.33275745326406,-4.31766659413976),
 .UNSPECIFIED.) ;
#1674=B_SPLINE_CURVE_WITH_KNOTS('',3,(#83493,#83494,#83495,#83496,#83497,
#83498,#83499,#83500,#83501,#83502,#83503,#83504,#83505,#83506,#83507,#83508,
#83509,#83510,#83511,#83512,#83513,#83514,#83515,#83516,#83517,#83518,#83519,
#83520,#83521,#83522,#83523,#83524,#83525,#83526,#83527,#83528),
 .UNSPECIFIED.,.F.,.F.,(4,2,2,2,2,2,2,2,2,2,2,2,2,2,2,2,2,4),(-7.64797087659483,
-7.60219585475731,-7.55729228392319,-7.51126807237905,-7.46442153868907,
-7.41961221540445,-7.37310843911013,-7.32698746884331,-7.28166466461712,
-7.23455623843522,-7.18957659516422,-7.14372391229961,-7.09692002617542,
-7.05221709702265,-7.0058749010068,-6.95940823504211,-6.91422291151097,
-6.90653741160255),.UNSPECIFIED.) ;
#1675=B_SPLINE_CURVE_WITH_KNOTS('',3,(#83533,#83534,#83535,#83536,#83537,
#83538,#83539,#83540,#83541,#83542,#83543,#83544,#83545,#83546,#83547,#83548,
#83549,#83550,#83551,#83552,#83553,#83554,#83555,#83556,#83557,#83558,#83559,
#83560,#83561,#83562,#83563,#83564,#83565,#83566,#83567,#83568),
 .UNSPECIFIED.,.F.,.F.,(4,2,2,2,2,2,2,2,2,2,2,2,2,2,2,2,2,4),(-5.80568588485352,
-5.76254620022904,-5.71693605613462,-5.66994085357101,-5.62471389566346,
-5.57751982231786,-5.53116693801469,-5.4863196315096,-5.43934574413778,
-5.39349474889934,-5.34812844394237,-5.30103565386192,-5.25571981922943,
-5.20895608059552,-5.16248732504782,-5.11763667173845,-5.07066608480533,
-5.06189018830862),.UNSPECIFIED.) ;
#1676=B_SPLINE_CURVE_WITH_KNOTS('',3,(#83569,#83570,#83571,#83572,#83573,
#83574,#83575,#83576,#83577,#83578,#83579,#83580,#83581,#83582,#83583,#83584,
#83585,#83586,#83587,#83588,#83589,#83590,#83591,#83592,#83593,#83594,#83595,
#83596,#83597,#83598,#83599,#83600,#83601,#83602,#83603,#83604),
 .UNSPECIFIED.,.F.,.F.,(4,2,2,2,2,2,2,2,2,2,2,2,2,2,2,2,2,4),(-6.90653741160255,
-6.86726387513544,-6.82212926045643,-6.77641183790277,-6.72961536262379,
-6.68494008118346,-6.63872492763704,-6.59184615335233,-6.54676151251456,
-6.49991264254877,-6.45455352979052,-6.40893266759151,-6.3621107437088,
-6.31738944954778,-6.27126398027799,-6.22445353975894,-6.17944803528691,
-6.16535718549382),.UNSPECIFIED.) ;
#1677=B_SPLINE_CURVE_WITH_KNOTS('',3,(#83609,#83610,#83611,#83612,#83613,
#83614,#83615,#83616,#83617,#83618,#83619,#83620,#83621,#83622,#83623,#83624,
#83625,#83626,#83627,#83628,#83629,#83630,#83631,#83632,#83633,#83634,#83635,
#83636,#83637,#83638,#83639,#83640,#83641,#83642,#83643,#83644,#83645,#83646),
 .UNSPECIFIED.,.F.,.F.,(4,2,2,2,2,2,2,2,2,2,2,2,2,2,2,2,2,2,4),(-6.5485693399367,
-6.54469452430869,-6.4978255135919,-6.45306354789751,-6.40687923124368,
-6.35954447090233,-6.31446735523363,-6.26763036535901,-6.22197751540764,
-6.1763582302673,-6.12943610112621,-6.08457118639726,-6.03844133336597,
-5.99153489517415,-5.94651305142779,-5.90023767360354,-5.85532263233972,
-5.80831310746145,-5.80568588485352),.UNSPECIFIED.) ;
#1678=B_SPLINE_CURVE_WITH_KNOTS('',3,(#83647,#83648,#83649,#83650,#83651,
#83652,#83653,#83654,#83655,#83656,#83657,#83658,#83659,#83660,#83661,#83662,
#83663,#83664,#83665,#83666,#83667,#83668,#83669,#83670,#83671,#83672,#83673,
#83674,#83675,#83676,#83677,#83678,#83679,#83680,#83681,#83682),
 .UNSPECIFIED.,.F.,.F.,(4,2,2,2,2,2,2,2,2,2,2,2,2,2,2,2,2,4),(-6.16535718549382,
-6.13268670498756,-6.08699929169078,-6.04145007032189,-5.99409453761209,
-5.94925789990988,-5.90318034616918,-5.85635525600001,-5.81150873241543,
-5.76495891990493,-5.72024348147513,-5.67344467205068,-5.62788672168556,
-5.58247359644929,-5.53569334689852,-5.49067310216224,-5.44367706639317,
-5.4240172864351),.UNSPECIFIED.) ;
#1679=B_SPLINE_CURVE_WITH_KNOTS('',3,(#83687,#83688,#83689,#83690,#83691,
#83692,#83693,#83694,#83695,#83696,#83697,#83698,#83699,#83700,#83701,#83702,
#83703,#83704,#83705,#83706,#83707,#83708,#83709,#83710,#83711,#83712,#83713,
#83714,#83715,#83716,#83717,#83718,#83719,#83720,#83721,#83722),
 .UNSPECIFIED.,.F.,.F.,(4,2,2,2,2,2,2,2,2,2,2,2,2,2,2,2,2,4),(-7.2903982875493,
-7.28026237605557,-7.23340402376256,-7.18864394453266,-7.14223433209178,
-7.09575895219682,-7.05051031092062,-7.00348478836652,-6.95832150536336,
-6.91254051700472,-6.86569340257366,-6.82096968707691,-6.77469126511584,
-6.72780971778659,-6.68266609136878,-6.63575535824411,-6.59037439851765,
-6.5485693399367),.UNSPECIFIED.) ;
#1680=B_SPLINE_CURVE_WITH_KNOTS('',3,(#83723,#83724,#83725,#83726,#83727,
#83728,#83729,#83730,#83731,#83732,#83733,#83734,#83735,#83736,#83737,#83738,
#83739,#83740,#83741,#83742,#83743,#83744,#83745,#83746,#83747,#83748,#83749,
#83750,#83751,#83752,#83753,#83754,#83755,#83756,#83757,#83758),
 .UNSPECIFIED.,.F.,.F.,(4,2,2,2,2,2,2,2,2,2,2,2,2,2,2,2,2,4),(-5.4240172864351,
-5.39753691479611,-5.3528911128382,-5.30612883532888,-5.26048854219916,
-5.21532000638465,-5.16844399254702,-5.12333656913247,-5.07677055162506,
-5.03051629773879,-4.98586970138458,-4.93911182979272,-4.89334974740763,
-4.84836207585291,-4.80135035441491,-4.75611829156816,-4.70992336812542,
-4.68362193225928),.UNSPECIFIED.) ;
#1681=B_SPLINE_CURVE_WITH_KNOTS('',3,(#83763,#83764,#83765,#83766,#83767,
#83768,#83769,#83770,#83771,#83772,#83773,#83774,#83775,#83776,#83777,#83778,
#83779,#83780,#83781,#83782,#83783,#83784,#83785,#83786,#83787,#83788,#83789,
#83790,#83791,#83792,#83793,#83794,#83795,#83796,#83797,#83798),
 .UNSPECIFIED.,.F.,.F.,(4,2,2,2,2,2,2,2,2,2,2,2,2,2,2,2,2,4),(-8.03313136846868,
-8.01678752022364,-7.96992196508481,-7.92490377627534,-7.87813124306105,
-7.83224506796249,-7.78667850411988,-7.73930857188702,-7.694358942822,-7.64826272925189,
-7.60135756548507,-7.55648212666153,-7.50990705070329,-7.46376909578636,
-7.41837882573787,-7.37119949443887,-7.32618295935356,-7.2903982875493),
 .UNSPECIFIED.) ;
#1682=B_SPLINE_CURVE_WITH_KNOTS('',3,(#83799,#83800,#83801,#83802,#83803,
#83804,#83805,#83806,#83807,#83808,#83809,#83810,#83811,#83812,#83813,#83814,
#83815,#83816,#83817,#83818,#83819,#83820,#83821,#83822,#83823,#83824,#83825,
#83826,#83827,#83828,#83829,#83830,#83831,#83832,#83833,#83834),
 .UNSPECIFIED.,.F.,.F.,(4,2,2,2,2,2,2,2,2,2,2,2,2,2,2,2,2,4),(-4.68362193225928,
-4.66351951710304,-4.61879451160515,-4.57200673789761,-4.52608576131031,
-4.48120275436424,-4.43401758077193,-4.38862540199452,-4.34272311312387,
-4.29613678696753,-4.25125494346797,-4.20440028285465,-4.15828570684597,
-4.11342482121262,-4.06603060008173,-4.02044463673821,-3.97474347018052,
-3.94185895807078),.UNSPECIFIED.) ;
#1683=B_SPLINE_CURVE_WITH_KNOTS('',3,(#83839,#83840,#83841,#83842,#83843,
#83844,#83845,#83846,#83847,#83848,#83849,#83850,#83851,#83852,#83853,#83854,
#83855,#83856,#83857,#83858,#83859,#83860,#83861,#83862,#83863,#83864,#83865,
#83866,#83867,#83868,#83869,#83870,#83871,#83872,#83873,#83874),
 .UNSPECIFIED.,.F.,.F.,(4,2,2,2,2,2,2,2,2,2,2,2,2,2,2,2,2,4),(-8.77491333060422,
-8.75231389418036,-8.70562932404755,-8.66046095430428,-8.61352221281336,
-8.56825768216331,-8.5225551658115,-8.47571560127791,-8.43099402430489,
-8.38479009824252,-8.33766978968508,-8.29258457966775,-8.2457373223502,
-8.20022201624112,-8.15459759623412,-8.10771807906936,-8.06291978776965,
-8.03313136846868),.UNSPECIFIED.) ;
#1684=B_SPLINE_CURVE_WITH_KNOTS('',3,(#83875,#83876,#83877,#83878,#83879,
#83880,#83881,#83882,#83883,#83884,#83885,#83886,#83887,#83888,#83889,#83890,
#83891,#83892,#83893,#83894,#83895,#83896,#83897,#83898,#83899,#83900,#83901,
#83902,#83903,#83904,#83905,#83906,#83907,#83908,#83909,#83910),
 .UNSPECIFIED.,.F.,.F.,(4,2,2,2,2,2,2,2,2,2,2,2,2,2,2,2,2,4),(-3.94185895807078,
-3.92794359307557,-3.88290124803901,-3.83605797395444,-3.78989399397843,
-3.74514397062485,-3.698289555497,-3.65263018309304,-3.60725206137288,-3.56036298328301,
-3.5152399334815,-3.46835185771871,-3.42209586200823,-3.37738781550701,
-3.33055699830715,-3.28479866434645,-3.23964153573233,-3.20015024205927),
 .UNSPECIFIED.) ;
#1685=B_SPLINE_CURVE_WITH_KNOTS('',3,(#83915,#83916,#83917,#83918,#83919,
#83920,#83921,#83922,#83923,#83924,#83925,#83926,#83927,#83928,#83929,#83930,
#83931,#83932,#83933,#83934,#83935,#83936,#83937,#83938,#83939,#83940,#83941,
#83942,#83943,#83944,#83945,#83946,#83947,#83948,#83949,#83950),
 .UNSPECIFIED.,.F.,.F.,(4,2,2,2,2,2,2,2,2,2,2,2,2,2,2,2,2,4),(-9.51681717340635,
-9.48746469526357,-9.44146155525688,-9.39601566694291,-9.34877545441454,
-9.30381320687154,-9.25783760349915,-9.21097989719694,-9.16619559342027,
-9.11973524996446,-9.07342976330784,-9.02814050699756,-8.98107005349904,
-8.93599434700291,-8.89017400244873,-8.84334241713347,-8.79862810084481,
-8.77491333060422),.UNSPECIFIED.) ;
#1686=B_SPLINE_CURVE_WITH_KNOTS('',3,(#83951,#83952,#83953,#83954,#83955,
#83956,#83957,#83958,#83959,#83960,#83961,#83962,#83963,#83964,#83965,#83966,
#83967,#83968,#83969,#83970,#83971,#83972,#83973,#83974,#83975,#83976,#83977,
#83978,#83979,#83980,#83981,#83982,#83983,#83984,#83985,#83986),
 .UNSPECIFIED.,.F.,.F.,(4,2,2,2,2,2,2,2,2,2,2,2,2,2,2,2,2,4),(-3.20015024205927,
-3.19263985153786,-3.14741383327045,-3.10093486301163,-3.05454962939341,
-3.00980937954436,-2.9629691524755,-2.91707326441536,-2.87206684967415,
-2.82491343575938,-2.77954774098522,-2.73341022654117,-2.68686135074236,
-2.64200999664347,-2.59512494148472,-2.54905534698971,-2.50412022980151,
-2.45812360193803),.UNSPECIFIED.) ;
#1687=B_SPLINE_CURVE_WITH_KNOTS('',3,(#83991,#83992,#83993,#83994,#83995,
#83996,#83997,#83998,#83999,#84000,#84001,#84002,#84003,#84004,#84005,#84006,
#84007,#84008,#84009,#84010,#84011,#84012,#84013,#84014,#84015,#84016,#84017,
#84018,#84019,#84020,#84021,#84022,#84023,#84024,#84025,#84026),
 .UNSPECIFIED.,.F.,.F.,(4,2,2,2,2,2,2,2,2,2,2,2,2,2,2,2,2,4),(-10.2599619460435,
-10.2238795993298,-10.1784210421296,-10.1327140734422,-10.0857987625166,
-10.0409865492377,-9.99477371905538,-9.94787016080768,-9.90277888516916,
-9.85592862759665,-9.81013720350877,-9.76450078117451,-9.71705493603555,
-9.67212388099948,-9.6259580110907,-9.57903744350876,-9.53410435631313,
-9.51681717340635),.UNSPECIFIED.) ;
#1688=B_SPLINE_CURVE_WITH_KNOTS('',3,(#84027,#84028,#84029,#84030,#84031,
#84032,#84033,#84034,#84035,#84036,#84037,#84038,#84039,#84040,#84041,#84042,
#84043,#84044,#84045,#84046,#84047,#84048,#84049,#84050,#84051,#84052,#84053,
#84054,#84055,#84056,#84057,#84058,#84059,#84060,#84061,#84062,#84063,#84064),
 .UNSPECIFIED.,.F.,.F.,(4,2,2,2,2,2,2,2,2,2,2,2,2,2,2,2,2,2,4),(-2.45812360193803,
-2.45677819111201,-2.41123806917093,-2.36535712296393,-2.31861252364742,
-2.27362101086785,-2.22677840151894,-2.18067423534073,-2.13589460996303,
-2.08903779312993,-2.04344152483191,-1.99793613709164,-1.95111841743952,
-1.9060613966591,-1.85894205246388,-1.81276844099364,-1.76806895369967,
-1.72125375882939,-1.71626027993097),.UNSPECIFIED.) ;
#1689=B_SPLINE_CURVE_WITH_KNOTS('',3,(#84069,#84070,#84071,#84072,#84073,
#84074,#84075,#84076,#84077,#84078,#84079,#84080,#84081,#84082,#84083,#84084,
#84085,#84086,#84087,#84088,#84089,#84090,#84091,#84092,#84093,#84094,#84095,
#84096,#84097,#84098,#84099,#84100,#84101,#84102,#84103,#84104),
 .UNSPECIFIED.,.F.,.F.,(4,2,2,2,2,2,2,2,2,2,2,2,2,2,2,2,2,4),(-11.0024392821081,
-10.9599663286644,-10.9148936873785,-10.8689576925085,-10.8220632122557,
-10.7772755291895,-10.7308486859947,-10.6842749853735,-10.6390062126163,
-10.5919607038823,-10.5467296415202,-10.5009275958716,-10.4540391183822,
-10.4092759003239,-10.3629748375851,-10.3159858990373,-10.2708164187479,
-10.2599619460435),.UNSPECIFIED.) ;
#1690=B_SPLINE_CURVE_WITH_KNOTS('',3,(#84105,#84106,#84107,#84108,#84109,
#84110,#84111,#84112,#84113,#84114,#84115,#84116,#84117,#84118,#84119,#84120,
#84121,#84122,#84123,#84124,#84125,#84126,#84127,#84128,#84129,#84130,#84131,
#84132,#84133,#84134,#84135,#84136,#84137,#84138,#84139,#84140),
 .UNSPECIFIED.,.F.,.F.,(4,2,2,2,2,2,2,2,2,2,2,2,2,2,2,2,2,4),(-1.71626027993097,
-1.67558165604805,-1.63032975843029,-1.58342285229462,-1.53828482577707,
-1.49160342090406,-1.44532162530017,-1.40063343013664,-1.35382800245341,
-1.30804024643797,-1.2629808833479,-1.21594447590769,-1.17068763509309,
-1.12438875183991,-1.07796278093185,-1.03320894854416,-0.986379336876156,
-0.975053485488691),.UNSPECIFIED.) ;
#1691=B_SPLINE_CURVE_WITH_KNOTS('',3,(#84145,#84146,#84147,#84148,#84149,
#84150,#84151,#84152,#84153,#84154,#84155,#84156,#84157,#84158,#84159,#84160,
#84161,#84162,#84163,#84164,#84165,#84166,#84167,#84168,#84169,#84170,#84171,
#84172,#84173,#84174,#84175,#84176,#84177,#84178,#84179,#84180,#84181,#84182),
 .UNSPECIFIED.,.F.,.F.,(4,2,2,2,2,2,2,2,2,2,2,2,2,2,2,2,2,2,4),(-11.745553964402,
-11.7437796313797,-11.6968771639769,-11.6520478978994,-11.6059097355514,
-11.5590219451859,-11.5139958135559,-11.4672156546915,-11.4212575032449,
-11.3756812580484,-11.328302426854,-11.2833094575338,-11.2372030713339,
-11.1902673929136,-11.1453764273601,-11.0987890831327,-11.0525649378165,
-11.0071599187327,-11.0024392821081),.UNSPECIFIED.) ;
#1692=B_SPLINE_CURVE_WITH_KNOTS('',3,(#84183,#84184,#84185,#84186,#84187,
#84188,#84189,#84190,#84191,#84192,#84193,#84194,#84195,#84196,#84197,#84198,
#84199,#84200,#84201,#84202,#84203,#84204,#84205,#84206,#84207,#84208,#84209,
#84210,#84211,#84212,#84213,#84214,#84215,#84216,#84217,#84218),
 .UNSPECIFIED.,.F.,.F.,(4,2,2,2,2,2,2,2,2,2,2,2,2,2,2,2,2,4),(-0.975053485488691,
-0.940438383434336,-0.895496741425073,-0.848292684069909,-0.802881195188261,
-0.756889100969424,-0.710285662172893,-0.665387348006602,-0.618496985028334,
-0.572367719394815,-0.527461816105139,-0.480054142080902,-0.434454029561906,
-0.388678699600084,-0.341866450150363,-0.296811533381677,-0.249941016724657,
-0.232520228075875),.UNSPECIFIED.) ;
#1693=B_SPLINE_CURVE_WITH_KNOTS('',3,(#84224,#84225,#84226,#84227,#84228,
#84229,#84230,#84231,#84232,#84233,#84234,#84235),.UNSPECIFIED.,.F.,.F.,
(4,2,2,2,2,4),(-0.597330195429814,-0.544079370208448,-0.490056450117875,
-0.432782108807466,-0.373472117043514,-0.370559454039791),.UNSPECIFIED.) ;
#1694=B_SPLINE_CURVE_WITH_KNOTS('',3,(#84236,#84237,#84238,#84239,#84240,
#84241,#84242,#84243,#84244,#84245,#84246,#84247,#84248,#84249,#84250,#84251,
#84252,#84253,#84254,#84255),.UNSPECIFIED.,.F.,.F.,(4,2,2,2,2,2,2,2,2,4),
(-0.649716652274618,-0.564337691326781,-0.481346182278479,-0.363784182044033,
-0.257506122927,-0.162647153734189,-0.114596047443497,-0.051841763469862,
-0.0257254202730378,0.),.UNSPECIFIED.) ;
#1695=B_SPLINE_CURVE_WITH_KNOTS('',3,(#84259,#84260,#84261,#84262,#84263,
#84264,#84265,#84266,#84267,#84268,#84269,#84270),.UNSPECIFIED.,.F.,.F.,
(4,2,2,2,2,4),(0.,0.0418293556303661,0.0810203615126183,0.121024586302138,
0.157958985747223,0.188938551649128),.UNSPECIFIED.) ;
#1696=B_SPLINE_CURVE_WITH_KNOTS('',3,(#84271,#84272,#84273,#84274,#84275,
#84276,#84277,#84278,#84279,#84280,#84281,#84282,#84283,#84284),
 .UNSPECIFIED.,.F.,.F.,(4,2,2,2,2,2,4),(-0.370559454039791,-0.314596141147387,
-0.247797040916131,-0.17177268662274,-0.0929222455585059,-0.0416908555263841,
-9.99999990425327E-7),.UNSPECIFIED.) ;
#1697=B_SPLINE_CURVE_WITH_KNOTS('',3,(#84287,#84288,#84289,#84290,#84291,
#84292,#84293,#84294,#84295,#84296,#84297,#84298,#84299,#84300),
 .UNSPECIFIED.,.F.,.F.,(4,2,2,2,2,2,4),(-0.232520228075875,-0.203766248810284,
-0.158983315267675,-0.112100958247863,-0.0664320735278172,-0.0337545420634901,
-9.9999999686462E-7),.UNSPECIFIED.) ;
#1698=B_SPLINE_CURVE_WITH_KNOTS('',3,(#84303,#84304,#84305,#84306,#84307,
#84308,#84309,#84310,#84311,#84312),.UNSPECIFIED.,.F.,.F.,(4,2,2,2,4),(-11.8840105514171,
-11.8593886360263,-11.834981196036,-11.789408525476,-11.745553964402),
 .UNSPECIFIED.) ;
#1699=B_SPLINE_CURVE_WITH_KNOTS('',3,(#84315,#84316,#84317,#84318,#84319,
#84320,#84321,#84322,#84323,#84324,#84325,#84326,#84327,#84328,#84329,#84330,
#84331,#84332,#84333,#84334,#84335,#84336,#84337,#84338,#84339,#84340,#84341,
#84342,#84343,#84344),.UNSPECIFIED.,.F.,.F.,(4,2,2,2,2,2,2,2,2,2,2,2,2,
2,4),(13.764829475703,13.7801798863136,13.8376035555737,13.897643352408,
13.956519485524,14.0134991405525,14.073172406556,14.1313993619064,14.189048326989,
14.2488660827664,14.3064227017816,14.3658641164806,14.4249063546466,14.4790961696761,
14.5339228824178),.UNSPECIFIED.) ;
#1700=B_SPLINE_CURVE_WITH_KNOTS('',3,(#84347,#84348,#84349,#84350,#84351,
#84352,#84353,#84354,#84355,#84356,#84357,#84358,#84359,#84360,#84361,#84362,
#84363,#84364,#84365,#84366,#84367,#84368,#84369,#84370,#84371,#84372,#84373,
#84374),.UNSPECIFIED.,.F.,.F.,(4,2,2,2,2,2,2,2,2,2,2,2,2,4),(9.99999998019281E-7,
0.0303227215428037,0.0604117772912196,0.118540071650349,0.176589582480443,
0.236954853625382,0.294123775847925,0.352848945254168,0.412557664472652,
0.469738883770964,0.529106788707932,0.587728785588294,0.645562701786344,
0.649736777376371),.UNSPECIFIED.) ;
#1701=B_SPLINE_CURVE_WITH_KNOTS('',3,(#84455,#84456,#84457,#84458,#84459,
#84460,#84461,#84462,#84463,#84464,#84465,#84466,#84467,#84468,#84469,#84470),
 .UNSPECIFIED.,.F.,.F.,(4,2,2,2,2,2,2,4),(-0.393680344589454,-0.341967463828253,
-0.280075465042844,-0.199030941955768,-0.120297878012763,-0.0601931247465125,
-0.0292201673629089,0.),.UNSPECIFIED.) ;
#1702=B_SPLINE_CURVE_WITH_KNOTS('',3,(#84471,#84472,#84473,#84474,#84475,
#84476,#84477,#84478,#84479,#84480,#84481,#84482,#84483,#84484,#84485,#84486),
 .UNSPECIFIED.,.F.,.F.,(4,2,2,2,2,2,2,4),(-0.334612951676255,-0.279460360491098,
-0.2151903907044,-0.163552299907468,-0.123594611698629,-0.0765880757042877,
-0.0381084216339553,-1.00000011143964E-6),.UNSPECIFIED.) ;
#2247=PLANE('',#36459) ;
#2248=PLANE('',#36460) ;
#2249=PLANE('',#36463) ;
#2250=PLANE('',#36464) ;
#2251=PLANE('',#36465) ;
#2252=PLANE('',#36466) ;
#2253=PLANE('',#36467) ;
#2254=PLANE('',#36469) ;
#2255=PLANE('',#36470) ;
#2256=PLANE('',#36471) ;
#2257=PLANE('',#36472) ;
#2258=PLANE('',#36473) ;
#2259=PLANE('',#36474) ;
#2260=PLANE('',#36475) ;
#2261=PLANE('',#36476) ;
#2262=PLANE('',#36478) ;
#2263=PLANE('',#36479) ;
#2264=PLANE('',#36480) ;
#2265=PLANE('',#36481) ;
#4081=FACE_OUTER_BOUND('',#6154,.T.) ;
#4082=FACE_OUTER_BOUND('',#6155,.T.) ;
#4083=FACE_OUTER_BOUND('',#6156,.T.) ;
#4084=FACE_OUTER_BOUND('',#6157,.T.) ;
#4085=FACE_OUTER_BOUND('',#6158,.T.) ;
#4086=FACE_OUTER_BOUND('',#6159,.T.) ;
#4087=FACE_OUTER_BOUND('',#6160,.T.) ;
#4088=FACE_OUTER_BOUND('',#6161,.T.) ;
#4089=FACE_OUTER_BOUND('',#6162,.T.) ;
#4090=FACE_OUTER_BOUND('',#6163,.T.) ;
#4091=FACE_OUTER_BOUND('',#6164,.T.) ;
#4092=FACE_OUTER_BOUND('',#6165,.T.) ;
#4093=FACE_OUTER_BOUND('',#6166,.T.) ;
#4094=FACE_OUTER_BOUND('',#6167,.T.) ;
#4095=FACE_OUTER_BOUND('',#6168,.T.) ;
#4096=FACE_OUTER_BOUND('',#6169,.T.) ;
#4097=FACE_OUTER_BOUND('',#6170,.T.) ;
#4098=FACE_OUTER_BOUND('',#6171,.T.) ;
#4099=FACE_OUTER_BOUND('',#6172,.T.) ;
#4100=FACE_OUTER_BOUND('',#6173,.T.) ;
#4101=FACE_OUTER_BOUND('',#6174,.T.) ;
#4102=FACE_OUTER_BOUND('',#6175,.T.) ;
#4103=FACE_OUTER_BOUND('',#6176,.T.) ;
#4104=FACE_OUTER_BOUND('',#6177,.T.) ;
#4105=FACE_OUTER_BOUND('',#6178,.T.) ;
#4106=FACE_OUTER_BOUND('',#6179,.T.) ;
#4107=FACE_OUTER_BOUND('',#6180,.T.) ;
#4108=FACE_OUTER_BOUND('',#6181,.T.) ;
#4109=FACE_OUTER_BOUND('',#6182,.T.) ;
#4110=FACE_OUTER_BOUND('',#6183,.T.) ;
#4111=FACE_OUTER_BOUND('',#6184,.T.) ;
#4112=FACE_OUTER_BOUND('',#6185,.T.) ;
#4113=FACE_OUTER_BOUND('',#6186,.T.) ;
#4114=FACE_OUTER_BOUND('',#6187,.T.) ;
#4115=FACE_OUTER_BOUND('',#6188,.T.) ;
#4116=FACE_OUTER_BOUND('',#6189,.T.) ;
#4117=FACE_OUTER_BOUND('',#6190,.T.) ;
#4118=FACE_OUTER_BOUND('',#6191,.T.) ;
#4119=FACE_OUTER_BOUND('',#6192,.T.) ;
#4120=FACE_OUTER_BOUND('',#6194,.T.) ;
#4121=FACE_OUTER_BOUND('',#6195,.T.) ;
#4122=FACE_OUTER_BOUND('',#6196,.T.) ;
#4123=FACE_OUTER_BOUND('',#6198,.T.) ;
#4124=FACE_OUTER_BOUND('',#6199,.T.) ;
#4125=FACE_OUTER_BOUND('',#6200,.T.) ;
#4126=FACE_OUTER_BOUND('',#6201,.T.) ;
#4127=FACE_OUTER_BOUND('',#6202,.T.) ;
#4128=FACE_OUTER_BOUND('',#6203,.T.) ;
#4129=FACE_OUTER_BOUND('',#6204,.T.) ;
#4130=FACE_OUTER_BOUND('',#6205,.T.) ;
#4131=FACE_OUTER_BOUND('',#6206,.T.) ;
#4132=FACE_OUTER_BOUND('',#6207,.T.) ;
#4133=FACE_OUTER_BOUND('',#6208,.T.) ;
#4134=FACE_OUTER_BOUND('',#6209,.T.) ;
#4135=FACE_OUTER_BOUND('',#6210,.T.) ;
#4136=FACE_OUTER_BOUND('',#6211,.T.) ;
#4137=FACE_OUTER_BOUND('',#6212,.T.) ;
#4138=FACE_OUTER_BOUND('',#6213,.T.) ;
#4139=FACE_OUTER_BOUND('',#6214,.T.) ;
#4140=FACE_OUTER_BOUND('',#6215,.T.) ;
#4141=FACE_OUTER_BOUND('',#6216,.T.) ;
#4142=FACE_OUTER_BOUND('',#6217,.T.) ;
#4143=FACE_OUTER_BOUND('',#6218,.T.) ;
#4144=FACE_OUTER_BOUND('',#6219,.T.) ;
#4145=FACE_OUTER_BOUND('',#6220,.T.) ;
#6154=EDGE_LOOP('',(#29538,#29539,#29540,#29541)) ;
#6155=EDGE_LOOP('',(#29542,#29543,#29544,#29545)) ;
#6156=EDGE_LOOP('',(#29546,#29547,#29548,#29549)) ;
#6157=EDGE_LOOP('',(#29550,#29551,#29552,#29553)) ;
#6158=EDGE_LOOP('',(#29554,#29555,#29556,#29557)) ;
#6159=EDGE_LOOP('',(#29558,#29559,#29560,#29561)) ;
#6160=EDGE_LOOP('',(#29562,#29563,#29564,#29565)) ;
#6161=EDGE_LOOP('',(#29566,#29567,#29568,#29569)) ;
#6162=EDGE_LOOP('',(#29570,#29571,#29572,#29573)) ;
#6163=EDGE_LOOP('',(#29574,#29575,#29576,#29577)) ;
#6164=EDGE_LOOP('',(#29578,#29579,#29580,#29581)) ;
#6165=EDGE_LOOP('',(#29582,#29583,#29584,#29585)) ;
#6166=EDGE_LOOP('',(#29586,#29587,#29588,#29589)) ;
#6167=EDGE_LOOP('',(#29590,#29591,#29592,#29593)) ;
#6168=EDGE_LOOP('',(#29594,#29595,#29596,#29597)) ;
#6169=EDGE_LOOP('',(#29598,#29599,#29600,#29601,#29602)) ;
#6170=EDGE_LOOP('',(#29603,#29604,#29605,#29606)) ;
#6171=EDGE_LOOP('',(#29607,#29608,#29609,#29610)) ;
#6172=EDGE_LOOP('',(#29611,#29612,#29613,#29614)) ;
#6173=EDGE_LOOP('',(#29615,#29616,#29617,#29618)) ;
#6174=EDGE_LOOP('',(#29619,#29620,#29621,#29622)) ;
#6175=EDGE_LOOP('',(#29623,#29624,#29625,#29626)) ;
#6176=EDGE_LOOP('',(#29627,#29628,#29629,#29630)) ;
#6177=EDGE_LOOP('',(#29631,#29632,#29633,#29634)) ;
#6178=EDGE_LOOP('',(#29635,#29636,#29637,#29638)) ;
#6179=EDGE_LOOP('',(#29639,#29640,#29641,#29642)) ;
#6180=EDGE_LOOP('',(#29643,#29644,#29645,#29646)) ;
#6181=EDGE_LOOP('',(#29647,#29648,#29649,#29650)) ;
#6182=EDGE_LOOP('',(#29651,#29652,#29653,#29654)) ;
#6183=EDGE_LOOP('',(#29655,#29656,#29657,#29658)) ;
#6184=EDGE_LOOP('',(#29659,#29660,#29661,#29662)) ;
#6185=EDGE_LOOP('',(#29663,#29664,#29665,#29666)) ;
#6186=EDGE_LOOP('',(#29667,#29668,#29669,#29670,#29671)) ;
#6187=EDGE_LOOP('',(#29672,#29673,#29674,#29675)) ;
#6188=EDGE_LOOP('',(#29676,#29677,#29678,#29679)) ;
#6189=EDGE_LOOP('',(#29680,#29681,#29682,#29683)) ;
#6190=EDGE_LOOP('',(#29684,#29685,#29686,#29687)) ;
#6191=EDGE_LOOP('',(#29688,#29689,#29690,#29691,#29692)) ;
#6192=EDGE_LOOP('',(#29693)) ;
#6193=EDGE_LOOP('',(#29694,#29695,#29696,#29697,#29698,#29699,#29700,#29701,
#29702,#29703,#29704,#29705,#29706,#29707,#29708,#29709,#29710,#29711,#29712,
#29713)) ;
#6194=EDGE_LOOP('',(#29714,#29715,#29716,#29717,#29718,#29719)) ;
#6195=EDGE_LOOP('',(#29720,#29721,#29722,#29723,#29724)) ;
#6196=EDGE_LOOP('',(#29725)) ;
#6197=EDGE_LOOP('',(#29726,#29727,#29728,#29729)) ;
#6198=EDGE_LOOP('',(#29730,#29731,#29732,#29733,#29734,#29735,#29736,#29737,
#29738,#29739,#29740,#29741,#29742,#29743,#29744,#29745,#29746,#29747,#29748,
#29749,#29750,#29751,#29752,#29753,#29754,#29755,#29756,#29757,#29758,#29759,
#29760,#29761,#29762,#29763,#29764,#29765,#29766)) ;
#6199=EDGE_LOOP('',(#29767,#29768,#29769,#29770,#29771,#29772,#29773,#29774,
#29775,#29776,#29777,#29778,#29779,#29780,#29781,#29782,#29783,#29784,#29785,
#29786,#29787,#29788,#29789,#29790,#29791,#29792,#29793,#29794,#29795,#29796,
#29797,#29798,#29799,#29800,#29801)) ;
#6200=EDGE_LOOP('',(#29802,#29803,#29804)) ;
#6201=EDGE_LOOP('',(#29805,#29806,#29807)) ;
#6202=EDGE_LOOP('',(#29808,#29809,#29810,#29811)) ;
#6203=EDGE_LOOP('',(#29812,#29813,#29814,#29815)) ;
#6204=EDGE_LOOP('',(#29816,#29817,#29818,#29819)) ;
#6205=EDGE_LOOP('',(#29820,#29821,#29822,#29823)) ;
#6206=EDGE_LOOP('',(#29824,#29825,#29826,#29827)) ;
#6207=EDGE_LOOP('',(#29828,#29829,#29830,#29831,#29832,#29833,#29834,#29835,
#29836,#29837,#29838,#29839,#29840,#29841,#29842,#29843,#29844,#29845,#29846,
#29847)) ;
#6208=EDGE_LOOP('',(#29848,#29849,#29850,#29851)) ;
#6209=EDGE_LOOP('',(#29852,#29853,#29854,#29855)) ;
#6210=EDGE_LOOP('',(#29856,#29857,#29858,#29859)) ;
#6211=EDGE_LOOP('',(#29860,#29861,#29862,#29863)) ;
#6212=EDGE_LOOP('',(#29864,#29865,#29866,#29867)) ;
#6213=EDGE_LOOP('',(#29868,#29869,#29870,#29871)) ;
#6214=EDGE_LOOP('',(#29872,#29873,#29874,#29875)) ;
#6215=EDGE_LOOP('',(#29876,#29877,#29878,#29879)) ;
#6216=EDGE_LOOP('',(#29880,#29881,#29882,#29883)) ;
#6217=EDGE_LOOP('',(#29884,#29885,#29886,#29887)) ;
#6218=EDGE_LOOP('',(#29888,#29889,#29890,#29891)) ;
#6219=EDGE_LOOP('',(#29892,#29893,#29894,#29895)) ;
#6220=EDGE_LOOP('',(#29896,#29897,#29898,#29899)) ;
#8482=LINE('',#81800,#10801) ;
#8483=LINE('',#81853,#10802) ;
#8484=LINE('',#81929,#10803) ;
#8485=LINE('',#82007,#10804) ;
#8486=LINE('',#82085,#10805) ;
#8487=LINE('',#82161,#10806) ;
#8488=LINE('',#82237,#10807) ;
#8489=LINE('',#82313,#10808) ;
#8490=LINE('',#82389,#10809) ;
#8491=LINE('',#82467,#10810) ;
#8492=LINE('',#82543,#10811) ;
#8493=LINE('',#82621,#10812) ;
#8494=LINE('',#82697,#10813) ;
#8495=LINE('',#82773,#10814) ;
#8496=LINE('',#82849,#10815) ;
#8497=LINE('',#82925,#10816) ;
#8498=LINE('',#83074,#10817) ;
#8499=LINE('',#83150,#10818) ;
#8500=LINE('',#83226,#10819) ;
#8501=LINE('',#83302,#10820) ;
#8502=LINE('',#83378,#10821) ;
#8503=LINE('',#83456,#10822) ;
#8504=LINE('',#83532,#10823) ;
#8505=LINE('',#83608,#10824) ;
#8506=LINE('',#83686,#10825) ;
#8507=LINE('',#83762,#10826) ;
#8508=LINE('',#83838,#10827) ;
#8509=LINE('',#83914,#10828) ;
#8510=LINE('',#83990,#10829) ;
#8511=LINE('',#84068,#10830) ;
#8512=LINE('',#84144,#10831) ;
#8513=LINE('',#84222,#10832) ;
#8514=LINE('',#84448,#10833) ;
#8515=LINE('',#84921,#10834) ;
#8516=LINE('',#85395,#10835) ;
#8517=LINE('',#85396,#10836) ;
#8518=LINE('',#85399,#10837) ;
#8519=LINE('',#85400,#10838) ;
#8520=LINE('',#85403,#10839) ;
#8521=LINE('',#85404,#10840) ;
#8522=LINE('',#85406,#10841) ;
#8523=LINE('',#85409,#10842) ;
#8524=LINE('',#85411,#10843) ;
#8525=LINE('',#85413,#10844) ;
#8526=LINE('',#85415,#10845) ;
#8527=LINE('',#85417,#10846) ;
#8528=LINE('',#85421,#10847) ;
#8529=LINE('',#85423,#10848) ;
#8530=LINE('',#85425,#10849) ;
#8531=LINE('',#85426,#10850) ;
#8532=LINE('',#85428,#10851) ;
#8533=LINE('',#85430,#10852) ;
#8534=LINE('',#85431,#10853) ;
#8535=LINE('',#85433,#10854) ;
#8536=LINE('',#85435,#10855) ;
#8537=LINE('',#85437,#10856) ;
#8538=LINE('',#85440,#10857) ;
#8539=LINE('',#85442,#10858) ;
#8540=LINE('',#85444,#10859) ;
#8541=LINE('',#85454,#10860) ;
#8542=LINE('',#85456,#10861) ;
#8543=LINE('',#85458,#10862) ;
#10801=VECTOR('',#45994,1.5) ;
#10802=VECTOR('',#45999,1.5) ;
#10803=VECTOR('',#46002,1.5) ;
#10804=VECTOR('',#46005,1.5) ;
#10805=VECTOR('',#46008,1.5) ;
#10806=VECTOR('',#46011,1.5) ;
#10807=VECTOR('',#46014,1.5) ;
#10808=VECTOR('',#46017,1.5) ;
#10809=VECTOR('',#46020,1.5) ;
#10810=VECTOR('',#46023,1.5) ;
#10811=VECTOR('',#46026,1.5) ;
#10812=VECTOR('',#46029,1.5) ;
#10813=VECTOR('',#46032,1.5) ;
#10814=VECTOR('',#46035,1.5) ;
#10815=VECTOR('',#46038,1.5) ;
#10816=VECTOR('',#46041,1.17524047358084) ;
#10817=VECTOR('',#46046,1.17524047358084) ;
#10818=VECTOR('',#46049,1.17524047358084) ;
#10819=VECTOR('',#46052,1.17524047358084) ;
#10820=VECTOR('',#46055,1.17524047358084) ;
#10821=VECTOR('',#46058,1.17524047358084) ;
#10822=VECTOR('',#46061,1.17524047358084) ;
#10823=VECTOR('',#46064,1.17524047358084) ;
#10824=VECTOR('',#46067,1.17524047358084) ;
#10825=VECTOR('',#46070,1.17524047358084) ;
#10826=VECTOR('',#46073,1.17524047358084) ;
#10827=VECTOR('',#46076,1.17524047358084) ;
#10828=VECTOR('',#46079,1.17524047358084) ;
#10829=VECTOR('',#46082,1.17524047358084) ;
#10830=VECTOR('',#46085,1.17524047358084) ;
#10831=VECTOR('',#46088,1.17524047358084) ;
#10832=VECTOR('',#46091,4.35024047358084) ;
#10833=VECTOR('',#46170,2.99999999999999) ;
#10834=VECTOR('',#46181,1000.) ;
#10835=VECTOR('',#46190,1000.) ;
#10836=VECTOR('',#46191,1000.) ;
#10837=VECTOR('',#46194,1000.) ;
#10838=VECTOR('',#46195,1000.) ;
#10839=VECTOR('',#46198,1000.) ;
#10840=VECTOR('',#46199,1000.) ;
#10841=VECTOR('',#46202,1000.) ;
#10842=VECTOR('',#46205,1000.) ;
#10843=VECTOR('',#46206,1000.) ;
#10844=VECTOR('',#46207,1000.) ;
#10845=VECTOR('',#46208,999.999999999999) ;
#10846=VECTOR('',#46209,1000.) ;
#10847=VECTOR('',#46212,1000.) ;
#10848=VECTOR('',#46213,1000.) ;
#10849=VECTOR('',#46214,1000.) ;
#10850=VECTOR('',#46215,1000.) ;
#10851=VECTOR('',#46216,1000.) ;
#10852=VECTOR('',#46217,1000.) ;
#10853=VECTOR('',#46218,1000.) ;
#10854=VECTOR('',#46221,1000.) ;
#10855=VECTOR('',#46224,1000.) ;
#10856=VECTOR('',#46227,1000.) ;
#10857=VECTOR('',#46232,999.999999999999) ;
#10858=VECTOR('',#46235,1000.) ;
#10859=VECTOR('',#46238,1000.) ;
#10860=VECTOR('',#46245,1000.) ;
#10861=VECTOR('',#46248,1000.) ;
#10862=VECTOR('',#46251,1000.) ;
#12619=CIRCLE('',#36383,1.5) ;
#12620=CIRCLE('',#36399,1.17524047358084) ;
#12621=CIRCLE('',#36416,1.17524047358084) ;
#12622=CIRCLE('',#36418,1.17524047358084) ;
#12623=CIRCLE('',#36420,1.17524047358084) ;
#12624=CIRCLE('',#36422,1.5) ;
#12625=CIRCLE('',#36424,0.930607966083863) ;
#12626=CIRCLE('',#36425,1.4329043419966) ;
#12627=CIRCLE('',#36427,0.930607966083863) ;
#12628=CIRCLE('',#36428,1.4329043419966) ;
#12629=CIRCLE('',#36430,2.85397350993377) ;
#12630=CIRCLE('',#36431,0.449999999999999) ;
#12631=CIRCLE('',#36432,3.) ;
#12632=CIRCLE('',#36433,3.) ;
#12633=CIRCLE('',#36435,1.4329043419966) ;
#12634=CIRCLE('',#36436,4.22489174394716) ;
#12635=CIRCLE('',#36437,4.21532021625621) ;
#12636=CIRCLE('',#36438,4.21532021625621) ;
#12637=CIRCLE('',#36439,4.22489174394716) ;
#12638=CIRCLE('',#36440,4.22489174394716) ;
#12639=CIRCLE('',#36441,4.21532021625621) ;
#12640=CIRCLE('',#36442,4.21532021625621) ;
#12641=CIRCLE('',#36443,4.22489174394716) ;
#12642=CIRCLE('',#36444,4.22489174394716) ;
#12643=CIRCLE('',#36445,4.21532021625621) ;
#12644=CIRCLE('',#36446,4.21532021625621) ;
#12645=CIRCLE('',#36447,4.22489174394717) ;
#12646=CIRCLE('',#36448,1.4329043419966) ;
#12647=CIRCLE('',#36449,4.22489174394716) ;
#12648=CIRCLE('',#36450,4.21532021625621) ;
#12649=CIRCLE('',#36451,4.21532021625621) ;
#12650=CIRCLE('',#36452,4.22489174394716) ;
#12651=CIRCLE('',#36454,3.) ;
#12652=CIRCLE('',#36455,3.) ;
#12653=CIRCLE('',#36457,0.45) ;
#12654=CIRCLE('',#36458,2.55) ;
#12655=CIRCLE('',#36462,0.930607966083863) ;
#12656=CIRCLE('',#36468,0.930607966083863) ;
#15460=VERTEX_POINT('',#81798) ;
#15461=VERTEX_POINT('',#81799) ;
#15462=VERTEX_POINT('',#81801) ;
#15463=VERTEX_POINT('',#81826) ;
#15464=VERTEX_POINT('',#81851) ;
#15465=VERTEX_POINT('',#81852) ;
#15466=VERTEX_POINT('',#81927) ;
#15467=VERTEX_POINT('',#81928) ;
#15468=VERTEX_POINT('',#82005) ;
#15469=VERTEX_POINT('',#82006) ;
#15470=VERTEX_POINT('',#82083) ;
#15471=VERTEX_POINT('',#82084) ;
#15472=VERTEX_POINT('',#82159) ;
#15473=VERTEX_POINT('',#82160) ;
#15474=VERTEX_POINT('',#82235) ;
#15475=VERTEX_POINT('',#82236) ;
#15476=VERTEX_POINT('',#82311) ;
#15477=VERTEX_POINT('',#82312) ;
#15478=VERTEX_POINT('',#82387) ;
#15479=VERTEX_POINT('',#82388) ;
#15480=VERTEX_POINT('',#82465) ;
#15481=VERTEX_POINT('',#82466) ;
#15482=VERTEX_POINT('',#82541) ;
#15483=VERTEX_POINT('',#82542) ;
#15484=VERTEX_POINT('',#82619) ;
#15485=VERTEX_POINT('',#82620) ;
#15486=VERTEX_POINT('',#82695) ;
#15487=VERTEX_POINT('',#82696) ;
#15488=VERTEX_POINT('',#82771) ;
#15489=VERTEX_POINT('',#82772) ;
#15490=VERTEX_POINT('',#82847) ;
#15491=VERTEX_POINT('',#82848) ;
#15492=VERTEX_POINT('',#82923) ;
#15493=VERTEX_POINT('',#82924) ;
#15494=VERTEX_POINT('',#82926) ;
#15495=VERTEX_POINT('',#82959) ;
#15496=VERTEX_POINT('',#82961) ;
#15497=VERTEX_POINT('',#83072) ;
#15498=VERTEX_POINT('',#83073) ;
#15499=VERTEX_POINT('',#83148) ;
#15500=VERTEX_POINT('',#83149) ;
#15501=VERTEX_POINT('',#83224) ;
#15502=VERTEX_POINT('',#83225) ;
#15503=VERTEX_POINT('',#83300) ;
#15504=VERTEX_POINT('',#83301) ;
#15505=VERTEX_POINT('',#83376) ;
#15506=VERTEX_POINT('',#83377) ;
#15507=VERTEX_POINT('',#83454) ;
#15508=VERTEX_POINT('',#83455) ;
#15509=VERTEX_POINT('',#83530) ;
#15510=VERTEX_POINT('',#83531) ;
#15511=VERTEX_POINT('',#83606) ;
#15512=VERTEX_POINT('',#83607) ;
#15513=VERTEX_POINT('',#83684) ;
#15514=VERTEX_POINT('',#83685) ;
#15515=VERTEX_POINT('',#83760) ;
#15516=VERTEX_POINT('',#83761) ;
#15517=VERTEX_POINT('',#83836) ;
#15518=VERTEX_POINT('',#83837) ;
#15519=VERTEX_POINT('',#83912) ;
#15520=VERTEX_POINT('',#83913) ;
#15521=VERTEX_POINT('',#83988) ;
#15522=VERTEX_POINT('',#83989) ;
#15523=VERTEX_POINT('',#84066) ;
#15524=VERTEX_POINT('',#84067) ;
#15525=VERTEX_POINT('',#84142) ;
#15526=VERTEX_POINT('',#84143) ;
#15527=VERTEX_POINT('',#84220) ;
#15528=VERTEX_POINT('',#84221) ;
#15529=VERTEX_POINT('',#84223) ;
#15530=VERTEX_POINT('',#84286) ;
#15531=VERTEX_POINT('',#84301) ;
#15532=VERTEX_POINT('',#84314) ;
#15533=VERTEX_POINT('',#84345) ;
#15534=VERTEX_POINT('',#84376) ;
#15535=VERTEX_POINT('',#84377) ;
#15536=VERTEX_POINT('',#84379) ;
#15537=VERTEX_POINT('',#84383) ;
#15538=VERTEX_POINT('',#84389) ;
#15539=VERTEX_POINT('',#84390) ;
#15540=VERTEX_POINT('',#84392) ;
#15541=VERTEX_POINT('',#84396) ;
#15542=VERTEX_POINT('',#84402) ;
#15543=VERTEX_POINT('',#84404) ;
#15544=VERTEX_POINT('',#84406) ;
#15545=VERTEX_POINT('',#84410) ;
#15546=VERTEX_POINT('',#84411) ;
#15547=VERTEX_POINT('',#84413) ;
#15548=VERTEX_POINT('',#84415) ;
#15549=VERTEX_POINT('',#84417) ;
#15550=VERTEX_POINT('',#84420) ;
#15551=VERTEX_POINT('',#84422) ;
#15552=VERTEX_POINT('',#84424) ;
#15553=VERTEX_POINT('',#84427) ;
#15554=VERTEX_POINT('',#84429) ;
#15555=VERTEX_POINT('',#84431) ;
#15556=VERTEX_POINT('',#84433) ;
#15557=VERTEX_POINT('',#84435) ;
#15558=VERTEX_POINT('',#84437) ;
#15559=VERTEX_POINT('',#84439) ;
#15560=VERTEX_POINT('',#84441) ;
#15561=VERTEX_POINT('',#84445) ;
#15562=VERTEX_POINT('',#84446) ;
#15563=VERTEX_POINT('',#84451) ;
#15564=VERTEX_POINT('',#85384) ;
#15565=VERTEX_POINT('',#85388) ;
#15566=VERTEX_POINT('',#85394) ;
#15567=VERTEX_POINT('',#85398) ;
#15568=VERTEX_POINT('',#85402) ;
#15569=VERTEX_POINT('',#85408) ;
#15570=VERTEX_POINT('',#85410) ;
#15571=VERTEX_POINT('',#85412) ;
#15572=VERTEX_POINT('',#85414) ;
#15573=VERTEX_POINT('',#85416) ;
#15574=VERTEX_POINT('',#85418) ;
#15575=VERTEX_POINT('',#85420) ;
#15576=VERTEX_POINT('',#85422) ;
#15577=VERTEX_POINT('',#85424) ;
#15578=VERTEX_POINT('',#85427) ;
#15579=VERTEX_POINT('',#85429) ;
#20175=EDGE_CURVE('',#15460,#15461,#8482,.T.) ;
#20176=EDGE_CURVE('',#15462,#15460,#1630,.F.) ;
#20177=EDGE_CURVE('',#15463,#15462,#12619,.T.) ;
#20178=EDGE_CURVE('',#15463,#15461,#1631,.T.) ;
#20179=EDGE_CURVE('',#15464,#15465,#8483,.T.) ;
#20180=EDGE_CURVE('',#15460,#15464,#1632,.F.) ;
#20181=EDGE_CURVE('',#15461,#15465,#1633,.T.) ;
#20182=EDGE_CURVE('',#15466,#15467,#8484,.T.) ;
#20183=EDGE_CURVE('',#15464,#15466,#1634,.F.) ;
#20184=EDGE_CURVE('',#15465,#15467,#1635,.T.) ;
#20185=EDGE_CURVE('',#15468,#15469,#8485,.T.) ;
#20186=EDGE_CURVE('',#15466,#15468,#1636,.F.) ;
#20187=EDGE_CURVE('',#15467,#15469,#1637,.T.) ;
#20188=EDGE_CURVE('',#15470,#15471,#8486,.T.) ;
#20189=EDGE_CURVE('',#15468,#15470,#1638,.F.) ;
#20190=EDGE_CURVE('',#15469,#15471,#1639,.T.) ;
#20191=EDGE_CURVE('',#15472,#15473,#8487,.T.) ;
#20192=EDGE_CURVE('',#15470,#15472,#1640,.F.) ;
#20193=EDGE_CURVE('',#15471,#15473,#1641,.T.) ;
#20194=EDGE_CURVE('',#15474,#15475,#8488,.T.) ;
#20195=EDGE_CURVE('',#15472,#15474,#1642,.F.) ;
#20196=EDGE_CURVE('',#15473,#15475,#1643,.T.) ;
#20197=EDGE_CURVE('',#15476,#15477,#8489,.T.) ;
#20198=EDGE_CURVE('',#15474,#15476,#1644,.F.) ;
#20199=EDGE_CURVE('',#15475,#15477,#1645,.T.) ;
#20200=EDGE_CURVE('',#15478,#15479,#8490,.T.) ;
#20201=EDGE_CURVE('',#15476,#15478,#1646,.F.) ;
#20202=EDGE_CURVE('',#15477,#15479,#1647,.T.) ;
#20203=EDGE_CURVE('',#15480,#15481,#8491,.T.) ;
#20204=EDGE_CURVE('',#15478,#15480,#1648,.F.) ;
#20205=EDGE_CURVE('',#15479,#15481,#1649,.T.) ;
#20206=EDGE_CURVE('',#15482,#15483,#8492,.T.) ;
#20207=EDGE_CURVE('',#15480,#15482,#1650,.F.) ;
#20208=EDGE_CURVE('',#15481,#15483,#1651,.T.) ;
#20209=EDGE_CURVE('',#15484,#15485,#8493,.T.) ;
#20210=EDGE_CURVE('',#15482,#15484,#1652,.F.) ;
#20211=EDGE_CURVE('',#15483,#15485,#1653,.T.) ;
#20212=EDGE_CURVE('',#15486,#15487,#8494,.T.) ;
#20213=EDGE_CURVE('',#15484,#15486,#1654,.F.) ;
#20214=EDGE_CURVE('',#15485,#15487,#1655,.T.) ;
#20215=EDGE_CURVE('',#15488,#15489,#8495,.T.) ;
#20216=EDGE_CURVE('',#15486,#15488,#1656,.F.) ;
#20217=EDGE_CURVE('',#15487,#15489,#1657,.T.) ;
#20218=EDGE_CURVE('',#15490,#15491,#8496,.T.) ;
#20219=EDGE_CURVE('',#15488,#15490,#1658,.F.) ;
#20220=EDGE_CURVE('',#15489,#15491,#1659,.T.) ;
#20221=EDGE_CURVE('',#15492,#15493,#8497,.T.) ;
#20222=EDGE_CURVE('',#15494,#15492,#1660,.F.) ;
#20223=EDGE_CURVE('',#15494,#15495,#12620,.T.) ;
#20224=EDGE_CURVE('',#15496,#15495,#1661,.F.) ;
#20225=EDGE_CURVE('',#15496,#15493,#1662,.T.) ;
#20226=EDGE_CURVE('',#15497,#15498,#8498,.T.) ;
#20227=EDGE_CURVE('',#15492,#15497,#1663,.F.) ;
#20228=EDGE_CURVE('',#15493,#15498,#1664,.T.) ;
#20229=EDGE_CURVE('',#15499,#15500,#8499,.T.) ;
#20230=EDGE_CURVE('',#15497,#15499,#1665,.F.) ;
#20231=EDGE_CURVE('',#15498,#15500,#1666,.T.) ;
#20232=EDGE_CURVE('',#15501,#15502,#8500,.T.) ;
#20233=EDGE_CURVE('',#15499,#15501,#1667,.F.) ;
#20234=EDGE_CURVE('',#15500,#15502,#1668,.T.) ;
#20235=EDGE_CURVE('',#15503,#15504,#8501,.T.) ;
#20236=EDGE_CURVE('',#15501,#15503,#1669,.F.) ;
#20237=EDGE_CURVE('',#15502,#15504,#1670,.T.) ;
#20238=EDGE_CURVE('',#15505,#15506,#8502,.T.) ;
#20239=EDGE_CURVE('',#15503,#15505,#1671,.F.) ;
#20240=EDGE_CURVE('',#15504,#15506,#1672,.T.) ;
#20241=EDGE_CURVE('',#15507,#15508,#8503,.T.) ;
#20242=EDGE_CURVE('',#15505,#15507,#1673,.F.) ;
#20243=EDGE_CURVE('',#15506,#15508,#1674,.T.) ;
#20244=EDGE_CURVE('',#15509,#15510,#8504,.T.) ;
#20245=EDGE_CURVE('',#15507,#15509,#1675,.F.) ;
#20246=EDGE_CURVE('',#15508,#15510,#1676,.T.) ;
#20247=EDGE_CURVE('',#15511,#15512,#8505,.T.) ;
#20248=EDGE_CURVE('',#15509,#15511,#1677,.F.) ;
#20249=EDGE_CURVE('',#15510,#15512,#1678,.T.) ;
#20250=EDGE_CURVE('',#15513,#15514,#8506,.T.) ;
#20251=EDGE_CURVE('',#15511,#15513,#1679,.F.) ;
#20252=EDGE_CURVE('',#15512,#15514,#1680,.T.) ;
#20253=EDGE_CURVE('',#15515,#15516,#8507,.T.) ;
#20254=EDGE_CURVE('',#15513,#15515,#1681,.F.) ;
#20255=EDGE_CURVE('',#15514,#15516,#1682,.T.) ;
#20256=EDGE_CURVE('',#15517,#15518,#8508,.T.) ;
#20257=EDGE_CURVE('',#15515,#15517,#1683,.F.) ;
#20258=EDGE_CURVE('',#15516,#15518,#1684,.T.) ;
#20259=EDGE_CURVE('',#15519,#15520,#8509,.T.) ;
#20260=EDGE_CURVE('',#15517,#15519,#1685,.F.) ;
#20261=EDGE_CURVE('',#15518,#15520,#1686,.T.) ;
#20262=EDGE_CURVE('',#15521,#15522,#8510,.T.) ;
#20263=EDGE_CURVE('',#15519,#15521,#1687,.F.) ;
#20264=EDGE_CURVE('',#15520,#15522,#1688,.T.) ;
#20265=EDGE_CURVE('',#15523,#15524,#8511,.T.) ;
#20266=EDGE_CURVE('',#15521,#15523,#1689,.F.) ;
#20267=EDGE_CURVE('',#15522,#15524,#1690,.T.) ;
#20268=EDGE_CURVE('',#15525,#15526,#8512,.T.) ;
#20269=EDGE_CURVE('',#15523,#15525,#1691,.F.) ;
#20270=EDGE_CURVE('',#15524,#15526,#1692,.T.) ;
#20271=EDGE_CURVE('',#15527,#15528,#8513,.T.) ;
#20272=EDGE_CURVE('',#15527,#15529,#1693,.F.) ;
#20273=EDGE_CURVE('',#15495,#15529,#1694,.F.) ;
#20274=EDGE_CURVE('',#15495,#15528,#12621,.T.) ;
#20275=EDGE_CURVE('',#15528,#15494,#12622,.T.) ;
#20276=EDGE_CURVE('',#15494,#15463,#1695,.T.) ;
#20277=EDGE_CURVE('',#15462,#15527,#1696,.F.) ;
#20278=EDGE_CURVE('',#15526,#15530,#1697,.T.) ;
#20279=EDGE_CURVE('',#15531,#15530,#12623,.T.) ;
#20280=EDGE_CURVE('',#15525,#15531,#1698,.F.) ;
#20281=EDGE_CURVE('',#15491,#15532,#1699,.T.) ;
#20282=EDGE_CURVE('',#15533,#15532,#12624,.T.) ;
#20283=EDGE_CURVE('',#15490,#15533,#1700,.F.) ;
#20284=EDGE_CURVE('',#15534,#15535,#12625,.T.) ;
#20285=EDGE_CURVE('',#15534,#15536,#805,.T.) ;
#20286=EDGE_CURVE('',#15536,#15537,#12626,.T.) ;
#20287=EDGE_CURVE('',#15535,#15537,#806,.T.) ;
#20288=EDGE_CURVE('',#15538,#15539,#12627,.T.) ;
#20289=EDGE_CURVE('',#15538,#15540,#807,.T.) ;
#20290=EDGE_CURVE('',#15540,#15541,#12628,.T.) ;
#20291=EDGE_CURVE('',#15539,#15541,#808,.T.) ;
#20292=EDGE_CURVE('',#15542,#15542,#12629,.T.) ;
#20293=EDGE_CURVE('',#15542,#15543,#12630,.T.) ;
#20294=EDGE_CURVE('',#15543,#15544,#12631,.T.) ;
#20295=EDGE_CURVE('',#15544,#15543,#12632,.T.) ;
#20296=EDGE_CURVE('',#15545,#15546,#12633,.T.) ;
#20297=EDGE_CURVE('',#15547,#15545,#12634,.T.) ;
#20298=EDGE_CURVE('',#15548,#15547,#12635,.T.) ;
#20299=EDGE_CURVE('',#15549,#15548,#12636,.T.) ;
#20300=EDGE_CURVE('',#15541,#15549,#12637,.T.) ;
#20301=EDGE_CURVE('',#15550,#15540,#12638,.T.) ;
#20302=EDGE_CURVE('',#15551,#15550,#12639,.T.) ;
#20303=EDGE_CURVE('',#15552,#15551,#12640,.T.) ;
#20304=EDGE_CURVE('',#15537,#15552,#12641,.T.) ;
#20305=EDGE_CURVE('',#15553,#15536,#12642,.T.) ;
#20306=EDGE_CURVE('',#15554,#15553,#12643,.T.) ;
#20307=EDGE_CURVE('',#15555,#15554,#12644,.T.) ;
#20308=EDGE_CURVE('',#15556,#15555,#12645,.T.) ;
#20309=EDGE_CURVE('',#15557,#15556,#12646,.T.) ;
#20310=EDGE_CURVE('',#15558,#15557,#12647,.T.) ;
#20311=EDGE_CURVE('',#15559,#15558,#12648,.T.) ;
#20312=EDGE_CURVE('',#15560,#15559,#12649,.T.) ;
#20313=EDGE_CURVE('',#15546,#15560,#12650,.T.) ;
#20314=EDGE_CURVE('',#15561,#15562,#12651,.T.) ;
#20315=EDGE_CURVE('',#15562,#15544,#8514,.T.) ;
#20316=EDGE_CURVE('',#15562,#15561,#12652,.T.) ;
#20317=EDGE_CURVE('',#15561,#15563,#12653,.T.) ;
#20318=EDGE_CURVE('',#15563,#15563,#12654,.T.) ;
#20319=EDGE_CURVE('',#15532,#15531,#1701,.T.) ;
#20320=EDGE_CURVE('',#15530,#15533,#1702,.T.) ;
#20321=EDGE_CURVE('',#15529,#15496,#8515,.T.) ;
#20322=EDGE_CURVE('',#15564,#15546,#809,.T.) ;
#20323=EDGE_CURVE('',#15565,#15564,#12655,.T.) ;
#20324=EDGE_CURVE('',#15565,#15545,#810,.T.) ;
#20325=EDGE_CURVE('',#15566,#15565,#8516,.T.) ;
#20326=EDGE_CURVE('',#15566,#15547,#8517,.T.) ;
#20327=EDGE_CURVE('',#15567,#15566,#8518,.T.) ;
#20328=EDGE_CURVE('',#15567,#15548,#8519,.T.) ;
#20329=EDGE_CURVE('',#15568,#15567,#8520,.T.) ;
#20330=EDGE_CURVE('',#15568,#15549,#8521,.T.) ;
#20331=EDGE_CURVE('',#15539,#15568,#8522,.T.) ;
#20332=EDGE_CURVE('',#15569,#15538,#8523,.T.) ;
#20333=EDGE_CURVE('',#15564,#15570,#8524,.T.) ;
#20334=EDGE_CURVE('',#15570,#15571,#8525,.T.) ;
#20335=EDGE_CURVE('',#15571,#15572,#8526,.T.) ;
#20336=EDGE_CURVE('',#15572,#15573,#8527,.T.) ;
#20337=EDGE_CURVE('',#15573,#15574,#12656,.T.) ;
#20338=EDGE_CURVE('',#15574,#15575,#8528,.T.) ;
#20339=EDGE_CURVE('',#15575,#15576,#8529,.T.) ;
#20340=EDGE_CURVE('',#15576,#15577,#8530,.T.) ;
#20341=EDGE_CURVE('',#15577,#15534,#8531,.T.) ;
#20342=EDGE_CURVE('',#15535,#15578,#8532,.T.) ;
#20343=EDGE_CURVE('',#15578,#15579,#8533,.T.) ;
#20344=EDGE_CURVE('',#15579,#15569,#8534,.T.) ;
#20345=EDGE_CURVE('',#15569,#15550,#8535,.T.) ;
#20346=EDGE_CURVE('',#15579,#15551,#8536,.T.) ;
#20347=EDGE_CURVE('',#15578,#15552,#8537,.T.) ;
#20348=EDGE_CURVE('',#15577,#15553,#8538,.T.) ;
#20349=EDGE_CURVE('',#15576,#15554,#8539,.T.) ;
#20350=EDGE_CURVE('',#15575,#15555,#8540,.T.) ;
#20351=EDGE_CURVE('',#15574,#15556,#811,.T.) ;
#20352=EDGE_CURVE('',#15573,#15557,#812,.T.) ;
#20353=EDGE_CURVE('',#15572,#15558,#8541,.T.) ;
#20354=EDGE_CURVE('',#15571,#15559,#8542,.T.) ;
#20355=EDGE_CURVE('',#15570,#15560,#8543,.T.) ;
#29538=ORIENTED_EDGE('',*,*,#20175,.F.) ;
#29539=ORIENTED_EDGE('',*,*,#20176,.F.) ;
#29540=ORIENTED_EDGE('',*,*,#20177,.F.) ;
#29541=ORIENTED_EDGE('',*,*,#20178,.T.) ;
#29542=ORIENTED_EDGE('',*,*,#20179,.F.) ;
#29543=ORIENTED_EDGE('',*,*,#20180,.F.) ;
#29544=ORIENTED_EDGE('',*,*,#20175,.T.) ;
#29545=ORIENTED_EDGE('',*,*,#20181,.T.) ;
#29546=ORIENTED_EDGE('',*,*,#20182,.F.) ;
#29547=ORIENTED_EDGE('',*,*,#20183,.F.) ;
#29548=ORIENTED_EDGE('',*,*,#20179,.T.) ;
#29549=ORIENTED_EDGE('',*,*,#20184,.T.) ;
#29550=ORIENTED_EDGE('',*,*,#20185,.F.) ;
#29551=ORIENTED_EDGE('',*,*,#20186,.F.) ;
#29552=ORIENTED_EDGE('',*,*,#20182,.T.) ;
#29553=ORIENTED_EDGE('',*,*,#20187,.T.) ;
#29554=ORIENTED_EDGE('',*,*,#20188,.F.) ;
#29555=ORIENTED_EDGE('',*,*,#20189,.F.) ;
#29556=ORIENTED_EDGE('',*,*,#20185,.T.) ;
#29557=ORIENTED_EDGE('',*,*,#20190,.T.) ;
#29558=ORIENTED_EDGE('',*,*,#20191,.F.) ;
#29559=ORIENTED_EDGE('',*,*,#20192,.F.) ;
#29560=ORIENTED_EDGE('',*,*,#20188,.T.) ;
#29561=ORIENTED_EDGE('',*,*,#20193,.T.) ;
#29562=ORIENTED_EDGE('',*,*,#20194,.F.) ;
#29563=ORIENTED_EDGE('',*,*,#20195,.F.) ;
#29564=ORIENTED_EDGE('',*,*,#20191,.T.) ;
#29565=ORIENTED_EDGE('',*,*,#20196,.T.) ;
#29566=ORIENTED_EDGE('',*,*,#20197,.F.) ;
#29567=ORIENTED_EDGE('',*,*,#20198,.F.) ;
#29568=ORIENTED_EDGE('',*,*,#20194,.T.) ;
#29569=ORIENTED_EDGE('',*,*,#20199,.T.) ;
#29570=ORIENTED_EDGE('',*,*,#20200,.F.) ;
#29571=ORIENTED_EDGE('',*,*,#20201,.F.) ;
#29572=ORIENTED_EDGE('',*,*,#20197,.T.) ;
#29573=ORIENTED_EDGE('',*,*,#20202,.T.) ;
#29574=ORIENTED_EDGE('',*,*,#20203,.F.) ;
#29575=ORIENTED_EDGE('',*,*,#20204,.F.) ;
#29576=ORIENTED_EDGE('',*,*,#20200,.T.) ;
#29577=ORIENTED_EDGE('',*,*,#20205,.T.) ;
#29578=ORIENTED_EDGE('',*,*,#20206,.F.) ;
#29579=ORIENTED_EDGE('',*,*,#20207,.F.) ;
#29580=ORIENTED_EDGE('',*,*,#20203,.T.) ;
#29581=ORIENTED_EDGE('',*,*,#20208,.T.) ;
#29582=ORIENTED_EDGE('',*,*,#20209,.F.) ;
#29583=ORIENTED_EDGE('',*,*,#20210,.F.) ;
#29584=ORIENTED_EDGE('',*,*,#20206,.T.) ;
#29585=ORIENTED_EDGE('',*,*,#20211,.T.) ;
#29586=ORIENTED_EDGE('',*,*,#20212,.F.) ;
#29587=ORIENTED_EDGE('',*,*,#20213,.F.) ;
#29588=ORIENTED_EDGE('',*,*,#20209,.T.) ;
#29589=ORIENTED_EDGE('',*,*,#20214,.T.) ;
#29590=ORIENTED_EDGE('',*,*,#20215,.F.) ;
#29591=ORIENTED_EDGE('',*,*,#20216,.F.) ;
#29592=ORIENTED_EDGE('',*,*,#20212,.T.) ;
#29593=ORIENTED_EDGE('',*,*,#20217,.T.) ;
#29594=ORIENTED_EDGE('',*,*,#20218,.F.) ;
#29595=ORIENTED_EDGE('',*,*,#20219,.F.) ;
#29596=ORIENTED_EDGE('',*,*,#20215,.T.) ;
#29597=ORIENTED_EDGE('',*,*,#20220,.T.) ;
#29598=ORIENTED_EDGE('',*,*,#20221,.F.) ;
#29599=ORIENTED_EDGE('',*,*,#20222,.F.) ;
#29600=ORIENTED_EDGE('',*,*,#20223,.T.) ;
#29601=ORIENTED_EDGE('',*,*,#20224,.F.) ;
#29602=ORIENTED_EDGE('',*,*,#20225,.T.) ;
#29603=ORIENTED_EDGE('',*,*,#20226,.F.) ;
#29604=ORIENTED_EDGE('',*,*,#20227,.F.) ;
#29605=ORIENTED_EDGE('',*,*,#20221,.T.) ;
#29606=ORIENTED_EDGE('',*,*,#20228,.T.) ;
#29607=ORIENTED_EDGE('',*,*,#20229,.F.) ;
#29608=ORIENTED_EDGE('',*,*,#20230,.F.) ;
#29609=ORIENTED_EDGE('',*,*,#20226,.T.) ;
#29610=ORIENTED_EDGE('',*,*,#20231,.T.) ;
#29611=ORIENTED_EDGE('',*,*,#20232,.F.) ;
#29612=ORIENTED_EDGE('',*,*,#20233,.F.) ;
#29613=ORIENTED_EDGE('',*,*,#20229,.T.) ;
#29614=ORIENTED_EDGE('',*,*,#20234,.T.) ;
#29615=ORIENTED_EDGE('',*,*,#20235,.F.) ;
#29616=ORIENTED_EDGE('',*,*,#20236,.F.) ;
#29617=ORIENTED_EDGE('',*,*,#20232,.T.) ;
#29618=ORIENTED_EDGE('',*,*,#20237,.T.) ;
#29619=ORIENTED_EDGE('',*,*,#20238,.F.) ;
#29620=ORIENTED_EDGE('',*,*,#20239,.F.) ;
#29621=ORIENTED_EDGE('',*,*,#20235,.T.) ;
#29622=ORIENTED_EDGE('',*,*,#20240,.T.) ;
#29623=ORIENTED_EDGE('',*,*,#20241,.F.) ;
#29624=ORIENTED_EDGE('',*,*,#20242,.F.) ;
#29625=ORIENTED_EDGE('',*,*,#20238,.T.) ;
#29626=ORIENTED_EDGE('',*,*,#20243,.T.) ;
#29627=ORIENTED_EDGE('',*,*,#20244,.F.) ;
#29628=ORIENTED_EDGE('',*,*,#20245,.F.) ;
#29629=ORIENTED_EDGE('',*,*,#20241,.T.) ;
#29630=ORIENTED_EDGE('',*,*,#20246,.T.) ;
#29631=ORIENTED_EDGE('',*,*,#20247,.F.) ;
#29632=ORIENTED_EDGE('',*,*,#20248,.F.) ;
#29633=ORIENTED_EDGE('',*,*,#20244,.T.) ;
#29634=ORIENTED_EDGE('',*,*,#20249,.T.) ;
#29635=ORIENTED_EDGE('',*,*,#20250,.F.) ;
#29636=ORIENTED_EDGE('',*,*,#20251,.F.) ;
#29637=ORIENTED_EDGE('',*,*,#20247,.T.) ;
#29638=ORIENTED_EDGE('',*,*,#20252,.T.) ;
#29639=ORIENTED_EDGE('',*,*,#20253,.F.) ;
#29640=ORIENTED_EDGE('',*,*,#20254,.F.) ;
#29641=ORIENTED_EDGE('',*,*,#20250,.T.) ;
#29642=ORIENTED_EDGE('',*,*,#20255,.T.) ;
#29643=ORIENTED_EDGE('',*,*,#20256,.F.) ;
#29644=ORIENTED_EDGE('',*,*,#20257,.F.) ;
#29645=ORIENTED_EDGE('',*,*,#20253,.T.) ;
#29646=ORIENTED_EDGE('',*,*,#20258,.T.) ;
#29647=ORIENTED_EDGE('',*,*,#20259,.F.) ;
#29648=ORIENTED_EDGE('',*,*,#20260,.F.) ;
#29649=ORIENTED_EDGE('',*,*,#20256,.T.) ;
#29650=ORIENTED_EDGE('',*,*,#20261,.T.) ;
#29651=ORIENTED_EDGE('',*,*,#20262,.F.) ;
#29652=ORIENTED_EDGE('',*,*,#20263,.F.) ;
#29653=ORIENTED_EDGE('',*,*,#20259,.T.) ;
#29654=ORIENTED_EDGE('',*,*,#20264,.T.) ;
#29655=ORIENTED_EDGE('',*,*,#20265,.F.) ;
#29656=ORIENTED_EDGE('',*,*,#20266,.F.) ;
#29657=ORIENTED_EDGE('',*,*,#20262,.T.) ;
#29658=ORIENTED_EDGE('',*,*,#20267,.T.) ;
#29659=ORIENTED_EDGE('',*,*,#20268,.F.) ;
#29660=ORIENTED_EDGE('',*,*,#20269,.F.) ;
#29661=ORIENTED_EDGE('',*,*,#20265,.T.) ;
#29662=ORIENTED_EDGE('',*,*,#20270,.T.) ;
#29663=ORIENTED_EDGE('',*,*,#20271,.F.) ;
#29664=ORIENTED_EDGE('',*,*,#20272,.T.) ;
#29665=ORIENTED_EDGE('',*,*,#20273,.F.) ;
#29666=ORIENTED_EDGE('',*,*,#20274,.T.) ;
#29667=ORIENTED_EDGE('',*,*,#20271,.T.) ;
#29668=ORIENTED_EDGE('',*,*,#20275,.T.) ;
#29669=ORIENTED_EDGE('',*,*,#20276,.T.) ;
#29670=ORIENTED_EDGE('',*,*,#20177,.T.) ;
#29671=ORIENTED_EDGE('',*,*,#20277,.T.) ;
#29672=ORIENTED_EDGE('',*,*,#20268,.T.) ;
#29673=ORIENTED_EDGE('',*,*,#20278,.T.) ;
#29674=ORIENTED_EDGE('',*,*,#20279,.F.) ;
#29675=ORIENTED_EDGE('',*,*,#20280,.F.) ;
#29676=ORIENTED_EDGE('',*,*,#20218,.T.) ;
#29677=ORIENTED_EDGE('',*,*,#20281,.T.) ;
#29678=ORIENTED_EDGE('',*,*,#20282,.F.) ;
#29679=ORIENTED_EDGE('',*,*,#20283,.F.) ;
#29680=ORIENTED_EDGE('',*,*,#20284,.F.) ;
#29681=ORIENTED_EDGE('',*,*,#20285,.T.) ;
#29682=ORIENTED_EDGE('',*,*,#20286,.T.) ;
#29683=ORIENTED_EDGE('',*,*,#20287,.F.) ;
#29684=ORIENTED_EDGE('',*,*,#20288,.F.) ;
#29685=ORIENTED_EDGE('',*,*,#20289,.T.) ;
#29686=ORIENTED_EDGE('',*,*,#20290,.T.) ;
#29687=ORIENTED_EDGE('',*,*,#20291,.F.) ;
#29688=ORIENTED_EDGE('',*,*,#20292,.F.) ;
#29689=ORIENTED_EDGE('',*,*,#20293,.T.) ;
#29690=ORIENTED_EDGE('',*,*,#20294,.T.) ;
#29691=ORIENTED_EDGE('',*,*,#20295,.T.) ;
#29692=ORIENTED_EDGE('',*,*,#20293,.F.) ;
#29693=ORIENTED_EDGE('',*,*,#20292,.T.) ;
#29694=ORIENTED_EDGE('',*,*,#20296,.F.) ;
#29695=ORIENTED_EDGE('',*,*,#20297,.F.) ;
#29696=ORIENTED_EDGE('',*,*,#20298,.F.) ;
#29697=ORIENTED_EDGE('',*,*,#20299,.F.) ;
#29698=ORIENTED_EDGE('',*,*,#20300,.F.) ;
#29699=ORIENTED_EDGE('',*,*,#20290,.F.) ;
#29700=ORIENTED_EDGE('',*,*,#20301,.F.) ;
#29701=ORIENTED_EDGE('',*,*,#20302,.F.) ;
#29702=ORIENTED_EDGE('',*,*,#20303,.F.) ;
#29703=ORIENTED_EDGE('',*,*,#20304,.F.) ;
#29704=ORIENTED_EDGE('',*,*,#20286,.F.) ;
#29705=ORIENTED_EDGE('',*,*,#20305,.F.) ;
#29706=ORIENTED_EDGE('',*,*,#20306,.F.) ;
#29707=ORIENTED_EDGE('',*,*,#20307,.F.) ;
#29708=ORIENTED_EDGE('',*,*,#20308,.F.) ;
#29709=ORIENTED_EDGE('',*,*,#20309,.F.) ;
#29710=ORIENTED_EDGE('',*,*,#20310,.F.) ;
#29711=ORIENTED_EDGE('',*,*,#20311,.F.) ;
#29712=ORIENTED_EDGE('',*,*,#20312,.F.) ;
#29713=ORIENTED_EDGE('',*,*,#20313,.F.) ;
#29714=ORIENTED_EDGE('',*,*,#20314,.T.) ;
#29715=ORIENTED_EDGE('',*,*,#20315,.T.) ;
#29716=ORIENTED_EDGE('',*,*,#20294,.F.) ;
#29717=ORIENTED_EDGE('',*,*,#20295,.F.) ;
#29718=ORIENTED_EDGE('',*,*,#20315,.F.) ;
#29719=ORIENTED_EDGE('',*,*,#20316,.T.) ;
#29720=ORIENTED_EDGE('',*,*,#20314,.F.) ;
#29721=ORIENTED_EDGE('',*,*,#20317,.T.) ;
#29722=ORIENTED_EDGE('',*,*,#20318,.T.) ;
#29723=ORIENTED_EDGE('',*,*,#20317,.F.) ;
#29724=ORIENTED_EDGE('',*,*,#20316,.F.) ;
#29725=ORIENTED_EDGE('',*,*,#20318,.F.) ;
#29726=ORIENTED_EDGE('',*,*,#20282,.T.) ;
#29727=ORIENTED_EDGE('',*,*,#20319,.T.) ;
#29728=ORIENTED_EDGE('',*,*,#20279,.T.) ;
#29729=ORIENTED_EDGE('',*,*,#20320,.T.) ;
#29730=ORIENTED_EDGE('',*,*,#20320,.F.) ;
#29731=ORIENTED_EDGE('',*,*,#20278,.F.) ;
#29732=ORIENTED_EDGE('',*,*,#20270,.F.) ;
#29733=ORIENTED_EDGE('',*,*,#20267,.F.) ;
#29734=ORIENTED_EDGE('',*,*,#20264,.F.) ;
#29735=ORIENTED_EDGE('',*,*,#20261,.F.) ;
#29736=ORIENTED_EDGE('',*,*,#20258,.F.) ;
#29737=ORIENTED_EDGE('',*,*,#20255,.F.) ;
#29738=ORIENTED_EDGE('',*,*,#20252,.F.) ;
#29739=ORIENTED_EDGE('',*,*,#20249,.F.) ;
#29740=ORIENTED_EDGE('',*,*,#20246,.F.) ;
#29741=ORIENTED_EDGE('',*,*,#20243,.F.) ;
#29742=ORIENTED_EDGE('',*,*,#20240,.F.) ;
#29743=ORIENTED_EDGE('',*,*,#20237,.F.) ;
#29744=ORIENTED_EDGE('',*,*,#20234,.F.) ;
#29745=ORIENTED_EDGE('',*,*,#20231,.F.) ;
#29746=ORIENTED_EDGE('',*,*,#20228,.F.) ;
#29747=ORIENTED_EDGE('',*,*,#20225,.F.) ;
#29748=ORIENTED_EDGE('',*,*,#20321,.F.) ;
#29749=ORIENTED_EDGE('',*,*,#20272,.F.) ;
#29750=ORIENTED_EDGE('',*,*,#20277,.F.) ;
#29751=ORIENTED_EDGE('',*,*,#20176,.T.) ;
#29752=ORIENTED_EDGE('',*,*,#20180,.T.) ;
#29753=ORIENTED_EDGE('',*,*,#20183,.T.) ;
#29754=ORIENTED_EDGE('',*,*,#20186,.T.) ;
#29755=ORIENTED_EDGE('',*,*,#20189,.T.) ;
#29756=ORIENTED_EDGE('',*,*,#20192,.T.) ;
#29757=ORIENTED_EDGE('',*,*,#20195,.T.) ;
#29758=ORIENTED_EDGE('',*,*,#20198,.T.) ;
#29759=ORIENTED_EDGE('',*,*,#20201,.T.) ;
#29760=ORIENTED_EDGE('',*,*,#20204,.T.) ;
#29761=ORIENTED_EDGE('',*,*,#20207,.T.) ;
#29762=ORIENTED_EDGE('',*,*,#20210,.T.) ;
#29763=ORIENTED_EDGE('',*,*,#20213,.T.) ;
#29764=ORIENTED_EDGE('',*,*,#20216,.T.) ;
#29765=ORIENTED_EDGE('',*,*,#20219,.T.) ;
#29766=ORIENTED_EDGE('',*,*,#20283,.T.) ;
#29767=ORIENTED_EDGE('',*,*,#20319,.F.) ;
#29768=ORIENTED_EDGE('',*,*,#20281,.F.) ;
#29769=ORIENTED_EDGE('',*,*,#20220,.F.) ;
#29770=ORIENTED_EDGE('',*,*,#20217,.F.) ;
#29771=ORIENTED_EDGE('',*,*,#20214,.F.) ;
#29772=ORIENTED_EDGE('',*,*,#20211,.F.) ;
#29773=ORIENTED_EDGE('',*,*,#20208,.F.) ;
#29774=ORIENTED_EDGE('',*,*,#20205,.F.) ;
#29775=ORIENTED_EDGE('',*,*,#20202,.F.) ;
#29776=ORIENTED_EDGE('',*,*,#20199,.F.) ;
#29777=ORIENTED_EDGE('',*,*,#20196,.F.) ;
#29778=ORIENTED_EDGE('',*,*,#20193,.F.) ;
#29779=ORIENTED_EDGE('',*,*,#20190,.F.) ;
#29780=ORIENTED_EDGE('',*,*,#20187,.F.) ;
#29781=ORIENTED_EDGE('',*,*,#20184,.F.) ;
#29782=ORIENTED_EDGE('',*,*,#20181,.F.) ;
#29783=ORIENTED_EDGE('',*,*,#20178,.F.) ;
#29784=ORIENTED_EDGE('',*,*,#20276,.F.) ;
#29785=ORIENTED_EDGE('',*,*,#20222,.T.) ;
#29786=ORIENTED_EDGE('',*,*,#20227,.T.) ;
#29787=ORIENTED_EDGE('',*,*,#20230,.T.) ;
#29788=ORIENTED_EDGE('',*,*,#20233,.T.) ;
#29789=ORIENTED_EDGE('',*,*,#20236,.T.) ;
#29790=ORIENTED_EDGE('',*,*,#20239,.T.) ;
#29791=ORIENTED_EDGE('',*,*,#20242,.T.) ;
#29792=ORIENTED_EDGE('',*,*,#20245,.T.) ;
#29793=ORIENTED_EDGE('',*,*,#20248,.T.) ;
#29794=ORIENTED_EDGE('',*,*,#20251,.T.) ;
#29795=ORIENTED_EDGE('',*,*,#20254,.T.) ;
#29796=ORIENTED_EDGE('',*,*,#20257,.T.) ;
#29797=ORIENTED_EDGE('',*,*,#20260,.T.) ;
#29798=ORIENTED_EDGE('',*,*,#20263,.T.) ;
#29799=ORIENTED_EDGE('',*,*,#20266,.T.) ;
#29800=ORIENTED_EDGE('',*,*,#20269,.T.) ;
#29801=ORIENTED_EDGE('',*,*,#20280,.T.) ;
#29802=ORIENTED_EDGE('',*,*,#20224,.T.) ;
#29803=ORIENTED_EDGE('',*,*,#20273,.T.) ;
#29804=ORIENTED_EDGE('',*,*,#20321,.T.) ;
#29805=ORIENTED_EDGE('',*,*,#20274,.F.) ;
#29806=ORIENTED_EDGE('',*,*,#20223,.F.) ;
#29807=ORIENTED_EDGE('',*,*,#20275,.F.) ;
#29808=ORIENTED_EDGE('',*,*,#20296,.T.) ;
#29809=ORIENTED_EDGE('',*,*,#20322,.F.) ;
#29810=ORIENTED_EDGE('',*,*,#20323,.F.) ;
#29811=ORIENTED_EDGE('',*,*,#20324,.T.) ;
#29812=ORIENTED_EDGE('',*,*,#20297,.T.) ;
#29813=ORIENTED_EDGE('',*,*,#20324,.F.) ;
#29814=ORIENTED_EDGE('',*,*,#20325,.F.) ;
#29815=ORIENTED_EDGE('',*,*,#20326,.T.) ;
#29816=ORIENTED_EDGE('',*,*,#20298,.T.) ;
#29817=ORIENTED_EDGE('',*,*,#20326,.F.) ;
#29818=ORIENTED_EDGE('',*,*,#20327,.F.) ;
#29819=ORIENTED_EDGE('',*,*,#20328,.T.) ;
#29820=ORIENTED_EDGE('',*,*,#20299,.T.) ;
#29821=ORIENTED_EDGE('',*,*,#20328,.F.) ;
#29822=ORIENTED_EDGE('',*,*,#20329,.F.) ;
#29823=ORIENTED_EDGE('',*,*,#20330,.T.) ;
#29824=ORIENTED_EDGE('',*,*,#20300,.T.) ;
#29825=ORIENTED_EDGE('',*,*,#20330,.F.) ;
#29826=ORIENTED_EDGE('',*,*,#20331,.F.) ;
#29827=ORIENTED_EDGE('',*,*,#20291,.T.) ;
#29828=ORIENTED_EDGE('',*,*,#20332,.T.) ;
#29829=ORIENTED_EDGE('',*,*,#20288,.T.) ;
#29830=ORIENTED_EDGE('',*,*,#20331,.T.) ;
#29831=ORIENTED_EDGE('',*,*,#20329,.T.) ;
#29832=ORIENTED_EDGE('',*,*,#20327,.T.) ;
#29833=ORIENTED_EDGE('',*,*,#20325,.T.) ;
#29834=ORIENTED_EDGE('',*,*,#20323,.T.) ;
#29835=ORIENTED_EDGE('',*,*,#20333,.T.) ;
#29836=ORIENTED_EDGE('',*,*,#20334,.T.) ;
#29837=ORIENTED_EDGE('',*,*,#20335,.T.) ;
#29838=ORIENTED_EDGE('',*,*,#20336,.T.) ;
#29839=ORIENTED_EDGE('',*,*,#20337,.T.) ;
#29840=ORIENTED_EDGE('',*,*,#20338,.T.) ;
#29841=ORIENTED_EDGE('',*,*,#20339,.T.) ;
#29842=ORIENTED_EDGE('',*,*,#20340,.T.) ;
#29843=ORIENTED_EDGE('',*,*,#20341,.T.) ;
#29844=ORIENTED_EDGE('',*,*,#20284,.T.) ;
#29845=ORIENTED_EDGE('',*,*,#20342,.T.) ;
#29846=ORIENTED_EDGE('',*,*,#20343,.T.) ;
#29847=ORIENTED_EDGE('',*,*,#20344,.T.) ;
#29848=ORIENTED_EDGE('',*,*,#20301,.T.) ;
#29849=ORIENTED_EDGE('',*,*,#20289,.F.) ;
#29850=ORIENTED_EDGE('',*,*,#20332,.F.) ;
#29851=ORIENTED_EDGE('',*,*,#20345,.T.) ;
#29852=ORIENTED_EDGE('',*,*,#20302,.T.) ;
#29853=ORIENTED_EDGE('',*,*,#20345,.F.) ;
#29854=ORIENTED_EDGE('',*,*,#20344,.F.) ;
#29855=ORIENTED_EDGE('',*,*,#20346,.T.) ;
#29856=ORIENTED_EDGE('',*,*,#20303,.T.) ;
#29857=ORIENTED_EDGE('',*,*,#20346,.F.) ;
#29858=ORIENTED_EDGE('',*,*,#20343,.F.) ;
#29859=ORIENTED_EDGE('',*,*,#20347,.T.) ;
#29860=ORIENTED_EDGE('',*,*,#20304,.T.) ;
#29861=ORIENTED_EDGE('',*,*,#20347,.F.) ;
#29862=ORIENTED_EDGE('',*,*,#20342,.F.) ;
#29863=ORIENTED_EDGE('',*,*,#20287,.T.) ;
#29864=ORIENTED_EDGE('',*,*,#20305,.T.) ;
#29865=ORIENTED_EDGE('',*,*,#20285,.F.) ;
#29866=ORIENTED_EDGE('',*,*,#20341,.F.) ;
#29867=ORIENTED_EDGE('',*,*,#20348,.T.) ;
#29868=ORIENTED_EDGE('',*,*,#20306,.T.) ;
#29869=ORIENTED_EDGE('',*,*,#20348,.F.) ;
#29870=ORIENTED_EDGE('',*,*,#20340,.F.) ;
#29871=ORIENTED_EDGE('',*,*,#20349,.T.) ;
#29872=ORIENTED_EDGE('',*,*,#20307,.T.) ;
#29873=ORIENTED_EDGE('',*,*,#20349,.F.) ;
#29874=ORIENTED_EDGE('',*,*,#20339,.F.) ;
#29875=ORIENTED_EDGE('',*,*,#20350,.T.) ;
#29876=ORIENTED_EDGE('',*,*,#20308,.T.) ;
#29877=ORIENTED_EDGE('',*,*,#20350,.F.) ;
#29878=ORIENTED_EDGE('',*,*,#20338,.F.) ;
#29879=ORIENTED_EDGE('',*,*,#20351,.T.) ;
#29880=ORIENTED_EDGE('',*,*,#20309,.T.) ;
#29881=ORIENTED_EDGE('',*,*,#20351,.F.) ;
#29882=ORIENTED_EDGE('',*,*,#20337,.F.) ;
#29883=ORIENTED_EDGE('',*,*,#20352,.T.) ;
#29884=ORIENTED_EDGE('',*,*,#20310,.T.) ;
#29885=ORIENTED_EDGE('',*,*,#20352,.F.) ;
#29886=ORIENTED_EDGE('',*,*,#20336,.F.) ;
#29887=ORIENTED_EDGE('',*,*,#20353,.T.) ;
#29888=ORIENTED_EDGE('',*,*,#20311,.T.) ;
#29889=ORIENTED_EDGE('',*,*,#20353,.F.) ;
#29890=ORIENTED_EDGE('',*,*,#20335,.F.) ;
#29891=ORIENTED_EDGE('',*,*,#20354,.T.) ;
#29892=ORIENTED_EDGE('',*,*,#20312,.T.) ;
#29893=ORIENTED_EDGE('',*,*,#20354,.F.) ;
#29894=ORIENTED_EDGE('',*,*,#20334,.F.) ;
#29895=ORIENTED_EDGE('',*,*,#20355,.T.) ;
#29896=ORIENTED_EDGE('',*,*,#20313,.T.) ;
#29897=ORIENTED_EDGE('',*,*,#20355,.F.) ;
#29898=ORIENTED_EDGE('',*,*,#20333,.F.) ;
#29899=ORIENTED_EDGE('',*,*,#20322,.T.) ;
#30712=CYLINDRICAL_SURFACE('',#36382,1.5) ;
#30713=CYLINDRICAL_SURFACE('',#36384,1.5) ;
#30714=CYLINDRICAL_SURFACE('',#36385,1.5) ;
#30715=CYLINDRICAL_SURFACE('',#36386,1.5) ;
#30716=CYLINDRICAL_SURFACE('',#36387,1.5) ;
#30717=CYLINDRICAL_SURFACE('',#36388,1.5) ;
#30718=CYLINDRICAL_SURFACE('',#36389,1.5) ;
#30719=CYLINDRICAL_SURFACE('',#36390,1.5) ;
#30720=CYLINDRICAL_SURFACE('',#36391,1.5) ;
#30721=CYLINDRICAL_SURFACE('',#36392,1.5) ;
#30722=CYLINDRICAL_SURFACE('',#36393,1.5) ;
#30723=CYLINDRICAL_SURFACE('',#36394,1.5) ;
#30724=CYLINDRICAL_SURFACE('',#36395,1.5) ;
#30725=CYLINDRICAL_SURFACE('',#36396,1.5) ;
#30726=CYLINDRICAL_SURFACE('',#36397,1.5) ;
#30727=CYLINDRICAL_SURFACE('',#36398,1.17524047358084) ;
#30728=CYLINDRICAL_SURFACE('',#36400,1.17524047358084) ;
#30729=CYLINDRICAL_SURFACE('',#36401,1.17524047358084) ;
#30730=CYLINDRICAL_SURFACE('',#36402,1.17524047358084) ;
#30731=CYLINDRICAL_SURFACE('',#36403,1.17524047358084) ;
#30732=CYLINDRICAL_SURFACE('',#36404,1.17524047358084) ;
#30733=CYLINDRICAL_SURFACE('',#36405,1.17524047358084) ;
#30734=CYLINDRICAL_SURFACE('',#36406,1.17524047358084) ;
#30735=CYLINDRICAL_SURFACE('',#36407,1.17524047358084) ;
#30736=CYLINDRICAL_SURFACE('',#36408,1.17524047358084) ;
#30737=CYLINDRICAL_SURFACE('',#36409,1.17524047358084) ;
#30738=CYLINDRICAL_SURFACE('',#36410,1.17524047358084) ;
#30739=CYLINDRICAL_SURFACE('',#36411,1.17524047358084) ;
#30740=CYLINDRICAL_SURFACE('',#36412,1.17524047358084) ;
#30741=CYLINDRICAL_SURFACE('',#36413,1.17524047358084) ;
#30742=CYLINDRICAL_SURFACE('',#36414,1.17524047358084) ;
#30743=CYLINDRICAL_SURFACE('',#36419,1.17524047358084) ;
#30744=CYLINDRICAL_SURFACE('',#36421,1.5) ;
#30745=CYLINDRICAL_SURFACE('',#36453,2.99999999999999) ;
#32560=ADVANCED_FACE('',(#4081),#30712,.T.) ;
#32561=ADVANCED_FACE('',(#4082),#30713,.T.) ;
#32562=ADVANCED_FACE('',(#4083),#30714,.T.) ;
#32563=ADVANCED_FACE('',(#4084),#30715,.T.) ;
#32564=ADVANCED_FACE('',(#4085),#30716,.T.) ;
#32565=ADVANCED_FACE('',(#4086),#30717,.T.) ;
#32566=ADVANCED_FACE('',(#4087),#30718,.T.) ;
#32567=ADVANCED_FACE('',(#4088),#30719,.T.) ;
#32568=ADVANCED_FACE('',(#4089),#30720,.T.) ;
#32569=ADVANCED_FACE('',(#4090),#30721,.T.) ;
#32570=ADVANCED_FACE('',(#4091),#30722,.T.) ;
#32571=ADVANCED_FACE('',(#4092),#30723,.T.) ;
#32572=ADVANCED_FACE('',(#4093),#30724,.T.) ;
#32573=ADVANCED_FACE('',(#4094),#30725,.T.) ;
#32574=ADVANCED_FACE('',(#4095),#30726,.T.) ;
#32575=ADVANCED_FACE('',(#4096),#30727,.T.) ;
#32576=ADVANCED_FACE('',(#4097),#30728,.T.) ;
#32577=ADVANCED_FACE('',(#4098),#30729,.T.) ;
#32578=ADVANCED_FACE('',(#4099),#30730,.T.) ;
#32579=ADVANCED_FACE('',(#4100),#30731,.T.) ;
#32580=ADVANCED_FACE('',(#4101),#30732,.T.) ;
#32581=ADVANCED_FACE('',(#4102),#30733,.T.) ;
#32582=ADVANCED_FACE('',(#4103),#30734,.T.) ;
#32583=ADVANCED_FACE('',(#4104),#30735,.T.) ;
#32584=ADVANCED_FACE('',(#4105),#30736,.T.) ;
#32585=ADVANCED_FACE('',(#4106),#30737,.T.) ;
#32586=ADVANCED_FACE('',(#4107),#30738,.T.) ;
#32587=ADVANCED_FACE('',(#4108),#30739,.T.) ;
#32588=ADVANCED_FACE('',(#4109),#30740,.T.) ;
#32589=ADVANCED_FACE('',(#4110),#30741,.T.) ;
#32590=ADVANCED_FACE('',(#4111),#30742,.T.) ;
#32591=ADVANCED_FACE('',(#4112),#897,.T.) ;
#32592=ADVANCED_FACE('',(#4113),#898,.T.) ;
#32593=ADVANCED_FACE('',(#4114),#30743,.T.) ;
#32594=ADVANCED_FACE('',(#4115),#30744,.T.) ;
#32595=ADVANCED_FACE('',(#4116),#899,.F.) ;
#32596=ADVANCED_FACE('',(#4117),#900,.F.) ;
#32597=ADVANCED_FACE('',(#4118),#468,.T.) ;
#32598=ADVANCED_FACE('',(#4119,#1185),#121,.T.) ;
#32599=ADVANCED_FACE('',(#4120),#30745,.T.) ;
#32600=ADVANCED_FACE('',(#4121),#469,.T.) ;
#32601=ADVANCED_FACE('',(#4122,#1186),#2247,.T.) ;
#32602=ADVANCED_FACE('',(#4123),#758,.F.) ;
#32603=ADVANCED_FACE('',(#4124),#759,.F.) ;
#32604=ADVANCED_FACE('',(#4125),#760,.T.) ;
#32605=ADVANCED_FACE('',(#4126),#2248,.F.) ;
#32606=ADVANCED_FACE('',(#4127),#901,.F.) ;
#32607=ADVANCED_FACE('',(#4128),#2249,.T.) ;
#32608=ADVANCED_FACE('',(#4129),#2250,.T.) ;
#32609=ADVANCED_FACE('',(#4130),#2251,.T.) ;
#32610=ADVANCED_FACE('',(#4131),#2252,.T.) ;
#32611=ADVANCED_FACE('',(#4132),#2253,.T.) ;
#32612=ADVANCED_FACE('',(#4133),#2254,.T.) ;
#32613=ADVANCED_FACE('',(#4134),#2255,.T.) ;
#32614=ADVANCED_FACE('',(#4135),#2256,.T.) ;
#32615=ADVANCED_FACE('',(#4136),#2257,.T.) ;
#32616=ADVANCED_FACE('',(#4137),#2258,.T.) ;
#32617=ADVANCED_FACE('',(#4138),#2259,.T.) ;
#32618=ADVANCED_FACE('',(#4139),#2260,.T.) ;
#32619=ADVANCED_FACE('',(#4140),#2261,.T.) ;
#32620=ADVANCED_FACE('',(#4141),#902,.F.) ;
#32621=ADVANCED_FACE('',(#4142),#2262,.T.) ;
#32622=ADVANCED_FACE('',(#4143),#2263,.T.) ;
#32623=ADVANCED_FACE('',(#4144),#2264,.T.) ;
#32624=ADVANCED_FACE('',(#4145),#2265,.T.) ;
#32646=CLOSED_SHELL('',(#32560,#32561,#32562,#32563,#32564,#32565,#32566,
#32567,#32568,#32569,#32570,#32571,#32572,#32573,#32574,#32575,#32576,#32577,
#32578,#32579,#32580,#32581,#32582,#32583,#32584,#32585,#32586,#32587,#32588,
#32589,#32590,#32591,#32592,#32593,#32594,#32595,#32596,#32597,#32598,#32599,
#32600,#32601,#32602,#32603,#32604,#32605,#32606,#32607,#32608,#32609,#32610,
#32611,#32612,#32613,#32614,#32615,#32616,#32617,#32618,#32619,#32620,#32621,
#32622,#32623,#32624)) ;
#36381=AXIS2_PLACEMENT_3D('',#81796,#45990,#45991) ;
#36382=AXIS2_PLACEMENT_3D('',#81797,#45992,#45993) ;
#36383=AXIS2_PLACEMENT_3D('',#81827,#45995,#45996) ;
#36384=AXIS2_PLACEMENT_3D('',#81850,#45997,#45998) ;
#36385=AXIS2_PLACEMENT_3D('',#81926,#46000,#46001) ;
#36386=AXIS2_PLACEMENT_3D('',#82004,#46003,#46004) ;
#36387=AXIS2_PLACEMENT_3D('',#82082,#46006,#46007) ;
#36388=AXIS2_PLACEMENT_3D('',#82158,#46009,#46010) ;
#36389=AXIS2_PLACEMENT_3D('',#82234,#46012,#46013) ;
#36390=AXIS2_PLACEMENT_3D('',#82310,#46015,#46016) ;
#36391=AXIS2_PLACEMENT_3D('',#82386,#46018,#46019) ;
#36392=AXIS2_PLACEMENT_3D('',#82464,#46021,#46022) ;
#36393=AXIS2_PLACEMENT_3D('',#82540,#46024,#46025) ;
#36394=AXIS2_PLACEMENT_3D('',#82618,#46027,#46028) ;
#36395=AXIS2_PLACEMENT_3D('',#82694,#46030,#46031) ;
#36396=AXIS2_PLACEMENT_3D('',#82770,#46033,#46034) ;
#36397=AXIS2_PLACEMENT_3D('',#82846,#46036,#46037) ;
#36398=AXIS2_PLACEMENT_3D('',#82922,#46039,#46040) ;
#36399=AXIS2_PLACEMENT_3D('',#82960,#46042,#46043) ;
#36400=AXIS2_PLACEMENT_3D('',#83071,#46044,#46045) ;
#36401=AXIS2_PLACEMENT_3D('',#83147,#46047,#46048) ;
#36402=AXIS2_PLACEMENT_3D('',#83223,#46050,#46051) ;
#36403=AXIS2_PLACEMENT_3D('',#83299,#46053,#46054) ;
#36404=AXIS2_PLACEMENT_3D('',#83375,#46056,#46057) ;
#36405=AXIS2_PLACEMENT_3D('',#83453,#46059,#46060) ;
#36406=AXIS2_PLACEMENT_3D('',#83529,#46062,#46063) ;
#36407=AXIS2_PLACEMENT_3D('',#83605,#46065,#46066) ;
#36408=AXIS2_PLACEMENT_3D('',#83683,#46068,#46069) ;
#36409=AXIS2_PLACEMENT_3D('',#83759,#46071,#46072) ;
#36410=AXIS2_PLACEMENT_3D('',#83835,#46074,#46075) ;
#36411=AXIS2_PLACEMENT_3D('',#83911,#46077,#46078) ;
#36412=AXIS2_PLACEMENT_3D('',#83987,#46080,#46081) ;
#36413=AXIS2_PLACEMENT_3D('',#84065,#46083,#46084) ;
#36414=AXIS2_PLACEMENT_3D('',#84141,#46086,#46087) ;
#36415=AXIS2_PLACEMENT_3D('',#84219,#46089,#46090) ;
#36416=AXIS2_PLACEMENT_3D('',#84256,#46092,#46093) ;
#36417=AXIS2_PLACEMENT_3D('',#84257,#46094,#46095) ;
#36418=AXIS2_PLACEMENT_3D('',#84258,#46096,#46097) ;
#36419=AXIS2_PLACEMENT_3D('',#84285,#46098,#46099) ;
#36420=AXIS2_PLACEMENT_3D('',#84302,#46100,#46101) ;
#36421=AXIS2_PLACEMENT_3D('',#84313,#46102,#46103) ;
#36422=AXIS2_PLACEMENT_3D('',#84346,#46104,#46105) ;
#36423=AXIS2_PLACEMENT_3D('',#84375,#46106,#46107) ;
#36424=AXIS2_PLACEMENT_3D('',#84378,#46108,#46109) ;
#36425=AXIS2_PLACEMENT_3D('',#84384,#46110,#46111) ;
#36426=AXIS2_PLACEMENT_3D('',#84388,#46112,#46113) ;
#36427=AXIS2_PLACEMENT_3D('',#84391,#46114,#46115) ;
#36428=AXIS2_PLACEMENT_3D('',#84397,#46116,#46117) ;
#36429=AXIS2_PLACEMENT_3D('',#84401,#46118,#46119) ;
#36430=AXIS2_PLACEMENT_3D('',#84403,#46120,#46121) ;
#36431=AXIS2_PLACEMENT_3D('',#84405,#46122,#46123) ;
#36432=AXIS2_PLACEMENT_3D('',#84407,#46124,#46125) ;
#36433=AXIS2_PLACEMENT_3D('',#84408,#46126,#46127) ;
#36434=AXIS2_PLACEMENT_3D('',#84409,#46128,#46129) ;
#36435=AXIS2_PLACEMENT_3D('',#84412,#46130,#46131) ;
#36436=AXIS2_PLACEMENT_3D('',#84414,#46132,#46133) ;
#36437=AXIS2_PLACEMENT_3D('',#84416,#46134,#46135) ;
#36438=AXIS2_PLACEMENT_3D('',#84418,#46136,#46137) ;
#36439=AXIS2_PLACEMENT_3D('',#84419,#46138,#46139) ;
#36440=AXIS2_PLACEMENT_3D('',#84421,#46140,#46141) ;
#36441=AXIS2_PLACEMENT_3D('',#84423,#46142,#46143) ;
#36442=AXIS2_PLACEMENT_3D('',#84425,#46144,#46145) ;
#36443=AXIS2_PLACEMENT_3D('',#84426,#46146,#46147) ;
#36444=AXIS2_PLACEMENT_3D('',#84428,#46148,#46149) ;
#36445=AXIS2_PLACEMENT_3D('',#84430,#46150,#46151) ;
#36446=AXIS2_PLACEMENT_3D('',#84432,#46152,#46153) ;
#36447=AXIS2_PLACEMENT_3D('',#84434,#46154,#46155) ;
#36448=AXIS2_PLACEMENT_3D('',#84436,#46156,#46157) ;
#36449=AXIS2_PLACEMENT_3D('',#84438,#46158,#46159) ;
#36450=AXIS2_PLACEMENT_3D('',#84440,#46160,#46161) ;
#36451=AXIS2_PLACEMENT_3D('',#84442,#46162,#46163) ;
#36452=AXIS2_PLACEMENT_3D('',#84443,#46164,#46165) ;
#36453=AXIS2_PLACEMENT_3D('',#84444,#46166,#46167) ;
#36454=AXIS2_PLACEMENT_3D('',#84447,#46168,#46169) ;
#36455=AXIS2_PLACEMENT_3D('',#84449,#46171,#46172) ;
#36456=AXIS2_PLACEMENT_3D('',#84450,#46173,#46174) ;
#36457=AXIS2_PLACEMENT_3D('',#84452,#46175,#46176) ;
#36458=AXIS2_PLACEMENT_3D('',#84453,#46177,#46178) ;
#36459=AXIS2_PLACEMENT_3D('',#84454,#46179,#46180) ;
#36460=AXIS2_PLACEMENT_3D('',#85382,#46182,#46183) ;
#36461=AXIS2_PLACEMENT_3D('',#85383,#46184,#46185) ;
#36462=AXIS2_PLACEMENT_3D('',#85389,#46186,#46187) ;
#36463=AXIS2_PLACEMENT_3D('',#85393,#46188,#46189) ;
#36464=AXIS2_PLACEMENT_3D('',#85397,#46192,#46193) ;
#36465=AXIS2_PLACEMENT_3D('',#85401,#46196,#46197) ;
#36466=AXIS2_PLACEMENT_3D('',#85405,#46200,#46201) ;
#36467=AXIS2_PLACEMENT_3D('',#85407,#46203,#46204) ;
#36468=AXIS2_PLACEMENT_3D('',#85419,#46210,#46211) ;
#36469=AXIS2_PLACEMENT_3D('',#85432,#46219,#46220) ;
#36470=AXIS2_PLACEMENT_3D('',#85434,#46222,#46223) ;
#36471=AXIS2_PLACEMENT_3D('',#85436,#46225,#46226) ;
#36472=AXIS2_PLACEMENT_3D('',#85438,#46228,#46229) ;
#36473=AXIS2_PLACEMENT_3D('',#85439,#46230,#46231) ;
#36474=AXIS2_PLACEMENT_3D('',#85441,#46233,#46234) ;
#36475=AXIS2_PLACEMENT_3D('',#85443,#46236,#46237) ;
#36476=AXIS2_PLACEMENT_3D('',#85445,#46239,#46240) ;
#36477=AXIS2_PLACEMENT_3D('',#85449,#46241,#46242) ;
#36478=AXIS2_PLACEMENT_3D('',#85453,#46243,#46244) ;
#36479=AXIS2_PLACEMENT_3D('',#85455,#46246,#46247) ;
#36480=AXIS2_PLACEMENT_3D('',#85457,#46249,#46250) ;
#36481=AXIS2_PLACEMENT_3D('',#85459,#46252,#46253) ;
#45990=DIRECTION('axis',(0.,0.,1.)) ;
#45991=DIRECTION('refdir',(1.,0.,0.)) ;
#45992=DIRECTION('center_axis',(0.,0.,1.)) ;
#45993=DIRECTION('ref_axis',(1.,0.,0.)) ;
#45994=DIRECTION('',(0.,0.,-1.)) ;
#45995=DIRECTION('center_axis',(0.,0.,-1.)) ;
#45996=DIRECTION('ref_axis',(1.,0.,0.)) ;
#45997=DIRECTION('center_axis',(0.,0.,1.)) ;
#45998=DIRECTION('ref_axis',(1.,0.,0.)) ;
#45999=DIRECTION('',(0.,0.,-1.)) ;
#46000=DIRECTION('center_axis',(0.,0.,1.)) ;
#46001=DIRECTION('ref_axis',(1.,0.,0.)) ;
#46002=DIRECTION('',(0.,0.,-1.)) ;
#46003=DIRECTION('center_axis',(0.,0.,1.)) ;
#46004=DIRECTION('ref_axis',(1.,0.,0.)) ;
#46005=DIRECTION('',(0.,0.,-1.)) ;
#46006=DIRECTION('center_axis',(0.,0.,1.)) ;
#46007=DIRECTION('ref_axis',(1.,0.,0.)) ;
#46008=DIRECTION('',(0.,0.,-1.)) ;
#46009=DIRECTION('center_axis',(0.,0.,1.)) ;
#46010=DIRECTION('ref_axis',(1.,0.,0.)) ;
#46011=DIRECTION('',(0.,0.,-1.)) ;
#46012=DIRECTION('center_axis',(0.,0.,1.)) ;
#46013=DIRECTION('ref_axis',(1.,0.,0.)) ;
#46014=DIRECTION('',(0.,0.,-1.)) ;
#46015=DIRECTION('center_axis',(0.,0.,1.)) ;
#46016=DIRECTION('ref_axis',(1.,0.,0.)) ;
#46017=DIRECTION('',(0.,0.,-1.)) ;
#46018=DIRECTION('center_axis',(0.,0.,1.)) ;
#46019=DIRECTION('ref_axis',(1.,0.,0.)) ;
#46020=DIRECTION('',(0.,0.,-1.)) ;
#46021=DIRECTION('center_axis',(0.,0.,1.)) ;
#46022=DIRECTION('ref_axis',(1.,0.,0.)) ;
#46023=DIRECTION('',(0.,0.,-1.)) ;
#46024=DIRECTION('center_axis',(0.,0.,1.)) ;
#46025=DIRECTION('ref_axis',(1.,0.,0.)) ;
#46026=DIRECTION('',(0.,0.,-1.)) ;
#46027=DIRECTION('center_axis',(0.,0.,1.)) ;
#46028=DIRECTION('ref_axis',(1.,0.,0.)) ;
#46029=DIRECTION('',(0.,0.,-1.)) ;
#46030=DIRECTION('center_axis',(0.,0.,1.)) ;
#46031=DIRECTION('ref_axis',(1.,0.,0.)) ;
#46032=DIRECTION('',(0.,0.,-1.)) ;
#46033=DIRECTION('center_axis',(0.,0.,1.)) ;
#46034=DIRECTION('ref_axis',(1.,0.,0.)) ;
#46035=DIRECTION('',(0.,0.,-1.)) ;
#46036=DIRECTION('center_axis',(0.,0.,1.)) ;
#46037=DIRECTION('ref_axis',(1.,0.,0.)) ;
#46038=DIRECTION('',(0.,0.,-1.)) ;
#46039=DIRECTION('center_axis',(0.,0.,1.)) ;
#46040=DIRECTION('ref_axis',(1.,0.,0.)) ;
#46041=DIRECTION('',(0.,0.,-1.)) ;
#46042=DIRECTION('center_axis',(0.,0.,1.)) ;
#46043=DIRECTION('ref_axis',(1.,0.,0.)) ;
#46044=DIRECTION('center_axis',(0.,0.,1.)) ;
#46045=DIRECTION('ref_axis',(1.,0.,0.)) ;
#46046=DIRECTION('',(0.,0.,-1.)) ;
#46047=DIRECTION('center_axis',(0.,0.,1.)) ;
#46048=DIRECTION('ref_axis',(1.,0.,0.)) ;
#46049=DIRECTION('',(0.,0.,-1.)) ;
#46050=DIRECTION('center_axis',(0.,0.,1.)) ;
#46051=DIRECTION('ref_axis',(1.,0.,0.)) ;
#46052=DIRECTION('',(0.,0.,-1.)) ;
#46053=DIRECTION('center_axis',(0.,0.,1.)) ;
#46054=DIRECTION('ref_axis',(1.,0.,0.)) ;
#46055=DIRECTION('',(0.,0.,-1.)) ;
#46056=DIRECTION('center_axis',(0.,0.,1.)) ;
#46057=DIRECTION('ref_axis',(1.,0.,0.)) ;
#46058=DIRECTION('',(0.,0.,-1.)) ;
#46059=DIRECTION('center_axis',(0.,0.,1.)) ;
#46060=DIRECTION('ref_axis',(1.,0.,0.)) ;
#46061=DIRECTION('',(0.,0.,-1.)) ;
#46062=DIRECTION('center_axis',(0.,0.,1.)) ;
#46063=DIRECTION('ref_axis',(1.,0.,0.)) ;
#46064=DIRECTION('',(0.,0.,-1.)) ;
#46065=DIRECTION('center_axis',(0.,0.,1.)) ;
#46066=DIRECTION('ref_axis',(1.,0.,0.)) ;
#46067=DIRECTION('',(0.,0.,-1.)) ;
#46068=DIRECTION('center_axis',(0.,0.,1.)) ;
#46069=DIRECTION('ref_axis',(1.,0.,0.)) ;
#46070=DIRECTION('',(0.,0.,-1.)) ;
#46071=DIRECTION('center_axis',(0.,0.,1.)) ;
#46072=DIRECTION('ref_axis',(1.,0.,0.)) ;
#46073=DIRECTION('',(0.,0.,-1.)) ;
#46074=DIRECTION('center_axis',(0.,0.,1.)) ;
#46075=DIRECTION('ref_axis',(1.,0.,0.)) ;
#46076=DIRECTION('',(0.,0.,-1.)) ;
#46077=DIRECTION('center_axis',(0.,0.,1.)) ;
#46078=DIRECTION('ref_axis',(1.,0.,0.)) ;
#46079=DIRECTION('',(0.,0.,-1.)) ;
#46080=DIRECTION('center_axis',(0.,0.,1.)) ;
#46081=DIRECTION('ref_axis',(1.,0.,0.)) ;
#46082=DIRECTION('',(0.,0.,-1.)) ;
#46083=DIRECTION('center_axis',(0.,0.,1.)) ;
#46084=DIRECTION('ref_axis',(1.,0.,0.)) ;
#46085=DIRECTION('',(0.,0.,-1.)) ;
#46086=DIRECTION('center_axis',(0.,0.,1.)) ;
#46087=DIRECTION('ref_axis',(1.,0.,0.)) ;
#46088=DIRECTION('',(0.,0.,-1.)) ;
#46089=DIRECTION('center_axis',(0.,0.,1.)) ;
#46090=DIRECTION('ref_axis',(1.,0.,0.)) ;
#46091=DIRECTION('',(0.707106781186544,8.65956056235489E-17,-0.707106781186551)) ;
#46092=DIRECTION('center_axis',(0.,0.,1.)) ;
#46093=DIRECTION('ref_axis',(1.,0.,0.)) ;
#46094=DIRECTION('center_axis',(0.,0.,1.)) ;
#46095=DIRECTION('ref_axis',(1.,0.,0.)) ;
#46096=DIRECTION('center_axis',(0.,0.,1.)) ;
#46097=DIRECTION('ref_axis',(1.,0.,0.)) ;
#46098=DIRECTION('center_axis',(0.,0.,1.)) ;
#46099=DIRECTION('ref_axis',(1.,0.,0.)) ;
#46100=DIRECTION('center_axis',(0.,0.,1.)) ;
#46101=DIRECTION('ref_axis',(1.,0.,0.)) ;
#46102=DIRECTION('center_axis',(0.,0.,1.)) ;
#46103=DIRECTION('ref_axis',(1.,0.,0.)) ;
#46104=DIRECTION('center_axis',(0.,0.,1.)) ;
#46105=DIRECTION('ref_axis',(1.,0.,0.)) ;
#46106=DIRECTION('center_axis',(-1.37769458707663E-29,-3.94587412439991E-15,
1.)) ;
#46107=DIRECTION('ref_axis',(6.56371136615486E-45,-1.,-3.94587412439991E-15)) ;
#46108=DIRECTION('center_axis',(0.,0.,1.)) ;
#46109=DIRECTION('ref_axis',(1.,0.,0.)) ;
#46110=DIRECTION('center_axis',(-1.37769458707663E-29,-3.94587412439991E-15,
1.)) ;
#46111=DIRECTION('ref_axis',(-4.32555501796151E-45,1.,3.94587412439991E-15)) ;
#46112=DIRECTION('center_axis',(0.,0.,1.)) ;
#46113=DIRECTION('ref_axis',(1.,0.,0.)) ;
#46114=DIRECTION('center_axis',(0.,0.,1.)) ;
#46115=DIRECTION('ref_axis',(1.,0.,0.)) ;
#46116=DIRECTION('center_axis',(0.,0.,1.)) ;
#46117=DIRECTION('ref_axis',(-1.,0.,0.)) ;
#46118=DIRECTION('center_axis',(0.,-1.97293706219996E-15,1.)) ;
#46119=DIRECTION('ref_axis',(0.,-1.,-1.77635683940025E-15)) ;
#46120=DIRECTION('center_axis',(0.,-1.97293706219996E-15,1.)) ;
#46121=DIRECTION('ref_axis',(0.,-1.,-1.97293706219996E-15)) ;
#46122=DIRECTION('center_axis',(-1.,-1.22464679914735E-16,-2.41615105814236E-31)) ;
#46123=DIRECTION('ref_axis',(-1.22464679914735E-16,1.,1.85037170770859E-15)) ;
#46124=DIRECTION('center_axis',(0.,-1.97293706219996E-15,1.)) ;
#46125=DIRECTION('ref_axis',(0.,-1.,-1.97293706219996E-15)) ;
#46126=DIRECTION('center_axis',(0.,-1.97293706219996E-15,1.)) ;
#46127=DIRECTION('ref_axis',(0.,-1.,-1.97293706219996E-15)) ;
#46128=DIRECTION('center_axis',(-1.,1.83697019872103E-16,0.)) ;
#46129=DIRECTION('ref_axis',(1.22464679914735E-16,1.,2.10219744307722E-15)) ;
#46130=DIRECTION('center_axis',(0.,0.,1.)) ;
#46131=DIRECTION('ref_axis',(-1.,7.99360577730113E-15,0.)) ;
#46132=DIRECTION('center_axis',(-0.996194698091746,-1.55254059623772E-16,
0.0871557427476584)) ;
#46133=DIRECTION('ref_axis',(0.0871557427476584,2.43428429401259E-33,0.996194698091746)) ;
#46134=DIRECTION('center_axis',(-0.920363891963228,-0.381227206369645,0.0871557427476584)) ;
#46135=DIRECTION('ref_axis',(0.382683432365081,-0.92387953251129,-5.41926931333106E-18)) ;
#46136=DIRECTION('center_axis',(-0.381227206369648,-0.920363891963227,0.0871557427476584)) ;
#46137=DIRECTION('ref_axis',(0.923879532511289,-0.382683432365084,-6.23920499234797E-18)) ;
#46138=DIRECTION('center_axis',(0.,-0.996194698091746,0.0871557427476584)) ;
#46139=DIRECTION('ref_axis',(0.,-0.0871557427476584,-0.996194698091746)) ;
#46140=DIRECTION('center_axis',(3.49489393366845E-15,0.996194698091745,
0.0871557427476603)) ;
#46141=DIRECTION('ref_axis',(1.18266251815146E-32,-0.0871557427476603,0.996194698091745)) ;
#46142=DIRECTION('center_axis',(-0.381227206369642,0.920363891963229,0.0871557427476609)) ;
#46143=DIRECTION('ref_axis',(-0.923879532511291,-0.382683432365078,-2.80799776071203E-17)) ;
#46144=DIRECTION('center_axis',(-0.920363891963225,0.381227206369651,0.0871557427476609)) ;
#46145=DIRECTION('ref_axis',(-0.382683432365087,-0.923879532511288,7.9370913940361E-17)) ;
#46146=DIRECTION('center_axis',(-0.996194698091745,3.30624240319137E-15,
0.0871557427476603)) ;
#46147=DIRECTION('ref_axis',(0.0871557427476603,1.93558059421515E-34,0.996194698091745)) ;
#46148=DIRECTION('center_axis',(0.996194698091746,-7.14504192696067E-15,
0.0871557427476584)) ;
#46149=DIRECTION('ref_axis',(0.0871557427476584,1.49618138940667E-31,-0.996194698091746)) ;
#46150=DIRECTION('center_axis',(0.920363891963231,0.381227206369638,0.0871557427476599)) ;
#46151=DIRECTION('ref_axis',(-0.382683432365074,0.923879532511293,8.60234787324834E-17)) ;
#46152=DIRECTION('center_axis',(0.381227206369654,0.920363891963224,0.087155742747662)) ;
#46153=DIRECTION('ref_axis',(-0.923879532511287,0.38268343236509,7.82165862635586E-17)) ;
#46154=DIRECTION('center_axis',(6.9563903964836E-15,0.996194698091745,0.0871557427476623)) ;
#46155=DIRECTION('ref_axis',(-7.29504144019363E-32,-0.0871557427476623,
0.996194698091745)) ;
#46156=DIRECTION('center_axis',(-1.97293706219996E-15,-1.97293706219993E-15,
1.)) ;
#46157=DIRECTION('ref_axis',(-1.,-8.84530818399176E-31,-1.97293706219996E-15)) ;
#46158=DIRECTION('center_axis',(-1.0451284330152E-14,-0.996194698091746,
0.0871557427476564)) ;
#46159=DIRECTION('ref_axis',(-3.08095231401847E-32,-0.0871557427476564,
-0.996194698091746)) ;
#46160=DIRECTION('center_axis',(0.381227206369635,-0.920363891963232,0.0871557427476573)) ;
#46161=DIRECTION('ref_axis',(0.923879532511294,0.382683432365071,8.31057747593213E-17)) ;
#46162=DIRECTION('center_axis',(0.920363891963223,-0.381227206369657,0.0871557427476594)) ;
#46163=DIRECTION('ref_axis',(0.382683432365093,0.923879532511285,-7.95739253828632E-17)) ;
#46164=DIRECTION('center_axis',(0.996194698091745,-1.06065383897758E-14,
0.0871557427476603)) ;
#46165=DIRECTION('ref_axis',(0.0871557427476603,-6.35553601982602E-32,-0.996194698091745)) ;
#46166=DIRECTION('center_axis',(0.,0.,-1.)) ;
#46167=DIRECTION('ref_axis',(-1.,0.,0.)) ;
#46168=DIRECTION('center_axis',(0.,-1.97293706219996E-15,1.)) ;
#46169=DIRECTION('ref_axis',(0.,-1.,-1.97293706219996E-15)) ;
#46170=DIRECTION('',(0.,0.,1.)) ;
#46171=DIRECTION('center_axis',(0.,-1.97293706219996E-15,1.)) ;
#46172=DIRECTION('ref_axis',(0.,-1.,-1.97293706219996E-15)) ;
#46173=DIRECTION('center_axis',(0.,-1.97293706219996E-15,1.)) ;
#46174=DIRECTION('ref_axis',(0.,-1.,-1.77635683940025E-15)) ;
#46175=DIRECTION('center_axis',(-1.,-1.22464679914735E-16,-2.41615105814236E-31)) ;
#46176=DIRECTION('ref_axis',(-1.22464679914735E-16,1.,1.85037170770859E-15)) ;
#46177=DIRECTION('center_axis',(0.,-1.97293706219996E-15,1.)) ;
#46178=DIRECTION('ref_axis',(0.,-1.,-1.97293706219996E-15)) ;
#46179=DIRECTION('center_axis',(0.,0.,-1.)) ;
#46180=DIRECTION('ref_axis',(-1.,0.,0.)) ;
#46181=DIRECTION('',(0.,-0.866025403784433,0.50000000000001)) ;
#46182=DIRECTION('center_axis',(0.,0.,1.)) ;
#46183=DIRECTION('ref_axis',(1.,0.,0.)) ;
#46184=DIRECTION('center_axis',(0.,0.,1.)) ;
#46185=DIRECTION('ref_axis',(1.,0.,0.)) ;
#46186=DIRECTION('center_axis',(0.,0.,1.)) ;
#46187=DIRECTION('ref_axis',(1.,0.,0.)) ;
#46188=DIRECTION('center_axis',(-0.996194698091746,-1.55254059623772E-16,
0.0871557427476584)) ;
#46189=DIRECTION('ref_axis',(0.0871557427476584,8.9940333441683E-34,0.996194698091746)) ;
#46190=DIRECTION('',(-1.5584710490948E-16,1.,0.)) ;
#46191=DIRECTION('',(0.0871426484044397,0.0173337504938598,0.996045029063886)) ;
#46192=DIRECTION('center_axis',(-0.920363891963228,-0.381227206369645,0.0871557427476583)) ;
#46193=DIRECTION('ref_axis',(0.382683432365081,-0.92387953251129,3.89840055033188E-19)) ;
#46194=DIRECTION('',(-0.382683432365081,0.92387953251129,0.)) ;
#46195=DIRECTION('',(0.0666626913468327,0.0666626913468325,0.995546167269401)) ;
#46196=DIRECTION('center_axis',(-0.381227206369648,-0.920363891963227,0.0871557427476584)) ;
#46197=DIRECTION('ref_axis',(0.923879532511289,-0.382683432365084,1.47102406971995E-19)) ;
#46198=DIRECTION('',(-0.923879532511289,0.382683432365084,0.)) ;
#46199=DIRECTION('',(0.0173337504938599,0.0871426484044397,0.996045029063886)) ;
#46200=DIRECTION('center_axis',(0.,-0.996194698091746,0.0871557427476584)) ;
#46201=DIRECTION('ref_axis',(0.,-0.0871557427476584,-0.996194698091746)) ;
#46202=DIRECTION('',(-1.,0.,0.)) ;
#46203=DIRECTION('center_axis',(0.,0.,1.)) ;
#46204=DIRECTION('ref_axis',(1.,0.,0.)) ;
#46205=DIRECTION('',(1.,-3.50824386072629E-15,0.)) ;
#46206=DIRECTION('',(-1.0647053643322E-14,-1.,0.)) ;
#46207=DIRECTION('',(-0.382683432365094,-0.923879532511285,0.)) ;
#46208=DIRECTION('',(-0.923879532511294,-0.382683432365071,0.)) ;
#46209=DIRECTION('',(-1.,1.04912065384126E-14,0.)) ;
#46210=DIRECTION('center_axis',(0.,0.,1.)) ;
#46211=DIRECTION('ref_axis',(1.,0.,0.)) ;
#46212=DIRECTION('',(1.,-6.98296267768627E-15,0.)) ;
#46213=DIRECTION('',(0.923879532511286,-0.382683432365091,0.)) ;
#46214=DIRECTION('',(0.382683432365075,-0.923879532511293,0.)) ;
#46215=DIRECTION('',(-7.17233482636206E-15,-1.,0.)) ;
#46216=DIRECTION('',(3.31887171205049E-15,1.,0.)) ;
#46217=DIRECTION('',(0.382683432365087,0.923879532511288,0.)) ;
#46218=DIRECTION('',(0.923879532511292,0.382683432365078,0.)) ;
#46219=DIRECTION('center_axis',(3.49489393366845E-15,0.996194698091745,
0.0871557427476603)) ;
#46220=DIRECTION('ref_axis',(6.11304317578278E-32,-0.0871557427476603,0.996194698091745)) ;
#46221=DIRECTION('',(0.0173337504938615,-0.0871426484044417,0.996045029063885)) ;
#46222=DIRECTION('center_axis',(-0.381227206369642,0.920363891963229,0.0871557427476609)) ;
#46223=DIRECTION('ref_axis',(-0.923879532511292,-0.382683432365078,-6.27744471266564E-17)) ;
#46224=DIRECTION('',(0.0666626913468342,-0.0666626913468348,0.995546167269401)) ;
#46225=DIRECTION('center_axis',(-0.920363891963225,0.381227206369651,0.0871557427476609)) ;
#46226=DIRECTION('ref_axis',(-0.382683432365087,-0.923879532511288,7.9370913940361E-17)) ;
#46227=DIRECTION('',(0.0871426484044416,-0.0173337504938622,0.996045029063885)) ;
#46228=DIRECTION('center_axis',(-0.996194698091745,3.30624240319137E-15,
0.0871557427476603)) ;
#46229=DIRECTION('ref_axis',(0.0871557427476603,4.93097487664857E-32,0.996194698091745)) ;
#46230=DIRECTION('center_axis',(0.996194698091746,-7.14504192696067E-15,
0.0871557427476584)) ;
#46231=DIRECTION('ref_axis',(0.0871557427476584,2.47850520354795E-31,-0.996194698091746)) ;
#46232=DIRECTION('',(-0.0871426484044398,-0.0173337504938632,0.996045029063886)) ;
#46233=DIRECTION('center_axis',(0.920363891963231,0.381227206369638,0.0871557427476598)) ;
#46234=DIRECTION('ref_axis',(-0.382683432365074,0.923879532511293,8.02510185058152E-17)) ;
#46235=DIRECTION('',(-0.0666626913468331,-0.0666626913468359,0.995546167269401)) ;
#46236=DIRECTION('center_axis',(0.381227206369654,0.920363891963224,0.087155742747662)) ;
#46237=DIRECTION('ref_axis',(-0.923879532511287,0.38268343236509,7.82165862635586E-17)) ;
#46238=DIRECTION('',(-0.0173337504938606,-0.0871426484044434,0.996045029063885)) ;
#46239=DIRECTION('center_axis',(6.9563903964836E-15,0.996194698091745,0.0871557427476623)) ;
#46240=DIRECTION('ref_axis',(2.56571987506902E-32,-0.0871557427476623,0.996194698091745)) ;
#46241=DIRECTION('center_axis',(-1.97293706219996E-15,-1.97293706219993E-15,
1.)) ;
#46242=DIRECTION('ref_axis',(-1.,1.6109676234517E-14,-1.97293706219993E-15)) ;
#46243=DIRECTION('center_axis',(-1.0451284330152E-14,-0.996194698091746,
0.0871557427476564)) ;
#46244=DIRECTION('ref_axis',(-3.08095231401847E-32,-0.0871557427476564,
-0.996194698091746)) ;
#46245=DIRECTION('',(-0.0173337504938609,0.0871426484044379,0.996045029063886)) ;
#46246=DIRECTION('center_axis',(0.381227206369635,-0.920363891963232,0.0871557427476573)) ;
#46247=DIRECTION('ref_axis',(0.923879532511295,0.382683432365071,-2.87769700566421E-17)) ;
#46248=DIRECTION('',(-0.0666626913468338,0.0666626913468314,0.995546167269401)) ;
#46249=DIRECTION('center_axis',(0.920363891963223,-0.381227206369657,0.0871557427476594)) ;
#46250=DIRECTION('ref_axis',(0.382683432365093,0.923879532511285,-7.2635031478956E-17)) ;
#46251=DIRECTION('',(-0.0871426484044414,0.0173337504938589,0.996045029063885)) ;
#46252=DIRECTION('center_axis',(0.996194698091745,-1.06065383897758E-14,
0.0871557427476603)) ;
#46253=DIRECTION('ref_axis',(0.0871557427476603,-6.35553601982602E-32,-0.996194698091745)) ;
#81796=CARTESIAN_POINT('',(0.,0.,0.)) ;
#81797=CARTESIAN_POINT('Origin',(0.,0.,0.)) ;
#81798=CARTESIAN_POINT('',(-1.5,-8.72474074125615E-16,0.656249999999997)) ;
#81799=CARTESIAN_POINT('',(-1.5,-3.60730648712457E-16,0.593749999999997)) ;
#81800=CARTESIAN_POINT('',(-1.5,-1.83697019872103E-16,0.)) ;
#81801=CARTESIAN_POINT('',(0.778543926944327,-1.28213468630176,0.324759526419166)) ;
#81802=CARTESIAN_POINT('Ctrl Pts',(-1.5,-2.39391839684799E-15,0.656249999999998)) ;
#81803=CARTESIAN_POINT('Ctrl Pts',(-1.5,0.1607200270702,0.647321109607209)) ;
#81804=CARTESIAN_POINT('Ctrl Pts',(-1.4741670211068,0.320634454503277,0.638436974749825)) ;
#81805=CARTESIAN_POINT('Ctrl Pts',(-1.36283639967842,0.655239528350988,
0.619847803980508)) ;
#81806=CARTESIAN_POINT('Ctrl Pts',(-1.26817721619372,0.823642853630126,
0.611052903272752)) ;
#81807=CARTESIAN_POINT('Ctrl Pts',(-1.01524271305061,1.12213782029424,0.59059205946455)) ;
#81808=CARTESIAN_POINT('Ctrl Pts',(-0.856944680450145,1.24721443035943,
0.579501591540454)) ;
#81809=CARTESIAN_POINT('Ctrl Pts',(-0.507462070287139,1.42457367000859,
0.557760456073417)) ;
#81810=CARTESIAN_POINT('Ctrl Pts',(-0.320951378192811,1.47781505723871,
0.547308028793073)) ;
#81811=CARTESIAN_POINT('Ctrl Pts',(0.0666309309435816,1.51138923147558,
0.527727850299295)) ;
#81812=CARTESIAN_POINT('Ctrl Pts',(0.264147146078897,1.48962397255287,0.518252991524167)) ;
#81813=CARTESIAN_POINT('Ctrl Pts',(0.639980871457319,1.37089218869411,0.496872577873832)) ;
#81814=CARTESIAN_POINT('Ctrl Pts',(0.814538593466314,1.27492978139909,0.485808543133052)) ;
#81815=CARTESIAN_POINT('Ctrl Pts',(1.11103575990294,1.02555152867983,0.464616142875061)) ;
#81816=CARTESIAN_POINT('Ctrl Pts',(1.23191971314068,0.876637017425266,0.454952056523631)) ;
#81817=CARTESIAN_POINT('Ctrl Pts',(1.41577752646327,0.533957385879126,0.435914299215511)) ;
#81818=CARTESIAN_POINT('Ctrl Pts',(1.47399821495026,0.341819854608497,0.425239991922698)) ;
#81819=CARTESIAN_POINT('Ctrl Pts',(1.51178732396369,-0.0501021196454836,
0.403466548908587)) ;
#81820=CARTESIAN_POINT('Ctrl Pts',(1.49248613525052,-0.245976760588441,
0.392584624411756)) ;
#81821=CARTESIAN_POINT('Ctrl Pts',(1.38414872473132,-0.605597575963239,
0.372605690224267)) ;
#81822=CARTESIAN_POINT('Ctrl Pts',(1.30127330020684,-0.767657852056223,
0.364200378289862)) ;
#81823=CARTESIAN_POINT('Ctrl Pts',(1.07817949622543,-1.05942775932347,0.345362052994947)) ;
#81824=CARTESIAN_POINT('Ctrl Pts',(0.938095211434252,-1.18525119589866,
0.335127149240069)) ;
#81825=CARTESIAN_POINT('Ctrl Pts',(0.778543926944331,-1.28213468630175,
0.324759526419165)) ;
#81826=CARTESIAN_POINT('',(1.46053184144302,-0.34182852445499,0.324759526419167)) ;
#81827=CARTESIAN_POINT('Origin',(0.,0.,0.324759526419167)) ;
#81828=CARTESIAN_POINT('Ctrl Pts',(1.46053184144283,-0.3418285244558,0.32475952641912)) ;
#81829=CARTESIAN_POINT('Ctrl Pts',(1.48363731923417,-0.243105674805563,
0.330244129177467)) ;
#81830=CARTESIAN_POINT('Ctrl Pts',(1.49667194701901,-0.142307929062366,
0.335844003941008)) ;
#81831=CARTESIAN_POINT('Ctrl Pts',(1.50221691376025,0.0606643103737226,
0.347120239465234)) ;
#81832=CARTESIAN_POINT('Ctrl Pts',(1.49465417855031,0.162313399979073,0.352767411109976)) ;
#81833=CARTESIAN_POINT('Ctrl Pts',(1.44242100214408,0.456280577716692,0.369098920984288)) ;
#81834=CARTESIAN_POINT('Ctrl Pts',(1.37015036039608,0.641424489494071,0.378979290313343)) ;
#81835=CARTESIAN_POINT('Ctrl Pts',(1.16119559714889,0.96864281127129,0.398122028874589)) ;
#81836=CARTESIAN_POINT('Ctrl Pts',(1.02824815461798,1.10875059589915,0.408410348592026)) ;
#81837=CARTESIAN_POINT('Ctrl Pts',(0.710844326433935,1.33575618782009,0.429987158282374)) ;
#81838=CARTESIAN_POINT('Ctrl Pts',(0.527686779618663,1.41813255022657,0.441087562151267)) ;
#81839=CARTESIAN_POINT('Ctrl Pts',(0.145663306121761,1.50533022648136,0.461889832763359)) ;
#81840=CARTESIAN_POINT('Ctrl Pts',(-0.0489530922816456,1.51156802005474,
0.470783922860158)) ;
#81841=CARTESIAN_POINT('Ctrl Pts',(-0.430582684445121,1.44985830492366,
0.490859243927657)) ;
#81842=CARTESIAN_POINT('Ctrl Pts',(-0.613925254356179,1.38223457637478,
0.501558754339464)) ;
#81843=CARTESIAN_POINT('Ctrl Pts',(-0.949244480379525,1.17833725920884,
0.523355622489269)) ;
#81844=CARTESIAN_POINT('Ctrl Pts',(-1.09694604083355,1.04224392432656,0.53424228754332)) ;
#81845=CARTESIAN_POINT('Ctrl Pts',(-1.32547379116904,0.727490619845216,
0.55398048140448)) ;
#81846=CARTESIAN_POINT('Ctrl Pts',(-1.40689368697929,0.553880965707191,
0.562978835238514)) ;
#81847=CARTESIAN_POINT('Ctrl Pts',(-1.48452734965408,0.248571106902,0.579940494061024)) ;
#81848=CARTESIAN_POINT('Ctrl Pts',(-1.5,0.124386408551049,0.586839643969384)) ;
#81849=CARTESIAN_POINT('Ctrl Pts',(-1.5,1.38777878078145E-16,0.593749999999997)) ;
#81850=CARTESIAN_POINT('Origin',(0.,0.,0.)) ;
#81851=CARTESIAN_POINT('',(-1.5,3.25616779869919E-15,1.15625)) ;
#81852=CARTESIAN_POINT('',(-1.5,-1.11533536076237E-15,1.09375)) ;
#81853=CARTESIAN_POINT('',(-1.5,-1.83697019872103E-16,0.)) ;
#81854=CARTESIAN_POINT('Ctrl Pts',(-1.5,6.1409211049579E-15,1.15625)) ;
#81855=CARTESIAN_POINT('Ctrl Pts',(-1.5,0.189806105391236,1.14570521636715)) ;
#81856=CARTESIAN_POINT('Ctrl Pts',(-1.46397304873954,0.377951075523363,
1.13525271802649)) ;
#81857=CARTESIAN_POINT('Ctrl Pts',(-1.3222161587587,0.734327472585592,1.11545402930081)) ;
#81858=CARTESIAN_POINT('Ctrl Pts',(-1.21650652238285,0.898670433729232,
1.10648279641048)) ;
#81859=CARTESIAN_POINT('Ctrl Pts',(-0.945002587646155,1.1816907098443,1.08555838292342)) ;
#81860=CARTESIAN_POINT('Ctrl Pts',(-0.780467079717811,1.29625862406437,
1.07445972254562)) ;
#81861=CARTESIAN_POINT('Ctrl Pts',(-0.423205968198729,1.45169093957452,
1.05295342498368)) ;
#81862=CARTESIAN_POINT('Ctrl Pts',(-0.235004329546768,1.49375558567739,
1.04273010703046)) ;
#81863=CARTESIAN_POINT('Ctrl Pts',(0.154749090124977,1.50518049501528,1.02366072829066)) ;
#81864=CARTESIAN_POINT('Ctrl Pts',(0.352687859447389,1.47145138342095,1.01348828032349)) ;
#81865=CARTESIAN_POINT('Ctrl Pts',(0.721375141428468,1.3296905992613,0.991812005638621)) ;
#81866=CARTESIAN_POINT('Ctrl Pts',(0.888858008163141,1.22408904482572,0.980820605943696)) ;
#81867=CARTESIAN_POINT('Ctrl Pts',(1.16923496541125,0.958636529157075,0.959957282307752)) ;
#81868=CARTESIAN_POINT('Ctrl Pts',(1.28110302387416,0.80302881514754,0.950862711952652)) ;
#81869=CARTESIAN_POINT('Ctrl Pts',(1.44459447450888,0.450228209630156,0.931262678312795)) ;
#81870=CARTESIAN_POINT('Ctrl Pts',(1.49148846155318,0.254951726388306,0.920413984799357)) ;
#81871=CARTESIAN_POINT('Ctrl Pts',(1.50621480594731,-0.137478762899289,
0.898612290950045)) ;
#81872=CARTESIAN_POINT('Ctrl Pts',(1.47585978575147,-0.33080834689361,0.887871758505916)) ;
#81873=CARTESIAN_POINT('Ctrl Pts',(1.34374220319785,-0.693812003860026,
0.867704888674449)) ;
#81874=CARTESIAN_POINT('Ctrl Pts',(1.24378584267304,-0.860242010169573,
0.858862729529871)) ;
#81875=CARTESIAN_POINT('Ctrl Pts',(0.981871506228363,-1.15134823900421,
0.838175086007994)) ;
#81876=CARTESIAN_POINT('Ctrl Pts',(0.820487582424932,-1.27140244037549,
0.82707565942678)) ;
#81877=CARTESIAN_POINT('Ctrl Pts',(0.467093846979265,-1.438245245513,0.805438473037725)) ;
#81878=CARTESIAN_POINT('Ctrl Pts',(0.279686633416262,-1.48610985160416,
0.795092266879746)) ;
#81879=CARTESIAN_POINT('Ctrl Pts',(-0.109993306164626,-1.50909510092276,
0.775705302897438)) ;
#81880=CARTESIAN_POINT('Ctrl Pts',(-0.308690063405629,-1.48128448585284,
0.765878267006745)) ;
#81881=CARTESIAN_POINT('Ctrl Pts',(-0.681837802149646,-1.35047446149059,
0.744291576267959)) ;
#81882=CARTESIAN_POINT('Ctrl Pts',(-0.852850201293791,-1.24953248569501,
0.733259794605807)) ;
#81883=CARTESIAN_POINT('Ctrl Pts',(-1.14114328313784,-0.991903517435437,
0.712232927009028)) ;
#81884=CARTESIAN_POINT('Ctrl Pts',(-1.25742060362583,-0.839613205476229,
0.702895178082022)) ;
#81885=CARTESIAN_POINT('Ctrl Pts',(-1.43098751048226,-0.491755446248058,
0.683569747013789)) ;
#81886=CARTESIAN_POINT('Ctrl Pts',(-1.48349456128071,-0.297942723678847,
0.672802373537721)) ;
#81887=CARTESIAN_POINT('Ctrl Pts',(-1.49889952124722,-0.0663817994101106,
0.659937877745013)) ;
#81888=CARTESIAN_POINT('Ctrl Pts',(-1.5,-0.0331737388818849,0.658092985493435)) ;
#81889=CARTESIAN_POINT('Ctrl Pts',(-1.5,-2.37984979295154E-15,0.656249999999997)) ;
#81890=CARTESIAN_POINT('Ctrl Pts',(-1.5,2.97483362866747E-16,0.593749999999998)) ;
#81891=CARTESIAN_POINT('Ctrl Pts',(-1.5,-0.0705859863589315,0.597671443686605)) ;
#81892=CARTESIAN_POINT('Ctrl Pts',(-1.4950177408892,-0.141236928673874,
0.601596496037459)) ;
#81893=CARTESIAN_POINT('Ctrl Pts',(-1.45699567168959,-0.408302331935193,
0.616433462885309)) ;
#81894=CARTESIAN_POINT('Ctrl Pts',(-1.39010246512636,-0.597586788383109,
0.626801630307176)) ;
#81895=CARTESIAN_POINT('Ctrl Pts',(-1.19056528868096,-0.932189699523634,
0.645696392494476)) ;
#81896=CARTESIAN_POINT('Ctrl Pts',(-1.06244257795823,-1.07592532097647,
0.655853355439699)) ;
#81897=CARTESIAN_POINT('Ctrl Pts',(-0.753373782602369,-1.31214212345324,
0.677285012636009)) ;
#81898=CARTESIAN_POINT('Ctrl Pts',(-0.573575272037589,-1.40010946284613,
0.688379109714239)) ;
#81899=CARTESIAN_POINT('Ctrl Pts',(-0.193917233490111,-1.50005780821647,
0.709421758537475)) ;
#81900=CARTESIAN_POINT('Ctrl Pts',(0.0018330599722723,-1.51253682526368,
0.718489947992844)) ;
#81901=CARTESIAN_POINT('Ctrl Pts',(0.385955527725803,-1.46229454874621,
0.738366667631604)) ;
#81902=CARTESIAN_POINT('Ctrl Pts',(0.570728475938215,-1.40054270181248,
0.748971889328879)) ;
#81903=CARTESIAN_POINT('Ctrl Pts',(0.913371471429655,-1.20666008869792,
0.770842936277859)) ;
#81904=CARTESIAN_POINT('Ctrl Pts',(1.06645766524887,-1.07376035622208,0.781899958447527)) ;
#81905=CARTESIAN_POINT('Ctrl Pts',(1.30497513749981,-0.763741406097344,
0.801987273185199)) ;
#81906=CARTESIAN_POINT('Ctrl Pts',(1.39128549698088,-0.592107607993041,
0.810855132889296)) ;
#81907=CARTESIAN_POINT('Ctrl Pts',(1.49643461481373,-0.220970650242353,
0.831473852764334)) ;
#81908=CARTESIAN_POINT('Ctrl Pts',(1.51246123111777,-0.0244681350068359,
0.842390659166306)) ;
#81909=CARTESIAN_POINT('Ctrl Pts',(1.46791659667496,0.367046590015983,0.864141477223129)) ;
#81910=CARTESIAN_POINT('Ctrl Pts',(1.40641810169146,0.558136775334782,0.874757598629729)) ;
#81911=CARTESIAN_POINT('Ctrl Pts',(1.21663220344887,0.897775488161019,0.893626416008965)) ;
#81912=CARTESIAN_POINT('Ctrl Pts',(1.09304305016181,1.04474874788435,0.903515073615133)) ;
#81913=CARTESIAN_POINT('Ctrl Pts',(0.791766360539703,1.28924912967893,0.924801932375028)) ;
#81914=CARTESIAN_POINT('Ctrl Pts',(0.61519892799247,1.38224129434414,0.935880152619445)) ;
#81915=CARTESIAN_POINT('Ctrl Pts',(0.237878641222853,1.49391270346963,0.957135966967693)) ;
#81916=CARTESIAN_POINT('Ctrl Pts',(0.0410377219212674,1.51217248608932,
0.966437447069915)) ;
#81917=CARTESIAN_POINT('Ctrl Pts',(-0.345272897341869,1.47236296906486,
0.986129645322456)) ;
#81918=CARTESIAN_POINT('Ctrl Pts',(-0.531180586185464,1.41594320328274,
0.99664134888848)) ;
#81919=CARTESIAN_POINT('Ctrl Pts',(-0.878202474401868,1.23239540808013,
1.01843599713659)) ;
#81920=CARTESIAN_POINT('Ctrl Pts',(-1.03460132686121,1.10437888698023,1.02951675490895)) ;
#81921=CARTESIAN_POINT('Ctrl Pts',(-1.28218302036428,0.801557459123725,
1.04984024102083)) ;
#81922=CARTESIAN_POINT('Ctrl Pts',(-1.37372075766342,0.631966212932787,
1.05864076594819)) ;
#81923=CARTESIAN_POINT('Ctrl Pts',(-1.4768043966045,0.303965309506325,1.07686303836077)) ;
#81924=CARTESIAN_POINT('Ctrl Pts',(-1.5,0.152295076973703,1.08528916239035)) ;
#81925=CARTESIAN_POINT('Ctrl Pts',(-1.5,-3.40005801291454E-15,1.09375)) ;
#81926=CARTESIAN_POINT('Origin',(0.,0.,0.)) ;
#81927=CARTESIAN_POINT('',(-1.5,2.72443420019078E-16,1.65625)) ;
#81928=CARTESIAN_POINT('',(-1.5,2.61432011258777E-15,1.59375)) ;
#81929=CARTESIAN_POINT('',(-1.5,-1.83697019872103E-16,0.)) ;
#81930=CARTESIAN_POINT('Ctrl Pts',(-1.5,2.52859025224331E-15,1.65625)) ;
#81931=CARTESIAN_POINT('Ctrl Pts',(-1.5,0.0269229379010869,1.65475428122771)) ;
#81932=CARTESIAN_POINT('Ctrl Pts',(-1.49927516504667,0.0538717048422698,
1.65325712750878)) ;
#81933=CARTESIAN_POINT('Ctrl Pts',(-1.48746761788753,0.272705869696385,
1.64109967390577)) ;
#81934=CARTESIAN_POINT('Ctrl Pts',(-1.44033365134678,0.460854217967074,
1.63064698789073)) ;
#81935=CARTESIAN_POINT('Ctrl Pts',(-1.27564436649753,0.813306103094172,
1.6110663276059)) ;
#81936=CARTESIAN_POINT('Ctrl Pts',(-1.158051507112,0.97348254049987,1.60159226410001)) ;
#81937=CARTESIAN_POINT('Ctrl Pts',(-0.867332870775922,1.23961897270468,
1.5802123785154)) ;
#81938=CARTESIAN_POINT('Ctrl Pts',(-0.69695471868813,1.3428230629645,1.56914827556607)) ;
#81939=CARTESIAN_POINT('Ctrl Pts',(-0.332746010733414,1.47493620037078,
1.5479554665621)) ;
#81940=CARTESIAN_POINT('Ctrl Pts',(-0.143341745701085,1.50518173240013,
1.53829046996668)) ;
#81941=CARTESIAN_POINT('Ctrl Pts',(0.245357930273443,1.49309609456688,1.51925343592483)) ;
#81942=CARTESIAN_POINT('Ctrl Pts',(0.440867536333831,1.44746237525733,1.50857937230333)) ;
#81943=CARTESIAN_POINT('Ctrl Pts',(0.799189721411461,1.28425366185876,1.48680601276355)) ;
#81944=CARTESIAN_POINT('Ctrl Pts',(0.959181015582752,1.16961179356638,1.47592393169228)) ;
#81945=CARTESIAN_POINT('Ctrl Pts',(1.22342689292453,0.888601187059828,1.45540454581025)) ;
#81946=CARTESIAN_POINT('Ctrl Pts',(1.32637707938175,0.726020437393559,1.4465844687441)) ;
#81947=CARTESIAN_POINT('Ctrl Pts',(1.46939559633561,0.36198147466264,1.42636008192572)) ;
#81948=CARTESIAN_POINT('Ctrl Pts',(1.50455005374878,0.162688114647428,1.41528822859153)) ;
#81949=CARTESIAN_POINT('Ctrl Pts',(1.49469916815378,-0.230234719873201,
1.39345918222928)) ;
#81950=CARTESIAN_POINT('Ctrl Pts',(1.4527919325684,-0.420174405384774,1.38290697747864)) ;
#81951=CARTESIAN_POINT('Ctrl Pts',(1.29839962557302,-0.776049202454666,
1.3631361554192)) ;
#81952=CARTESIAN_POINT('Ctrl Pts',(1.18653192056656,-0.938213766586564,
1.35394221679549)) ;
#81953=CARTESIAN_POINT('Ctrl Pts',(0.904968657590171,-1.21251461247927,
1.33277603004791)) ;
#81954=CARTESIAN_POINT('Ctrl Pts',(0.73729361318162,-1.32119397820188,1.32168988944237)) ;
#81955=CARTESIAN_POINT('Ctrl Pts',(0.376231824750659,-1.46450418670203,
1.30033745692197)) ;
#81956=CARTESIAN_POINT('Ctrl Pts',(0.187372068618979,-1.50038585439249,
1.29027566103224)) ;
#81957=CARTESIAN_POINT('Ctrl Pts',(-0.201866281378398,-1.49959079808594,
1.271526337289)) ;
#81958=CARTESIAN_POINT('Ctrl Pts',(-0.39858166171527,-1.45966713696413,
1.26095287355302)) ;
#81959=CARTESIAN_POINT('Ctrl Pts',(-0.76197337545374,-1.30676058906481,
1.23922177746569)) ;
#81960=CARTESIAN_POINT('Ctrl Pts',(-0.925640847229525,-1.19642033877903,
1.22828231560602)) ;
#81961=CARTESIAN_POINT('Ctrl Pts',(-1.19770027094282,-0.922883848769447,
1.20759461464605)) ;
#81962=CARTESIAN_POINT('Ctrl Pts',(-1.30496242672345,-0.763718567813794,
1.198678809323)) ;
#81963=CARTESIAN_POINT('Ctrl Pts',(-1.45770502735446,-0.405787189141501,
1.1787937327301)) ;
#81964=CARTESIAN_POINT('Ctrl Pts',(-1.4986024017048,-0.209141325247903,
1.16786896251378)) ;
#81965=CARTESIAN_POINT('Ctrl Pts',(-1.49998827054254,-0.00685020096107011,
1.15663056672007)) ;
#81966=CARTESIAN_POINT('Ctrl Pts',(-1.5,-0.00342483006433634,1.15644026833691)) ;
#81967=CARTESIAN_POINT('Ctrl Pts',(-1.5,6.247106623104E-15,1.15625)) ;
#81968=CARTESIAN_POINT('Ctrl Pts',(-1.5,-3.30950241189258E-15,1.09375)) ;
#81969=CARTESIAN_POINT('Ctrl Pts',(-1.5,-0.0418239384105527,1.09607355213392)) ;
#81970=CARTESIAN_POINT('Ctrl Pts',(-1.49825079600136,-0.0836950016768401,
1.09839972231539)) ;
#81971=CARTESIAN_POINT('Ctrl Pts',(-1.4781077032983,-0.323597595814322,
1.11172764421192)) ;
#81972=CARTESIAN_POINT('Ctrl Pts',(-1.42225800040326,-0.516453274940869,
1.12244184860784)) ;
#81973=CARTESIAN_POINT('Ctrl Pts',(-1.24267625242295,-0.86130018627444,
1.14160001034859)) ;
#81974=CARTESIAN_POINT('Ctrl Pts',(-1.12371979539634,-1.01161623082117,
1.15111879032567)) ;
#81975=CARTESIAN_POINT('Ctrl Pts',(-0.830646029950509,-1.26445563596451,
1.17224262524959)) ;
#81976=CARTESIAN_POINT('Ctrl Pts',(-0.657553280567444,-1.36251432324379,
1.18329440646161)) ;
#81977=CARTESIAN_POINT('Ctrl Pts',(-0.282819454972746,-1.48629234946708,
1.20476207455794)) ;
#81978=CARTESIAN_POINT('Ctrl Pts',(-0.0848134752949405,-1.51057549585254,
1.21437564599363)) ;
#81979=CARTESIAN_POINT('Ctrl Pts',(0.303657029036045,-1.4814369520598,1.23387534584185)) ;
#81980=CARTESIAN_POINT('Ctrl Pts',(0.490562705267345,-1.43045141647857,
1.24428411425954)) ;
#81981=CARTESIAN_POINT('Ctrl Pts',(0.841724617985318,-1.25749715628138,
1.26598368466809)) ;
#81982=CARTESIAN_POINT('Ctrl Pts',(1.00133669730154,-1.13452023771357,1.27707904993045)) ;
#81983=CARTESIAN_POINT('Ctrl Pts',(1.25804932273866,-0.839114472837687,
1.29763585757149)) ;
#81984=CARTESIAN_POINT('Ctrl Pts',(1.35492854746899,-0.671542838127837,
1.30644206454847)) ;
#81985=CARTESIAN_POINT('Ctrl Pts',(1.48109817934729,-0.306699476178405,
1.32671114021232)) ;
#81986=CARTESIAN_POINT('Ctrl Pts',(1.50832038413776,-0.112580848819781,
1.33749550839891)) ;
#81987=CARTESIAN_POINT('Ctrl Pts',(1.48701678921495,0.27984357135668,1.35929686507538)) ;
#81988=CARTESIAN_POINT('Ctrl Pts',(1.43687108102397,0.474293788638321,1.37009965492436)) ;
#81989=CARTESIAN_POINT('Ctrl Pts',(1.26754574646804,0.824247894447991,1.38954154969156)) ;
#81990=CARTESIAN_POINT('Ctrl Pts',(1.15313619452512,0.977932993631929,1.39876784768523)) ;
#81991=CARTESIAN_POINT('Ctrl Pts',(0.868189736426075,1.23888540915647,1.41972601875158)) ;
#81992=CARTESIAN_POINT('Ctrl Pts',(0.698656891662839,1.34181485641221,1.43074182286096)) ;
#81993=CARTESIAN_POINT('Ctrl Pts',(0.326654853270976,1.47753710554394,1.45240984175389)) ;
#81994=CARTESIAN_POINT('Ctrl Pts',(0.127470830452023,1.50782568461737,1.46239967668215)) ;
#81995=CARTESIAN_POINT('Ctrl Pts',(-0.26303471783684,1.48912044873026,1.48170747351995)) ;
#81996=CARTESIAN_POINT('Ctrl Pts',(-0.450759234289304,1.44342001010308,
1.49200883015742)) ;
#81997=CARTESIAN_POINT('Ctrl Pts',(-0.80563852961626,1.28082682702653,1.51359944552234)) ;
#81998=CARTESIAN_POINT('Ctrl Pts',(-0.968219833275402,1.16281145361195,
1.52469984695881)) ;
#81999=CARTESIAN_POINT('Ctrl Pts',(-1.23372369758581,0.874707136645695,
1.54547680527986)) ;
#82000=CARTESIAN_POINT('Ctrl Pts',(-1.33582095620383,0.709060508116284,
1.5543577495491)) ;
#82001=CARTESIAN_POINT('Ctrl Pts',(-1.46744352783767,0.359516168214211,
1.57377687954366)) ;
#82002=CARTESIAN_POINT('Ctrl Pts',(-1.5,0.180429519935487,1.58372613778136)) ;
#82003=CARTESIAN_POINT('Ctrl Pts',(-1.5,8.11850586757146E-15,1.59375)) ;
#82004=CARTESIAN_POINT('Origin',(0.,0.,0.)) ;
#82005=CARTESIAN_POINT('',(-1.5,-2.58117669796277E-15,2.15625)) ;
#82006=CARTESIAN_POINT('',(-1.5,2.9582133382325E-17,2.09375)) ;
#82007=CARTESIAN_POINT('',(-1.5,-1.83697019872103E-16,0.)) ;
#82008=CARTESIAN_POINT('Ctrl Pts',(-1.5,-2.52859025224331E-15,2.15625)) ;
#82009=CARTESIAN_POINT('Ctrl Pts',(-1.5,0.0546162866586652,2.15321576185229)) ;
#82010=CARTESIAN_POINT('Ctrl Pts',(-1.49701714440264,0.10929679695477,2.15017795572474)) ;
#82011=CARTESIAN_POINT('Ctrl Pts',(-1.4701572983793,0.353799631349553,2.13659446492503)) ;
#82012=CARTESIAN_POINT('Ctrl Pts',(-1.41315423719555,0.538102637111959,
2.12635540904934)) ;
#82013=CARTESIAN_POINT('Ctrl Pts',(-1.22854362231576,0.883699336998718,
2.10715559238897)) ;
#82014=CARTESIAN_POINT('Ctrl Pts',(-1.09945939121703,1.03993932239023,2.09692722789047)) ;
#82015=CARTESIAN_POINT('Ctrl Pts',(-0.790949993784533,1.28951844902538,
2.07515130906822)) ;
#82016=CARTESIAN_POINT('Ctrl Pts',(-0.61576020033871,1.38177511072207,2.06415980115399)) ;
#82017=CARTESIAN_POINT('Ctrl Pts',(-0.245689765772974,1.49188833445163,
2.04329607841019)) ;
#82018=CARTESIAN_POINT('Ctrl Pts',(-0.0549972007493365,1.51097828870566,
2.03420100651883)) ;
#82019=CARTESIAN_POINT('Ctrl Pts',(0.332284786771767,1.47619288546302,2.01460163200534)) ;
#82020=CARTESIAN_POINT('Ctrl Pts',(0.524850107878419,1.41917953426664,2.00375312447399)) ;
#82021=CARTESIAN_POINT('Ctrl Pts',(0.872082013459065,1.23574144606107,1.98195141917731)) ;
#82022=CARTESIAN_POINT('Ctrl Pts',(1.0243423375181,1.11279807140185,1.97121069717992)) ;
#82023=CARTESIAN_POINT('Ctrl Pts',(1.27267313163213,0.816896771103869,1.9510433957136)) ;
#82024=CARTESIAN_POINT('Ctrl Pts',(1.36683819762821,0.647125879280804,1.94220143773783)) ;
#82025=CARTESIAN_POINT('Ctrl Pts',(1.48801309414954,0.274758127034861,1.92151434039083)) ;
#82026=CARTESIAN_POINT('Ctrl Pts',(1.51130549846425,0.0749686380007088,
1.91041492433338)) ;
#82027=CARTESIAN_POINT('Ctrl Pts',(1.47912566370554,-0.314505661155098,
1.88877746326917)) ;
#82028=CARTESIAN_POINT('Ctrl Pts',(1.42688641091888,-0.500742210877754,
1.87843098828458)) ;
#82029=CARTESIAN_POINT('Ctrl Pts',(1.25197726548271,-0.849716174972452,
1.85904354583488)) ;
#82030=CARTESIAN_POINT('Ctrl Pts',(1.12855862548595,-1.00789224699645,1.84921746199072)) ;
#82031=CARTESIAN_POINT('Ctrl Pts',(0.828722297248183,-1.2656634598045,1.82763126845541)) ;
#82032=CARTESIAN_POINT('Ctrl Pts',(0.65580381773927,-1.36330731114237,1.81659939502722)) ;
#82033=CARTESIAN_POINT('Ctrl Pts',(0.288551400119727,-1.48418959168278,
1.79557211372)) ;
#82034=CARTESIAN_POINT('Ctrl Pts',(0.0985270817800627,-1.50875755782986,
1.78623365192763)) ;
#82035=CARTESIAN_POINT('Ctrl Pts',(-0.289511811254275,-1.4851705482752,
1.76690892727199)) ;
#82036=CARTESIAN_POINT('Ctrl Pts',(-0.483615784390812,-1.43375092662312,
1.75614177268656)) ;
#82037=CARTESIAN_POINT('Ctrl Pts',(-0.836465693283654,-1.26020606783978,
1.73434458300791)) ;
#82038=CARTESIAN_POINT('Ctrl Pts',(-0.992594535458914,-1.14129789894949,
1.723529825895)) ;
#82039=CARTESIAN_POINT('Ctrl Pts',(-1.24881041653316,-0.852721314778345,
1.70318661734228)) ;
#82040=CARTESIAN_POINT('Ctrl Pts',(-1.34733341302686,-0.686551437019409,
1.69439174650109)) ;
#82041=CARTESIAN_POINT('Ctrl Pts',(-1.47028769977342,-0.343671917814022,
1.67534288432301)) ;
#82042=CARTESIAN_POINT('Ctrl Pts',(-1.5,-0.172365296862037,1.66582584982566)) ;
#82043=CARTESIAN_POINT('Ctrl Pts',(-1.5,2.25514051876985E-15,1.65625)) ;
#82044=CARTESIAN_POINT('Ctrl Pts',(-1.5,7.54864033274375E-15,1.59375)) ;
#82045=CARTESIAN_POINT('Ctrl Pts',(-1.5,-0.0129956598470896,1.59447198110261)) ;
#82046=CARTESIAN_POINT('Ctrl Pts',(-1.4998311134522,-0.0259982862158395,
1.59519434923422)) ;
#82047=CARTESIAN_POINT('Ctrl Pts',(-1.49432199544045,-0.237790581132439,
1.6069605878407)) ;
#82048=CARTESIAN_POINT('Ctrl Pts',(-1.44967258468572,-0.433602909230278,
1.6178390505128)) ;
#82049=CARTESIAN_POINT('Ctrl Pts',(-1.29020513942681,-0.788341747578342,
1.63754676375435)) ;
#82050=CARTESIAN_POINT('Ctrl Pts',(-1.18007256202236,-0.945278838891628,
1.64656481124586)) ;
#82051=CARTESIAN_POINT('Ctrl Pts',(-0.902824846038532,-1.2137886544314,
1.6673625041877)) ;
#82052=CARTESIAN_POINT('Ctrl Pts',(-0.736765013385657,-1.32119210250901,
1.67833549072461)) ;
#82053=CARTESIAN_POINT('Ctrl Pts',(-0.369999760342863,-1.46719105679223,
1.70003701869695)) ;
#82054=CARTESIAN_POINT('Ctrl Pts',(-0.172499063470922,-1.50324432377842,
1.71036051483423)) ;
#82055=CARTESIAN_POINT('Ctrl Pts',(0.217098298309571,-1.49643436804736,
1.7292941920795)) ;
#82056=CARTESIAN_POINT('Ctrl Pts',(0.405567626217661,-1.4566876028183,1.73946600365822)) ;
#82057=CARTESIAN_POINT('Ctrl Pts',(0.764272895356052,-1.30583450988432,
1.7609145826589)) ;
#82058=CARTESIAN_POINT('Ctrl Pts',(0.930016830917273,-1.19347891965801,
1.77200993009403)) ;
#82059=CARTESIAN_POINT('Ctrl Pts',(1.20532717911403,-0.913728422884884,
1.79302665253012)) ;
#82060=CARTESIAN_POINT('Ctrl Pts',(1.31335149919757,-0.750210145417528,
1.80207165858792)) ;
#82061=CARTESIAN_POINT('Ctrl Pts',(1.46068461359121,-0.392035362147135,
1.8219702576585)) ;
#82062=CARTESIAN_POINT('Ctrl Pts',(1.49896468002721,-0.200948327247076,
1.83258620404183)) ;
#82063=CARTESIAN_POINT('Ctrl Pts',(1.50103431974765,0.192875182678861,1.85446528792661)) ;
#82064=CARTESIAN_POINT('Ctrl Pts',(1.46177450149586,0.391838905988002,1.86551882811045)) ;
#82065=CARTESIAN_POINT('Ctrl Pts',(1.31125661025412,0.752891371694118,1.88557729842745)) ;
#82066=CARTESIAN_POINT('Ctrl Pts',(1.20524243635297,0.913036805574294,1.89445821306591)) ;
#82067=CARTESIAN_POINT('Ctrl Pts',(0.935442584319375,1.18874637796397,1.91509756373221)) ;
#82068=CARTESIAN_POINT('Ctrl Pts',(0.772829410305134,1.3003456666158,1.92602127395511)) ;
#82069=CARTESIAN_POINT('Ctrl Pts',(0.410876996161621,1.45625561726341,1.94776654956251)) ;
#82070=CARTESIAN_POINT('Ctrl Pts',(0.214493555574436,1.49783821050788,1.9583701242877)) ;
#82071=CARTESIAN_POINT('Ctrl Pts',(-0.174599479057064,1.50190859994096,
1.97720343801786)) ;
#82072=CARTESIAN_POINT('Ctrl Pts',(-0.363610770720251,1.46766903245709,
1.98714231379472)) ;
#82073=CARTESIAN_POINT('Ctrl Pts',(-0.725602415935666,1.32762477447494,
2.00844876322279)) ;
#82074=CARTESIAN_POINT('Ctrl Pts',(-0.894083220046043,1.22053486918689,
2.01952951928133)) ;
#82075=CARTESIAN_POINT('Ctrl Pts',(-1.17832317452849,0.948597663829845,
2.04075883172748)) ;
#82076=CARTESIAN_POINT('Ctrl Pts',(-1.29185235241837,0.78701312183995,2.05002704878667)) ;
#82077=CARTESIAN_POINT('Ctrl Pts',(-1.44925948417428,0.432132132919838,
2.06974265928224)) ;
#82078=CARTESIAN_POINT('Ctrl Pts',(-1.49270519361291,0.242702620053888,
2.08026652110812)) ;
#82079=CARTESIAN_POINT('Ctrl Pts',(-1.49971956391621,0.0335040329801223,
2.09188866483444)) ;
#82080=CARTESIAN_POINT('Ctrl Pts',(-1.5,0.016746278066708,2.09281965121851)) ;
#82081=CARTESIAN_POINT('Ctrl Pts',(-1.5,2.71453568615908E-15,2.09375)) ;
#82082=CARTESIAN_POINT('Origin',(0.,0.,0.)) ;
#82083=CARTESIAN_POINT('',(-1.5,2.95259119040324E-15,2.65625)) ;
#82084=CARTESIAN_POINT('',(-1.5,-2.17351668110822E-15,2.59374999999999)) ;
#82085=CARTESIAN_POINT('',(-1.5,-1.83697019872103E-16,0.)) ;
#82086=CARTESIAN_POINT('Ctrl Pts',(-1.5,4.90844004519485E-15,2.65625)) ;
#82087=CARTESIAN_POINT('Ctrl Pts',(-1.5,0.0856151677731844,2.65149360179037)) ;
#82088=CARTESIAN_POINT('Ctrl Pts',(-1.49267015243007,0.171275020595029,
2.64673472107806)) ;
#82089=CARTESIAN_POINT('Ctrl Pts',(-1.44552368503536,0.443435938984391,
2.63161467005643)) ;
#82090=CARTESIAN_POINT('Ctrl Pts',(-1.37772363683179,0.622905801337482,
2.62189948712345)) ;
#82091=CARTESIAN_POINT('Ctrl Pts',(-1.17421465332585,0.954334641509284,
2.60290179991787)) ;
#82092=CARTESIAN_POINT('Ctrl Pts',(-1.03753186268452,1.10137961099408,2.59224106360131)) ;
#82093=CARTESIAN_POINT('Ctrl Pts',(-0.717891608916212,1.33141761329456,
2.57047242021322)) ;
#82094=CARTESIAN_POINT('Ctrl Pts',(-0.538864177307172,1.41339116705685,
2.55958191573383)) ;
#82095=CARTESIAN_POINT('Ctrl Pts',(-0.163728105175774,1.50317931500609,
2.53903905782737)) ;
#82096=CARTESIAN_POINT('Ctrl Pts',(0.0284310311749173,1.51180110239942,
2.5302099197748)) ;
#82097=CARTESIAN_POINT('Ctrl Pts',(0.415438810102884,1.45519666383705,2.51001765381397)) ;
#82098=CARTESIAN_POINT('Ctrl Pts',(0.605959319102716,1.38671697207505,2.49894901789082)) ;
#82099=CARTESIAN_POINT('Ctrl Pts',(0.942235074590785,1.18294306354376,2.47710955671331)) ;
#82100=CARTESIAN_POINT('Ctrl Pts',(1.08632518335127,1.05217672404664,2.46654461980391)) ;
#82101=CARTESIAN_POINT('Ctrl Pts',(1.31840597987018,0.741499024173853,2.44674869116767)) ;
#82102=CARTESIAN_POINT('Ctrl Pts',(1.40351763898725,0.564058291685003,2.43758657176028)) ;
#82103=CARTESIAN_POINT('Ctrl Pts',(1.50182787618189,0.183588868926401,2.41644938160702)) ;
#82104=CARTESIAN_POINT('Ctrl Pts',(1.51292131336378,-0.0160007193501419,
2.40536107114722)) ;
#82105=CARTESIAN_POINT('Ctrl Pts',(1.45801957138463,-0.400610722115376,
2.38399384877137)) ;
#82106=CARTESIAN_POINT('Ctrl Pts',(1.39538669614711,-0.582434990200783,
2.37389250054441)) ;
#82107=CARTESIAN_POINT('Ctrl Pts',(1.2013344585767,-0.919931291483191,2.35514270602872)) ;
#82108=CARTESIAN_POINT('Ctrl Pts',(1.06900829993795,-1.07086927598327,2.34460298370062)) ;
#82109=CARTESIAN_POINT('Ctrl Pts',(0.755658547689445,-1.31043320461103,
2.32287238314336)) ;
#82110=CARTESIAN_POINT('Ctrl Pts',(0.578526738081543,-1.39770077925359,
2.31192602568447)) ;
#82111=CARTESIAN_POINT('Ctrl Pts',(0.205950389837252,-1.49792085516064,
2.29121654677434)) ;
#82112=CARTESIAN_POINT('Ctrl Pts',(0.0145779287054259,-1.51193972266469,
2.28228303988477)) ;
#82113=CARTESIAN_POINT('Ctrl Pts',(-0.371893252832265,-1.46671798710535,
2.26243277717244)) ;
#82114=CARTESIAN_POINT('Ctrl Pts',(-0.562875788981263,-1.40453509871487,
2.25151682316247)) ;
#82115=CARTESIAN_POINT('Ctrl Pts',(-0.904622987191438,-1.21204236583417,
2.22972748306456)) ;
#82116=CARTESIAN_POINT('Ctrl Pts',(-1.05318792417667,-1.08544895413135,
2.21906316554277)) ;
#82117=CARTESIAN_POINT('Ctrl Pts',(-1.29410955375517,-0.782757285562262,
2.19906371633051)) ;
#82118=CARTESIAN_POINT('Ctrl Pts',(-1.38416170816597,-0.609531542906844,
2.19011286349483)) ;
#82119=CARTESIAN_POINT('Ctrl Pts',(-1.4794846403777,-0.286011580132301,
2.17213953222958)) ;
#82120=CARTESIAN_POINT('Ctrl Pts',(-1.5,-0.143226625156057,2.16420703473089)) ;
#82121=CARTESIAN_POINT('Ctrl Pts',(-1.5,-2.22044604925031E-15,2.15625)) ;
#82122=CARTESIAN_POINT('Ctrl Pts',(-1.5,2.42861286636753E-15,2.09375)) ;
#82123=CARTESIAN_POINT('Ctrl Pts',(-1.5,-0.183119263433166,2.10392329241295)) ;
#82124=CARTESIAN_POINT('Ctrl Pts',(-1.46646507623563,-0.364866211108705,
2.1140203450616)) ;
#82125=CARTESIAN_POINT('Ctrl Pts',(-1.33264810871975,-0.714495462261993,
2.13344419234789)) ;
#82126=CARTESIAN_POINT('Ctrl Pts',(-1.23099892811952,-0.878122479994064,
2.14224916090078)) ;
#82127=CARTESIAN_POINT('Ctrl Pts',(-0.969112872690051,-1.16136842759558,
2.16271710260632)) ;
#82128=CARTESIAN_POINT('Ctrl Pts',(-0.810248162224439,-1.27728043816115,
2.17358026262359)) ;
#82129=CARTESIAN_POINT('Ctrl Pts',(-0.453507260029782,-1.44355364633095,
2.19536266750995)) ;
#82130=CARTESIAN_POINT('Ctrl Pts',(-0.258393502074163,-1.49089672958314,
2.20606516821237)) ;
#82131=CARTESIAN_POINT('Ctrl Pts',(0.13012335116139,-1.50637293458213,2.22518758861236)) ;
#82132=CARTESIAN_POINT('Ctrl Pts',(0.31970346636198,-1.47780726939408,2.23474820493614)) ;
#82133=CARTESIAN_POINT('Ctrl Pts',(0.684825873911802,-1.34902317392027,
2.25589250094536)) ;
#82134=CARTESIAN_POINT('Ctrl Pts',(0.855975079196342,-1.24746050606069,
2.26694810614223)) ;
#82135=CARTESIAN_POINT('Ctrl Pts',(1.14940356144279,-0.983785017423248,
2.28839000970545)) ;
#82136=CARTESIAN_POINT('Ctrl Pts',(1.26871450560737,-0.824200283726239,
2.29796109534854)) ;
#82137=CARTESIAN_POINT('Ctrl Pts',(1.43644424776305,-0.472774642873999,
2.31748474206255)) ;
#82138=CARTESIAN_POINT('Ctrl Pts',(1.48510597361535,-0.285181351989462,
2.32790659155614)) ;
#82139=CARTESIAN_POINT('Ctrl Pts',(1.50952613238539,0.105638303090151,2.34961879461612)) ;
#82140=CARTESIAN_POINT('Ctrl Pts',(1.48209760582561,0.305331840139509,2.36071288000775)) ;
#82141=CARTESIAN_POINT('Ctrl Pts',(1.35327120458257,0.674844555199689,2.38124136417776)) ;
#82142=CARTESIAN_POINT('Ctrl Pts',(1.25604736977719,0.842082751174055,2.3900429136113)) ;
#82143=CARTESIAN_POINT('Ctrl Pts',(1.00218649199299,1.13285682360821,2.41033385835603)) ;
#82144=CARTESIAN_POINT('Ctrl Pts',(0.847205378895785,1.25298607802845,2.42112731437042)) ;
#82145=CARTESIAN_POINT('Ctrl Pts',(0.496008451564929,1.42951229977629,2.4429277905745)) ;
#82146=CARTESIAN_POINT('Ctrl Pts',(0.302347799540614,1.48261176133978,2.45372027808274)) ;
#82147=CARTESIAN_POINT('Ctrl Pts',(-0.0854763866555089,1.50955261960386,
2.47312783511495)) ;
#82148=CARTESIAN_POINT('Ctrl Pts',(-0.275694147693553,1.48662992010136,
2.4823857319737)) ;
#82149=CARTESIAN_POINT('Ctrl Pts',(-0.643805120793757,1.3689898690344,2.50336425862092)) ;
#82150=CARTESIAN_POINT('Ctrl Pts',(-0.817424516468723,1.27296262986177,
2.5143849490004)) ;
#82151=CARTESIAN_POINT('Ctrl Pts',(-1.11987963846953,1.01763999896081,2.53602912314528)) ;
#82152=CARTESIAN_POINT('Ctrl Pts',(-1.24499584225552,0.860044432785634,
2.54596975373413)) ;
#82153=CARTESIAN_POINT('Ctrl Pts',(-1.4228357870948,0.512082877429392,2.56530095125392)) ;
#82154=CARTESIAN_POINT('Ctrl Pts',(-1.47652293354409,0.326418477279332,
2.57561564015114)) ;
#82155=CARTESIAN_POINT('Ctrl Pts',(-1.49795431175567,0.0905134319012143,
2.58872147600548)) ;
#82156=CARTESIAN_POINT('Ctrl Pts',(-1.5,0.0452298468524057,2.59123723073041)) ;
#82157=CARTESIAN_POINT('Ctrl Pts',(-1.5,-4.53662128371792E-15,2.59374999999999)) ;
#82158=CARTESIAN_POINT('Origin',(0.,0.,0.)) ;
#82159=CARTESIAN_POINT('',(-1.5,4.9605336138464E-15,3.15624999999999)) ;
#82160=CARTESIAN_POINT('',(-1.5,-1.366870264779E-15,3.09374999999999)) ;
#82161=CARTESIAN_POINT('',(-1.5,-1.83697019872103E-16,0.)) ;
#82162=CARTESIAN_POINT('Ctrl Pts',(-1.5,6.24500451351651E-15,3.15624999999999)) ;
#82163=CARTESIAN_POINT('Ctrl Pts',(-1.5,0.11516372949426,3.14985201502809)) ;
#82164=CARTESIAN_POINT('Ctrl Pts',(-1.48673694768359,0.230214992296067,
3.14346027820577)) ;
#82165=CARTESIAN_POINT('Ctrl Pts',(-1.41687259925006,0.52778747825224,3.12692847343043)) ;
#82166=CARTESIAN_POINT('Ctrl Pts',(-1.33873153172212,0.702759013395465,
3.11780533381227)) ;
#82167=CARTESIAN_POINT('Ctrl Pts',(-1.11619744824656,1.02159711063618,3.09824204391682)) ;
#82168=CARTESIAN_POINT('Ctrl Pts',(-0.971072864716749,1.16041120195476,
3.08740378715517)) ;
#82169=CARTESIAN_POINT('Ctrl Pts',(-0.639341229669528,1.37071314560809,
3.06560162076536)) ;
#82170=CARTESIAN_POINT('Ctrl Pts',(-0.456936833216421,1.44181586604181,
3.05485060958163)) ;
#82171=CARTESIAN_POINT('Ctrl Pts',(-0.076827813420807,1.51031865257357,
3.03465975065849)) ;
#82172=CARTESIAN_POINT('Ctrl Pts',(0.117152483621678,1.5077271851314,3.02582814253516)) ;
#82173=CARTESIAN_POINT('Ctrl Pts',(0.500482061088619,1.42801404311459,3.00517093569534)) ;
#82174=CARTESIAN_POINT('Ctrl Pts',(0.685533458305974,1.34897721804582,2.99407217883254)) ;
#82175=CARTESIAN_POINT('Ctrl Pts',(1.0077052814503,1.12751207314981,2.97241987018396)) ;
#82176=CARTESIAN_POINT('Ctrl Pts',(1.14343765683333,0.989608280268855,2.96205878231517)) ;
#82177=CARTESIAN_POINT('Ctrl Pts',(1.35929288258575,0.664593590765959,2.94264525710447)) ;
#82178=CARTESIAN_POINT('Ctrl Pts',(1.43519482065327,0.479168724862576,2.93287048471459)) ;
#82179=CARTESIAN_POINT('Ctrl Pts',(1.51010457232472,0.0911069665243634,
2.91131149814024)) ;
#82180=CARTESIAN_POINT('Ctrl Pts',(1.5090224152309,-0.10755521505248,2.90027471027486)) ;
#82181=CARTESIAN_POINT('Ctrl Pts',(1.43159011268547,-0.486451731858559,
2.87922490378564)) ;
#82182=CARTESIAN_POINT('Ctrl Pts',(1.35855993933727,-0.663607641540354,
2.86984686662555)) ;
#82183=CARTESIAN_POINT('Ctrl Pts',(1.14541164191085,-0.988726092516216,
2.85056069630151)) ;
#82184=CARTESIAN_POINT('Ctrl Pts',(1.00440406782438,-1.1316786535961,2.83980556175569)) ;
#82185=CARTESIAN_POINT('Ctrl Pts',(0.678507252619518,-1.35183260774445,
2.81801045630824)) ;
#82186=CARTESIAN_POINT('Ctrl Pts',(0.497694190148281,-1.42833269597271,
2.80718608133322)) ;
#82187=CARTESIAN_POINT('Ctrl Pts',(0.120010058617026,-1.50738721206899,
2.78681878630208)) ;
#82188=CARTESIAN_POINT('Ctrl Pts',(-0.0730332829740776,-1.51039185153122,
2.77802484707712)) ;
#82189=CARTESIAN_POINT('Ctrl Pts',(-0.458262098731161,-1.44219981361828,
2.75759629376202)) ;
#82190=CARTESIAN_POINT('Ctrl Pts',(-0.64611281319328,-1.36838199386208,
2.74650782705528)) ;
#82191=CARTESIAN_POINT('Ctrl Pts',(-0.97543592605115,-1.15563014064546,
2.72475348769992)) ;
#82192=CARTESIAN_POINT('Ctrl Pts',(-1.11538240998354,-1.02122344350407,
2.71428678998734)) ;
#82193=CARTESIAN_POINT('Ctrl Pts',(-1.33937983434098,-0.703352071176045,
2.69467994854068)) ;
#82194=CARTESIAN_POINT('Ctrl Pts',(-1.41993041352524,-0.521972346371288,
2.6852484636873)) ;
#82195=CARTESIAN_POINT('Ctrl Pts',(-1.48771873938675,-0.221564625713655,
2.66855914587298)) ;
#82196=CARTESIAN_POINT('Ctrl Pts',(-1.5,-0.11081974676082,2.66240665259782)) ;
#82197=CARTESIAN_POINT('Ctrl Pts',(-1.5,4.8919202022546E-15,2.65625)) ;
#82198=CARTESIAN_POINT('Ctrl Pts',(-1.5,-4.71844785465692E-15,2.59374999999999)) ;
#82199=CARTESIAN_POINT('Ctrl Pts',(-1.5,-0.153082698281981,2.60225459434899)) ;
#82200=CARTESIAN_POINT('Ctrl Pts',(-1.47656373062122,-0.305549815759312,
2.6107249897644)) ;
#82201=CARTESIAN_POINT('Ctrl Pts',(-1.37219374715963,-0.635783357289578,
2.62907129762719)) ;
#82202=CARTESIAN_POINT('Ctrl Pts',(-1.27927337608324,-0.806593936310442,
2.637939651449)) ;
#82203=CARTESIAN_POINT('Ctrl Pts',(-1.0331884703089,-1.10456312202827,2.65805633882385)) ;
#82204=CARTESIAN_POINT('Ctrl Pts',(-0.882042538773507,-1.22862754510375,
2.66877458481975)) ;
#82205=CARTESIAN_POINT('Ctrl Pts',(-0.536452871603693,-1.41483555485109,
2.69057422014909)) ;
#82206=CARTESIAN_POINT('Ctrl Pts',(-0.344353610376509,-1.47342515704064,
2.70144408911385)) ;
#82207=CARTESIAN_POINT('Ctrl Pts',(0.0426928743225535,-1.5113830347619,
2.72112025728359)) ;
#82208=CARTESIAN_POINT('Ctrl Pts',(0.233586323798436,-1.49383764067041,
2.73015960389171)) ;
#82209=CARTESIAN_POINT('Ctrl Pts',(0.604430425126557,-1.38674616323053,
2.75097661229803)) ;
#82210=CARTESIAN_POINT('Ctrl Pts',(0.780228173717907,-1.29600964493656,
2.7619551442622)) ;
#82211=CARTESIAN_POINT('Ctrl Pts',(1.08925985428694,-1.05026891225514,2.7836495693893)) ;
#82212=CARTESIAN_POINT('Ctrl Pts',(1.21870925393897,-0.896800942013726,
2.79392772544368)) ;
#82213=CARTESIAN_POINT('Ctrl Pts',(1.4064648072281,-0.555274007709077,2.81290144401616)) ;
#82214=CARTESIAN_POINT('Ctrl Pts',(1.46565146626508,-0.371907038656333,
2.82308849785242)) ;
#82215=CARTESIAN_POINT('Ctrl Pts',(1.51298910573879,0.0144777298509668,
2.84455431832505)) ;
#82216=CARTESIAN_POINT('Ctrl Pts',(1.49781990267104,0.214214659586258,2.85565081442145)) ;
#82217=CARTESIAN_POINT('Ctrl Pts',(1.39181447279936,0.592030983292885,2.87664061018293)) ;
#82218=CARTESIAN_POINT('Ctrl Pts',(1.30366680435728,0.766874008586105,2.88566269075828)) ;
#82219=CARTESIAN_POINT('Ctrl Pts',(1.06616214320864,1.07266709457545,2.90558389148421)) ;
#82220=CARTESIAN_POINT('Ctrl Pts',(0.919318889984905,1.20089696350865,2.91621083160269)) ;
#82221=CARTESIAN_POINT('Ctrl Pts',(0.578469661586673,1.39846618248674,2.93809798161059)) ;
#82222=CARTESIAN_POINT('Ctrl Pts',(0.386223523438131,1.46327854042905,2.94914777152099)) ;
#82223=CARTESIAN_POINT('Ctrl Pts',(-0.00191788599131014,1.5120232743001,
2.96917625417444)) ;
#82224=CARTESIAN_POINT('Ctrl Pts',(-0.193515144967493,1.4995921901257,2.97807182980533)) ;
#82225=CARTESIAN_POINT('Ctrl Pts',(-0.566855974091238,1.40245224833857,
2.99873253053781)) ;
#82226=CARTESIAN_POINT('Ctrl Pts',(-0.744563820988319,1.31674461952063,
3.00966327077524)) ;
#82227=CARTESIAN_POINT('Ctrl Pts',(-1.05973596143589,1.08002680934193,3.0314024921798)) ;
#82228=CARTESIAN_POINT('Ctrl Pts',(-1.19338051697833,0.930251518216961,
3.04199289360978)) ;
#82229=CARTESIAN_POINT('Ctrl Pts',(-1.39023496041013,0.594544362523114,
3.0607892562046)) ;
#82230=CARTESIAN_POINT('Ctrl Pts',(-1.45442868124805,0.413433012454585,
3.07078149930807)) ;
#82231=CARTESIAN_POINT('Ctrl Pts',(-1.49434802658991,0.150424648214569,
3.08539307509918)) ;
#82232=CARTESIAN_POINT('Ctrl Pts',(-1.5,0.0751804928068105,3.08957330595517)) ;
#82233=CARTESIAN_POINT('Ctrl Pts',(-1.5,-4.53662128371792E-15,3.09374999999999)) ;
#82234=CARTESIAN_POINT('Origin',(0.,0.,0.)) ;
#82235=CARTESIAN_POINT('',(-1.5,3.76526828577686E-16,3.65624999999999)) ;
#82236=CARTESIAN_POINT('',(-1.5,-2.3990307329852E-15,3.59374999999999)) ;
#82237=CARTESIAN_POINT('',(-1.5,-1.83697019872103E-16,0.)) ;
#82238=CARTESIAN_POINT('Ctrl Pts',(-1.5,5.48172618408671E-15,3.65624999999999)) ;
#82239=CARTESIAN_POINT('Ctrl Pts',(-1.5,0.142496679359764,3.64833351781334)) ;
#82240=CARTESIAN_POINT('Ctrl Pts',(-1.47969327645223,0.284545958301245,
3.64044189120548)) ;
#82241=CARTESIAN_POINT('Ctrl Pts',(-1.38587417389988,0.604715323638973,
3.62265470424227)) ;
#82242=CARTESIAN_POINT('Ctrl Pts',(-1.29792548082208,0.775701489755982,
3.61381587187405)) ;
#82243=CARTESIAN_POINT('Ctrl Pts',(-1.05655434668454,1.08347140714469,3.5936537333964)) ;
#82244=CARTESIAN_POINT('Ctrl Pts',(-0.902412425877809,1.21484681248879,
3.58258825995869)) ;
#82245=CARTESIAN_POINT('Ctrl Pts',(-0.558362594348466,1.4054957323175,3.56073935139277)) ;
#82246=CARTESIAN_POINT('Ctrl Pts',(-0.373217195344678,1.46557591106783,
3.55016264537576)) ;
#82247=CARTESIAN_POINT('Ctrl Pts',(0.0115988163075127,1.5125503090816,3.5303433319935)) ;
#82248=CARTESIAN_POINT('Ctrl Pts',(0.207685058067254,1.49827154866902,3.52120973544787)) ;
#82249=CARTESIAN_POINT('Ctrl Pts',(0.586630438424552,1.39466352798266,3.50009971676013)) ;
#82250=CARTESIAN_POINT('Ctrl Pts',(0.76543470542945,1.30511535190838,3.48900954311744)) ;
#82251=CARTESIAN_POINT('Ctrl Pts',(1.07206353486311,1.06630935655377,3.46762335681191)) ;
#82252=CARTESIAN_POINT('Ctrl Pts',(1.19878375694058,0.921562637602475,3.45750578509147)) ;
#82253=CARTESIAN_POINT('Ctrl Pts',(1.39527810543078,0.585390369828785,3.43871382779262)) ;
#82254=CARTESIAN_POINT('Ctrl Pts',(1.46050827894949,0.395546863964534,3.42822482577581)) ;
#82255=CARTESIAN_POINT('Ctrl Pts',(1.51269993114629,0.00450706484213029,
3.40650039249123)) ;
#82256=CARTESIAN_POINT('Ctrl Pts',(1.50039210501571,-0.192640250105679,
3.39554776388301)) ;
#82257=CARTESIAN_POINT('Ctrl Pts',(1.40216511092891,-0.565773747141564,
3.3748181251588)) ;
#82258=CARTESIAN_POINT('Ctrl Pts',(1.31923545756705,-0.738766459596867,
3.36586712166821)) ;
#82259=CARTESIAN_POINT('Ctrl Pts',(1.08795698672388,-1.05162490322803,3.34604921872853)) ;
#82260=CARTESIAN_POINT('Ctrl Pts',(0.939086996871196,-1.18644950149429,
3.33514158027261)) ;
#82261=CARTESIAN_POINT('Ctrl Pts',(0.6021584415055,-1.3873787830828,3.31334972866142)) ;
#82262=CARTESIAN_POINT('Ctrl Pts',(0.418406018236275,-1.45339795551531,
3.30267507017396)) ;
#82263=CARTESIAN_POINT('Ctrl Pts',(0.0360862450027967,-1.51197500679322,
3.28265356119461)) ;
#82264=CARTESIAN_POINT('Ctrl Pts',(-0.158832651584457,-1.50404331095635,
3.27372047468086)) ;
#82265=CARTESIAN_POINT('Ctrl Pts',(-0.540230368816554,-1.41337675207924,
3.25285195293048)) ;
#82266=CARTESIAN_POINT('Ctrl Pts',(-0.722490448810619,-1.32946682039408,
3.24175212930753)) ;
#82267=CARTESIAN_POINT('Ctrl Pts',(-1.03765275048246,-1.09992646574874,
3.2202127550361)) ;
#82268=CARTESIAN_POINT('Ctrl Pts',(-1.1692973788514,-0.958815715680369,
3.20995925684313)) ;
#82269=CARTESIAN_POINT('Ctrl Pts',(-1.37731088447788,-0.627018029011212,
3.19073459997994)) ;
#82270=CARTESIAN_POINT('Ctrl Pts',(-1.44867384821221,-0.437629584726534,
3.18056275470703)) ;
#82271=CARTESIAN_POINT('Ctrl Pts',(-1.49357976662945,-0.160308684359475,
3.16515603801997)) ;
#82272=CARTESIAN_POINT('Ctrl Pts',(-1.5,-0.080127120084231,3.16070150667134)) ;
#82273=CARTESIAN_POINT('Ctrl Pts',(-1.5,4.90844004519486E-15,3.15624999999999)) ;
#82274=CARTESIAN_POINT('Ctrl Pts',(-1.5,-3.81639164714898E-15,3.09374999999999)) ;
#82275=CARTESIAN_POINT('Ctrl Pts',(-1.5,-0.121704222728767,3.10051134570714)) ;
#82276=CARTESIAN_POINT('Ctrl Pts',(-1.48518751341521,-0.243241611160598,
3.10726342284225)) ;
#82277=CARTESIAN_POINT('Ctrl Pts',(-1.40853373838638,-0.551575580172437,
3.12439308778735)) ;
#82278=CARTESIAN_POINT('Ctrl Pts',(-1.32477505881493,-0.730180718244438,
3.13362786132713)) ;
#82279=CARTESIAN_POINT('Ctrl Pts',(-1.09510085243453,-1.04301082593862,
3.1533677919475)) ;
#82280=CARTESIAN_POINT('Ctrl Pts',(-0.952239643711773,-1.17487850304191,
3.16390419608755)) ;
#82281=CARTESIAN_POINT('Ctrl Pts',(-0.618017382571796,-1.38135918941648,
3.18572004674559)) ;
#82282=CARTESIAN_POINT('Ctrl Pts',(-0.428279776959831,-1.45144424895783,
3.19679560876136)) ;
#82283=CARTESIAN_POINT('Ctrl Pts',(-0.0417903806202598,-1.51151426505888,
3.21705920007102)) ;
#82284=CARTESIAN_POINT('Ctrl Pts',(0.150626335212339,-1.50457189944236,
3.22587001572508)) ;
#82285=CARTESIAN_POINT('Ctrl Pts',(0.526536562508407,-1.41800688506666,
3.24636058870112)) ;
#82286=CARTESIAN_POINT('Ctrl Pts',(0.706117818651959,-1.33767455866574,
3.25723214942692)) ;
#82287=CARTESIAN_POINT('Ctrl Pts',(1.02767040139798,-1.11058884241468,3.27901079184003)) ;
#82288=CARTESIAN_POINT('Ctrl Pts',(1.16566595481994,-0.964759812582032,
3.28970091238387)) ;
#82289=CARTESIAN_POINT('Ctrl Pts',(1.37207905979523,-0.635217788060569,
3.30878591265294)) ;
#82290=CARTESIAN_POINT('Ctrl Pts',(1.44145359726056,-0.456452881821541,
3.31839150656546)) ;
#82291=CARTESIAN_POINT('Ctrl Pts',(1.51102102328224,-0.0754717113844235,
3.3395571271453)) ;
#82292=CARTESIAN_POINT('Ctrl Pts',(1.50784793467382,0.123598206813867,3.35061656704521)) ;
#82293=CARTESIAN_POINT('Ctrl Pts',(1.42468299433366,0.509064698350426,3.37203137213057)) ;
#82294=CARTESIAN_POINT('Ctrl Pts',(1.34553229762618,0.691660079507657,3.3815591604665)) ;
#82295=CARTESIAN_POINT('Ctrl Pts',(1.1239977878084,1.01170303964803,3.4011078267658)) ;
#82296=CARTESIAN_POINT('Ctrl Pts',(0.985322197553707,1.14718555235198,3.41154326234343)) ;
#82297=CARTESIAN_POINT('Ctrl Pts',(0.658147482027504,1.36260820231781,3.43326842568257)) ;
#82298=CARTESIAN_POINT('Ctrl Pts',(0.471132314614464,1.43802161298724,3.44436101408298)) ;
#82299=CARTESIAN_POINT('Ctrl Pts',(0.0864670322230408,1.50971448154214,
3.464859699682)) ;
#82300=CARTESIAN_POINT('Ctrl Pts',(-0.106856079585841,1.50840865112193,
3.47365754188383)) ;
#82301=CARTESIAN_POINT('Ctrl Pts',(-0.485287758308828,1.43257301216333,
3.49397139004218)) ;
#82302=CARTESIAN_POINT('Ctrl Pts',(-0.666603529977372,1.35771808035757,
3.50477425283521)) ;
#82303=CARTESIAN_POINT('Ctrl Pts',(-0.994313764835153,1.14055612369053,
3.52657349543525)) ;
#82304=CARTESIAN_POINT('Ctrl Pts',(-1.13659166351795,0.998854267157603,
3.53735500670874)) ;
#82305=CARTESIAN_POINT('Ctrl Pts',(-1.35261269373874,0.675643420895191,
3.55672640243397)) ;
#82306=CARTESIAN_POINT('Ctrl Pts',(-1.42720468076801,0.499163062174969,
3.56601871876805)) ;
#82307=CARTESIAN_POINT('Ctrl Pts',(-1.48895486038857,0.210151736290253,
3.58207490353942)) ;
#82308=CARTESIAN_POINT('Ctrl Pts',(-1.5,0.105095275150541,3.58791137360274)) ;
#82309=CARTESIAN_POINT('Ctrl Pts',(-1.5,-3.15719672627779E-15,3.59374999999999)) ;
#82310=CARTESIAN_POINT('Origin',(0.,0.,0.)) ;
#82311=CARTESIAN_POINT('',(-1.5,-4.02009930659002E-13,4.15625000000004)) ;
#82312=CARTESIAN_POINT('',(-1.5,-2.45107243726451E-15,4.09374999999999)) ;
#82313=CARTESIAN_POINT('',(-1.5,-1.83697019872103E-16,0.)) ;
#82314=CARTESIAN_POINT('Ctrl Pts',(-1.5,-8.04321886871406E-13,4.15625000000004)) ;
#82315=CARTESIAN_POINT('Ctrl Pts',(-1.50000000000009,0.171133603059582,
4.14674257760779)) ;
#82316=CARTESIAN_POINT('Ctrl Pts',(-1.47071121488924,0.341198831191777,
4.13729450937823)) ;
#82317=CARTESIAN_POINT('Ctrl Pts',(-1.3488319714892,0.683790252304662,4.11826165264973)) ;
#82318=CARTESIAN_POINT('Ctrl Pts',(-1.25026747431287,0.850734260237844,
4.1094386813423)) ;
#82319=CARTESIAN_POINT('Ctrl Pts',(-0.990699880929532,1.14378752497098,
4.08880986121809)) ;
#82320=CARTESIAN_POINT('Ctrl Pts',(-0.830110001358271,1.26516499485942,
4.077711880649)) ;
#82321=CARTESIAN_POINT('Ctrl Pts',(-0.477711658905107,1.43477190385086,
4.05604580446502)) ;
#82322=CARTESIAN_POINT('Ctrl Pts',(-0.290524636825963,1.48404678783509,
4.04567101788883)) ;
#82323=CARTESIAN_POINT('Ctrl Pts',(0.0986115526744294,1.50981516157915,
4.02623290608265)) ;
#82324=CARTESIAN_POINT('Ctrl Pts',(0.296994345781134,1.48360506722658,4.01650543807702)) ;
#82325=CARTESIAN_POINT('Ctrl Pts',(0.670868265347628,1.355980088746,3.99497228244384)) ;
#82326=CARTESIAN_POINT('Ctrl Pts',(0.84282849344545,1.25633852853655,3.98393102099506)) ;
#82327=CARTESIAN_POINT('Ctrl Pts',(1.13328837743446,1.0008741800697,3.96286003140905)) ;
#82328=CARTESIAN_POINT('Ctrl Pts',(1.25077829060998,0.84948125492726,3.95344340305152)) ;
#82329=CARTESIAN_POINT('Ctrl Pts',(1.42707774789501,0.502985826171431,3.93419365700952)) ;
#82330=CARTESIAN_POINT('Ctrl Pts',(1.48110434042375,0.309600183743426,3.92345001020796)) ;
#82331=CARTESIAN_POINT('Ctrl Pts',(1.51030351771318,-0.0826705098748036,
3.90165719389584)) ;
#82332=CARTESIAN_POINT('Ctrl Pts',(1.48686269123112,-0.277669729350829,
3.89082390392495)) ;
#82333=CARTESIAN_POINT('Ctrl Pts',(1.36782940170216,-0.644688161043389,
3.87043399105314)) ;
#82334=CARTESIAN_POINT('Ctrl Pts',(1.27459213170475,-0.813629810466613,
3.86163968112704)) ;
#82335=CARTESIAN_POINT('Ctrl Pts',(1.02409018249644,-1.1140981305869,3.84124105825081)) ;
#82336=CARTESIAN_POINT('Ctrl Pts',(0.866649844836005,-1.2405158785012,3.83015460236462)) ;
#82337=CARTESIAN_POINT('Ctrl Pts',(0.518273761921561,-1.42069517993084,
3.80838836966519)) ;
#82338=CARTESIAN_POINT('Ctrl Pts',(0.332030838647065,-1.47538359057195,
3.79790863032345)) ;
#82339=CARTESIAN_POINT('Ctrl Pts',(-0.0549754716884883,-1.51179841551055,
3.77827725762096)) ;
#82340=CARTESIAN_POINT('Ctrl Pts',(-0.252182033789337,-1.49163500350121,
3.76888452522838)) ;
#82341=CARTESIAN_POINT('Ctrl Pts',(-0.628701513673564,-1.37612462376939,
3.74756060164698)) ;
#82342=CARTESIAN_POINT('Ctrl Pts',(-0.804182037469132,-1.28151209916078,
3.73648966532583)) ;
#82343=CARTESIAN_POINT('Ctrl Pts',(-1.10286143022979,-1.03435426175478,
3.71525395085802)) ;
#82344=CARTESIAN_POINT('Ctrl Pts',(-1.22497837383202,-0.886328218669872,
3.70549045659277)) ;
#82345=CARTESIAN_POINT('Ctrl Pts',(-1.41154877671446,-0.54503485247189,
3.68652971402622)) ;
#82346=CARTESIAN_POINT('Ctrl Pts',(-1.4712707707181,-0.353369120526585,
3.67588161780703)) ;
#82347=CARTESIAN_POINT('Ctrl Pts',(-1.49730613246558,-0.103865648310611,
3.66202031379503)) ;
#82348=CARTESIAN_POINT('Ctrl Pts',(-1.5,-0.0519031454973351,3.65913350808318)) ;
#82349=CARTESIAN_POINT('Ctrl Pts',(-1.5,4.90844004519485E-15,3.65624999999999)) ;
#82350=CARTESIAN_POINT('Ctrl Pts',(-1.5,-4.53662128371792E-15,3.59374999999999)) ;
#82351=CARTESIAN_POINT('Ctrl Pts',(-1.5,-0.0905641075434439,3.59878133930796)) ;
#82352=CARTESIAN_POINT('Ctrl Pts',(-1.49179821598492,-0.181157037767087,
3.60381427987594)) ;
#82353=CARTESIAN_POINT('Ctrl Pts',(-1.43946376029427,-0.466437771598478,
3.61966320953324)) ;
#82354=CARTESIAN_POINT('Ctrl Pts',(-1.3649492311358,-0.6530734364045,3.62955311162014)) ;
#82355=CARTESIAN_POINT('Ctrl Pts',(-1.1515028967344,-0.980181871746283,
3.64890889859832)) ;
#82356=CARTESIAN_POINT('Ctrl Pts',(-1.01702360187864,-1.11908761046717,
3.65923752943101)) ;
#82357=CARTESIAN_POINT('Ctrl Pts',(-0.696993112621626,-1.34306654442955,
3.68085664057898)) ;
#82358=CARTESIAN_POINT('Ctrl Pts',(-0.512789648427401,-1.42361647993805,
3.69195663209073)) ;
#82359=CARTESIAN_POINT('Ctrl Pts',(-0.130042475882154,-1.5067093297347,
3.71267969873235)) ;
#82360=CARTESIAN_POINT('Ctrl Pts',(0.0642221720734728,-1.51094601393429,
3.72153583475192)) ;
#82361=CARTESIAN_POINT('Ctrl Pts',(0.445023198793493,-1.4455165182095,3.74167461868465)) ;
#82362=CARTESIAN_POINT('Ctrl Pts',(0.627860421384518,-1.37598756773571,
3.75240273839343)) ;
#82363=CARTESIAN_POINT('Ctrl Pts',(0.961231665515552,-1.16857762400818,
3.77420345718079)) ;
#82364=CARTESIAN_POINT('Ctrl Pts',(1.10752938938788,-1.03098917949774,3.78506411093882)) ;
#82365=CARTESIAN_POINT('Ctrl Pts',(1.33277994479441,-0.713995037954878,
3.80470687615938)) ;
#82366=CARTESIAN_POINT('Ctrl Pts',(1.41240534053575,-0.53964380029473,3.81376978887251)) ;
#82367=CARTESIAN_POINT('Ctrl Pts',(1.50377672399984,-0.164570939699714,
3.83460717001667)) ;
#82368=CARTESIAN_POINT('Ctrl Pts',(1.51239069939861,0.0331458714058803,
3.84559143730032)) ;
#82369=CARTESIAN_POINT('Ctrl Pts',(1.45265193985208,0.423505349670125,3.86727807498167)) ;
#82370=CARTESIAN_POINT('Ctrl Pts',(1.38377694290032,0.612103399456392,3.87750920633362)) ;
#82371=CARTESIAN_POINT('Ctrl Pts',(1.18061920560496,0.944794807510319,3.89652506552808)) ;
#82372=CARTESIAN_POINT('Ctrl Pts',(1.05083061160804,1.08730435962015,3.90672812083795)) ;
#82373=CARTESIAN_POINT('Ctrl Pts',(0.738873468516821,1.32039470365947,3.92821189766176)) ;
#82374=CARTESIAN_POINT('Ctrl Pts',(0.557904269288321,1.40645870723091,3.9393094490851)) ;
#82375=CARTESIAN_POINT('Ctrl Pts',(0.177414530578306,1.50203357785154,3.96027062769135)) ;
#82376=CARTESIAN_POINT('Ctrl Pts',(-0.0179401791249838,1.5123670491789,
3.96926961812673)) ;
#82377=CARTESIAN_POINT('Ctrl Pts',(-0.401221132172622,1.4582059859365,3.98921470555712)) ;
#82378=CARTESIAN_POINT('Ctrl Pts',(-0.585526905180342,1.39444825345553,
3.99985316931986)) ;
#82379=CARTESIAN_POINT('Ctrl Pts',(-0.926440532557907,1.1966931789007,4.02174858038001)) ;
#82380=CARTESIAN_POINT('Ctrl Pts',(-1.07823908104159,1.06197238198835,4.03279423580782)) ;
#82381=CARTESIAN_POINT('Ctrl Pts',(-1.31331721168121,0.749262857926172,
4.05279081331)) ;
#82382=CARTESIAN_POINT('Ctrl Pts',(-1.39766131060398,0.576842450533384,
4.06170319719258)) ;
#82383=CARTESIAN_POINT('Ctrl Pts',(-1.48243173092841,0.264783173922913,
4.07903982367094)) ;
#82384=CARTESIAN_POINT('Ctrl Pts',(-1.5,0.132541600323799,4.08638657775978)) ;
#82385=CARTESIAN_POINT('Ctrl Pts',(-1.5,-3.78169717762944E-15,4.09374999999999)) ;
#82386=CARTESIAN_POINT('Origin',(0.,0.,0.)) ;
#82387=CARTESIAN_POINT('',(-1.5,-1.25411323884051E-15,4.65624999999999)) ;
#82388=CARTESIAN_POINT('',(-1.5,5.49396108270927E-15,4.59374999999999)) ;
#82389=CARTESIAN_POINT('',(-1.5,-1.83697019872103E-16,0.)) ;
#82390=CARTESIAN_POINT('Ctrl Pts',(-1.5,0.,4.65624999999999)) ;
#82391=CARTESIAN_POINT('Ctrl Pts',(-1.5,0.00765172681326447,4.65582490406592)) ;
#82392=CARTESIAN_POINT('Ctrl Pts',(-1.49994145115902,0.0153060271662843,
4.65539966515743)) ;
#82393=CARTESIAN_POINT('Ctrl Pts',(-1.49678001132018,0.221801716357427,
4.64392768242458)) ;
#82394=CARTESIAN_POINT('Ctrl Pts',(-1.45422382952216,0.418088612371266,
4.63302285486826)) ;
#82395=CARTESIAN_POINT('Ctrl Pts',(-1.29850811284946,0.774615782250993,
4.61321578987494)) ;
#82396=CARTESIAN_POINT('Ctrl Pts',(-1.18998137611373,0.932794904983397,
4.60425870273628)) ;
#82397=CARTESIAN_POINT('Ctrl Pts',(-0.915634517518497,1.20412163064066,
4.58352232985737)) ;
#82398=CARTESIAN_POINT('Ctrl Pts',(-0.750907326550277,1.31317493739108,
4.57256763066582)) ;
#82399=CARTESIAN_POINT('Ctrl Pts',(-0.385960185672472,1.46307114925216,
4.55084531950087)) ;
#82400=CARTESIAN_POINT('Ctrl Pts',(-0.188887711273289,1.50126810659913,
4.54037308942916)) ;
#82401=CARTESIAN_POINT('Ctrl Pts',(0.200517010733479,1.49872002276902,4.52156706589991)) ;
#82402=CARTESIAN_POINT('Ctrl Pts',(0.389208644959509,1.46111640651101,4.51144409051933)) ;
#82403=CARTESIAN_POINT('Ctrl Pts',(0.749197883699321,1.31450704403914,4.49005161790413)) ;
#82404=CARTESIAN_POINT('Ctrl Pts',(0.916033315803187,1.20420703080166,4.47896085517791)) ;
#82405=CARTESIAN_POINT('Ctrl Pts',(1.19485086801825,0.927500969508377,4.45785995996203)) ;
#82406=CARTESIAN_POINT('Ctrl Pts',(1.30502448153115,0.764741922445452,4.44873566235808)) ;
#82407=CARTESIAN_POINT('Ctrl Pts',(1.45631999560281,0.407853490475697,4.42890852724865)) ;
#82408=CARTESIAN_POINT('Ctrl Pts',(1.4966402198032,0.217402276981722,4.41832790427676)) ;
#82409=CARTESIAN_POINT('Ctrl Pts',(1.50308295672099,-0.175933966475625,
4.39647589075135)) ;
#82410=CARTESIAN_POINT('Ctrl Pts',(1.46612859314491,-0.375092801046321,
4.38541151105298)) ;
#82411=CARTESIAN_POINT('Ctrl Pts',(1.31981917380275,-0.737829091200718,
4.36525949493329)) ;
#82412=CARTESIAN_POINT('Ctrl Pts',(1.21552803507139,-0.89933901492746,4.35641714721779)) ;
#82413=CARTESIAN_POINT('Ctrl Pts',(0.948850606174006,-1.17803578888138,
4.33584504638346)) ;
#82414=CARTESIAN_POINT('Ctrl Pts',(0.787706228951202,-1.2913547622266,4.32494423465987)) ;
#82415=CARTESIAN_POINT('Ctrl Pts',(0.427778741293969,-1.45138281896797,
4.30318199153753)) ;
#82416=CARTESIAN_POINT('Ctrl Pts',(0.231876508787605,-1.49524768493686,
4.29253817248236)) ;
#82417=CARTESIAN_POINT('Ctrl Pts',(-0.157001735674165,-1.50383036417844,
4.27358985146548)) ;
#82418=CARTESIAN_POINT('Ctrl Pts',(-0.34623035278147,-1.47184339249322,
4.26380985639869)) ;
#82419=CARTESIAN_POINT('Ctrl Pts',(-0.709480149048449,-1.33627470610578,
4.24256719558311)) ;
#82420=CARTESIAN_POINT('Ctrl Pts',(-0.879042040408571,-1.23137319434659,
4.23149521439916)) ;
#82421=CARTESIAN_POINT('Ctrl Pts',(-1.16694178851328,-0.962698703891227,
4.21018045101975)) ;
#82422=CARTESIAN_POINT('Ctrl Pts',(-1.28275904458616,-0.801908652806195,
4.20080048071145)) ;
#82423=CARTESIAN_POINT('Ctrl Pts',(-1.44428227005255,-0.448395681485922,
4.18116087119366)) ;
#82424=CARTESIAN_POINT('Ctrl Pts',(-1.48981764891001,-0.25968189653311,
4.17067677204504)) ;
#82425=CARTESIAN_POINT('Ctrl Pts',(-1.49949364665084,-0.0450232754631008,
4.15875129309639)) ;
#82426=CARTESIAN_POINT('Ctrl Pts',(-1.49999999999999,-0.0225024017976655,
4.1575001334332)) ;
#82427=CARTESIAN_POINT('Ctrl Pts',(-1.5,-8.04835511280435E-13,4.15625000000004)) ;
#82428=CARTESIAN_POINT('Ctrl Pts',(-1.5,-4.53662128371792E-15,4.09374999999999)) ;
#82429=CARTESIAN_POINT('Ctrl Pts',(-1.5,-0.0621643353056686,4.09720357418364)) ;
#82430=CARTESIAN_POINT('Ctrl Pts',(-1.49613569807775,-0.124394669725961,
4.10066081498477)) ;
#82431=CARTESIAN_POINT('Ctrl Pts',(-1.4636951723303,-0.383526246747067,
4.11505701370816)) ;
#82432=CARTESIAN_POINT('Ctrl Pts',(-1.40005833887612,-0.573898595494419,
4.12563325530524)) ;
#82433=CARTESIAN_POINT('Ctrl Pts',(-1.20639289314394,-0.911524647065871,
4.14439025817032)) ;
#82434=CARTESIAN_POINT('Ctrl Pts',(-1.08101171753964,-1.0572279674842,4.15444057636129)) ;
#82435=CARTESIAN_POINT('Ctrl Pts',(-0.778107783103184,-1.29727904975425,
4.17568213432053)) ;
#82436=CARTESIAN_POINT('Ctrl Pts',(-0.602191679243006,-1.38771539990994,
4.1866580226546)) ;
#82437=CARTESIAN_POINT('Ctrl Pts',(-0.23119587925635,-1.49421100262234,
4.20746577759026)) ;
#82438=CARTESIAN_POINT('Ctrl Pts',(-0.0402621150360292,-1.51145138543449,
4.21649479404729)) ;
#82439=CARTESIAN_POINT('Ctrl Pts',(0.346736688744763,-1.47286633657555,
4.23618608958829)) ;
#82440=CARTESIAN_POINT('Ctrl Pts',(0.538742248805719,-1.41396560245127,
4.24706009290733)) ;
#82441=CARTESIAN_POINT('Ctrl Pts',(0.884004652664943,-1.22721178111378,
4.26885914420636)) ;
#82442=CARTESIAN_POINT('Ctrl Pts',(1.03492934112488,-1.10292691552911,4.27957286904285)) ;
#82443=CARTESIAN_POINT('Ctrl Pts',(1.28056959752403,-0.804549316003377,
4.29967950804266)) ;
#82444=CARTESIAN_POINT('Ctrl Pts',(1.37324335257794,-0.633532114432611,
4.3085537714204)) ;
#82445=CARTESIAN_POINT('Ctrl Pts',(1.49067185552879,-0.259792178928917,
4.3293171011706)) ;
#82446=CARTESIAN_POINT('Ctrl Pts',(1.5119480039113,-0.0599858873288936,
4.34041745070394)) ;
#82447=CARTESIAN_POINT('Ctrl Pts',(1.47599570015083,0.328776967556811,4.36201538708648)) ;
#82448=CARTESIAN_POINT('Ctrl Pts',(1.42202227581893,0.514326649085503,4.37232370272696)) ;
#82449=CARTESIAN_POINT('Ctrl Pts',(1.24360105625019,0.862086606103215,4.39164370033906)) ;
#82450=CARTESIAN_POINT('Ctrl Pts',(1.11814673318228,1.01956661567486,4.40160776843016)) ;
#82451=CARTESIAN_POINT('Ctrl Pts',(0.815172055919553,1.2744009339664,4.42326337545008)) ;
#82452=CARTESIAN_POINT('Ctrl Pts',(0.641415145557375,1.37010641258235,4.43428174421479)) ;
#82453=CARTESIAN_POINT('Ctrl Pts',(0.273134641221515,1.48710228282742,4.45525053352567)) ;
#82454=CARTESIAN_POINT('Ctrl Pts',(0.082877658089358,1.50969770846992,4.46449316602518)) ;
#82455=CARTESIAN_POINT('Ctrl Pts',(-0.30490254158167,1.48208868848018,4.48391716680266)) ;
#82456=CARTESIAN_POINT('Ctrl Pts',(-0.498473081444425,1.42865500899227,
4.49471460261874)) ;
#82457=CARTESIAN_POINT('Ctrl Pts',(-0.849337655166835,1.25153667703389,
4.51651553595822)) ;
#82458=CARTESIAN_POINT('Ctrl Pts',(-1.00408899033133,1.1311654253393,4.52730465892319)) ;
#82459=CARTESIAN_POINT('Ctrl Pts',(-1.25747997168065,0.83995402889664,4.54758514365428)) ;
#82460=CARTESIAN_POINT('Ctrl Pts',(-1.35444448938871,0.672501804939245,
4.55638878861447)) ;
#82461=CARTESIAN_POINT('Ctrl Pts',(-1.47210926486592,0.333075112485226,
4.57524582708414)) ;
#82462=CARTESIAN_POINT('Ctrl Pts',(-1.5,0.166997886469703,4.58447233964056)) ;
#82463=CARTESIAN_POINT('Ctrl Pts',(-1.5,1.65839564303383E-14,4.59374999999999)) ;
#82464=CARTESIAN_POINT('Origin',(0.,0.,0.)) ;
#82465=CARTESIAN_POINT('',(-1.5,-2.7806698977001E-15,5.15624999999999)) ;
#82466=CARTESIAN_POINT('',(-1.5,-6.37154749297209E-15,5.09374999999999)) ;
#82467=CARTESIAN_POINT('',(-1.5,-1.83697019872103E-16,0.)) ;
#82468=CARTESIAN_POINT('Ctrl Pts',(-1.5,-9.66814085323955E-15,5.15624999999999)) ;
#82469=CARTESIAN_POINT('Ctrl Pts',(-1.5,0.0358778710446101,5.15425678494196)) ;
#82470=CARTESIAN_POINT('Ctrl Pts',(-1.49871280185265,0.0717941731031292,
5.1522614348276)) ;
#82471=CARTESIAN_POINT('Ctrl Pts',(-1.48185844774037,0.305972268779071,
5.13925154062338)) ;
#82472=CARTESIAN_POINT('Ctrl Pts',(-1.42830463508477,0.499492211148273,
5.12850043271399)) ;
#82473=CARTESIAN_POINT('Ctrl Pts',(-1.25285565470282,0.84641263616168,5.1092270757688)) ;
#82474=CARTESIAN_POINT('Ctrl Pts',(-1.13574394743954,0.998084772639103,
5.09983559579764)) ;
#82475=CARTESIAN_POINT('Ctrl Pts',(-0.845959362352989,1.25422483603939,
5.07877832668596)) ;
#82476=CARTESIAN_POINT('Ctrl Pts',(-0.674293667046528,1.35427282196232,
5.06773994634956)) ;
#82477=CARTESIAN_POINT('Ctrl Pts',(-0.300644760146208,1.48289082680636,
5.04619003257767)) ;
#82478=CARTESIAN_POINT('Ctrl Pts',(-0.102164262404235,1.50959942036534,
5.03643203093243)) ;
#82479=CARTESIAN_POINT('Ctrl Pts',(0.287142172077644,1.48469945082299,5.01700985054969)) ;
#82480=CARTESIAN_POINT('Ctrl Pts',(0.474399076081781,1.43586485023365,5.00664393187212)) ;
#82481=CARTESIAN_POINT('Ctrl Pts',(0.827110495698803,1.267120446311,4.9849867512302)) ;
#82482=CARTESIAN_POINT('Ctrl Pts',(0.98794944184971,1.14615564342732,4.97388825041206)) ;
#82483=CARTESIAN_POINT('Ctrl Pts',(1.24825034059657,0.85370948220949,4.95324101310364)) ;
#82484=CARTESIAN_POINT('Ctrl Pts',(1.34724911561222,0.686926261582246,4.9444125700879)) ;
#82485=CARTESIAN_POINT('Ctrl Pts',(1.47752437579179,0.323349875497477,4.92421388197208)) ;
#82486=CARTESIAN_POINT('Ctrl Pts',(1.50691094426993,0.12977056403595,4.91345947577977)) ;
#82487=CARTESIAN_POINT('Ctrl Pts',(1.49014787033123,-0.262669902249338,
4.89165722765281)) ;
#82488=CARTESIAN_POINT('Ctrl Pts',(1.44224511840853,-0.457696413105614,
4.88082242149413)) ;
#82489=CARTESIAN_POINT('Ctrl Pts',(1.27694453026968,-0.809618891741693,
4.86127117268102)) ;
#82490=CARTESIAN_POINT('Ctrl Pts',(1.1642916284679,-0.964629821186249,4.85213840094854)) ;
#82491=CARTESIAN_POINT('Ctrl Pts',(0.882501782854819,-1.22869548071468,
4.83124562347111)) ;
#82492=CARTESIAN_POINT('Ctrl Pts',(0.714381461137337,-1.33347598066378,
4.8202463612781)) ;
#82493=CARTESIAN_POINT('Ctrl Pts',(0.343487252002561,-1.4738235931734,4.79850316052909)) ;
#82494=CARTESIAN_POINT('Ctrl Pts',(0.143841614987716,-1.50645645807607,
4.78834992898549)) ;
#82495=CARTESIAN_POINT('Ctrl Pts',(-0.247427045197487,-1.49176808150959,
4.76911699633502)) ;
#82496=CARTESIAN_POINT('Ctrl Pts',(-0.43542601141659,-1.44809320631804,
4.75885870087798)) ;
#82497=CARTESIAN_POINT('Ctrl Pts',(-0.791649844461233,-1.28948614391686,
4.73731412198628)) ;
#82498=CARTESIAN_POINT('Ctrl Pts',(-0.955328727134092,-1.17338797641708,
4.72621416897474)) ;
#82499=CARTESIAN_POINT('Ctrl Pts',(-1.22417988671094,-0.888109521141881,
4.70535465999318)) ;
#82500=CARTESIAN_POINT('Ctrl Pts',(-1.32828705678375,-0.723190900739279,
4.69642727226329)) ;
#82501=CARTESIAN_POINT('Ctrl Pts',(-1.46552817676442,-0.369810352166903,
4.67679501956483)) ;
#82502=CARTESIAN_POINT('Ctrl Pts',(-1.5,-0.185662761463316,4.66656459785906)) ;
#82503=CARTESIAN_POINT('Ctrl Pts',(-1.5,-1.21430643318376E-15,4.65624999999999)) ;
#82504=CARTESIAN_POINT('Ctrl Pts',(-1.5,1.95223456881304E-14,4.59374999999999)) ;
#82505=CARTESIAN_POINT('Ctrl Pts',(-1.5,-0.0320111368243377,4.59552839649023)) ;
#82506=CARTESIAN_POINT('Ctrl Pts',(-1.49897530445879,-0.0640561019145464,
4.59730867232857)) ;
#82507=CARTESIAN_POINT('Ctrl Pts',(-1.48462161618699,-0.287671320592608,
4.60973174003291)) ;
#82508=CARTESIAN_POINT('Ctrl Pts',(-1.43565537777401,-0.475152250276413,
4.62014734723757)) ;
#82509=CARTESIAN_POINT('Ctrl Pts',(-1.26731784412456,-0.826371888221436,
4.63965954934563)) ;
#82510=CARTESIAN_POINT('Ctrl Pts',(-1.14766192513784,-0.985838022986705,
4.64925081274265)) ;
#82511=CARTESIAN_POINT('Ctrl Pts',(-0.853691440025888,-1.24901877064535,
4.67070505062593)) ;
#82512=CARTESIAN_POINT('Ctrl Pts',(-0.682389630276099,-1.35025200138103,
4.68175884697734)) ;
#82513=CARTESIAN_POINT('Ctrl Pts',(-0.317085410119675,-1.4783693765413,
4.70289337044097)) ;
#82514=CARTESIAN_POINT('Ctrl Pts',(-0.127469282574041,-1.50659832384462,
4.71243384450923)) ;
#82515=CARTESIAN_POINT('Ctrl Pts',(0.261009659059859,-1.49044119644595,
4.73157335539755)) ;
#82516=CARTESIAN_POINT('Ctrl Pts',(0.456042047119949,-1.44275517335332,
4.74228146729572)) ;
#82517=CARTESIAN_POINT('Ctrl Pts',(0.812462143084706,-1.27586824385568,
4.7640654851998)) ;
#82518=CARTESIAN_POINT('Ctrl Pts',(0.971099373314515,-1.15970239190812,
4.77492475171863)) ;
#82519=CARTESIAN_POINT('Ctrl Pts',(1.23251076416176,-0.87600802413215,4.79538231222975)) ;
#82520=CARTESIAN_POINT('Ctrl Pts',(1.333898276055,-0.712169709791253,4.80418501612269)) ;
#82521=CARTESIAN_POINT('Ctrl Pts',(1.47306533952245,-0.346621996132162,
4.82449322243709)) ;
#82522=CARTESIAN_POINT('Ctrl Pts',(1.50611694989444,-0.147191233787431,
4.83557270923402)) ;
#82523=CARTESIAN_POINT('Ctrl Pts',(1.49229096300096,0.245211971655472,4.85737288731418)) ;
#82524=CARTESIAN_POINT('Ctrl Pts',(1.44853602465491,0.434537231392048,4.86789095729955)) ;
#82525=CARTESIAN_POINT('Ctrl Pts',(1.29052135595237,0.789217113746672,4.88759539520814)) ;
#82526=CARTESIAN_POINT('Ctrl Pts',(1.17665589276148,0.95068459184539,4.89687935562658)) ;
#82527=CARTESIAN_POINT('Ctrl Pts',(0.891876127301889,1.22214282251285,4.91812133488799)) ;
#82528=CARTESIAN_POINT('Ctrl Pts',(0.723234361962776,1.32891104260048,4.92920089949725)) ;
#82529=CARTESIAN_POINT('Ctrl Pts',(0.361056190313792,1.46829590893425,4.95049800674786)) ;
#82530=CARTESIAN_POINT('Ctrl Pts',(0.172013588665832,1.50220377904007,4.96041277627217)) ;
#82531=CARTESIAN_POINT('Ctrl Pts',(-0.217048948562838,1.49747032732517,
4.97926304109208)) ;
#82532=CARTESIAN_POINT('Ctrl Pts',(-0.413363412819334,1.45555212138303,
4.98987261976694)) ;
#82533=CARTESIAN_POINT('Ctrl Pts',(-0.775021318655709,1.29903559041336,
5.0116205752902)) ;
#82534=CARTESIAN_POINT('Ctrl Pts',(-0.937419838664237,1.18718251485956,
5.0225410076036)) ;
#82535=CARTESIAN_POINT('Ctrl Pts',(-1.20676155290839,0.911033510993222,
5.04317052253512)) ;
#82536=CARTESIAN_POINT('Ctrl Pts',(-1.31252281641666,0.750688607805427,
5.05204507734413)) ;
#82537=CARTESIAN_POINT('Ctrl Pts',(-1.46110471375442,0.392569188654103,
5.07194060063031)) ;
#82538=CARTESIAN_POINT('Ctrl Pts',(-1.5,0.197217047500341,5.08279349736108)) ;
#82539=CARTESIAN_POINT('Ctrl Pts',(-1.5,-9.85322934354826E-15,5.09374999999999)) ;
#82540=CARTESIAN_POINT('Origin',(0.,0.,0.)) ;
#82541=CARTESIAN_POINT('',(-1.5,-5.13989382502856E-15,5.65624999999999)) ;
#82542=CARTESIAN_POINT('',(-1.5,-8.41852119462473E-15,5.59374999999999)) ;
#82543=CARTESIAN_POINT('',(-1.5,-1.83697019872103E-16,0.)) ;
#82544=CARTESIAN_POINT('Ctrl Pts',(-1.5,0.,5.65624999999999)) ;
#82545=CARTESIAN_POINT('Ctrl Pts',(-1.5,0.0650814565690276,5.65263436352393)) ;
#82546=CARTESIAN_POINT('Ctrl Pts',(-1.49576451485979,0.130229312342809,
5.64901503820318)) ;
#82547=CARTESIAN_POINT('Ctrl Pts',(-1.46141322360216,0.392188518898155,
5.63446174895011)) ;
#82548=CARTESIAN_POINT('Ctrl Pts',(-1.39662093449307,0.582176712153985,
5.62394004736951)) ;
#82549=CARTESIAN_POINT('Ctrl Pts',(-1.20092845884759,0.918757008787729,
5.60517533606088)) ;
#82550=CARTESIAN_POINT('Ctrl Pts',(-1.07457820645903,1.06376728008664,5.59506824361685)) ;
#82551=CARTESIAN_POINT('Ctrl Pts',(-0.768594274302649,1.3032498457893,5.57369429132526)) ;
#82552=CARTESIAN_POINT('Ctrl Pts',(-0.590053583094108,1.39321180250573,
5.56260530507226)) ;
#82553=CARTESIAN_POINT('Ctrl Pts',(-0.211298116530195,1.4977819459821,5.54147769798311)) ;
#82554=CARTESIAN_POINT('Ctrl Pts',(-0.0151228445687375,1.51253455941324,
5.53232578040448)) ;
#82555=CARTESIAN_POINT('Ctrl Pts',(0.369873909890915,1.46641759897383,5.51252158874024)) ;
#82556=CARTESIAN_POINT('Ctrl Pts',(0.555114459108075,1.40677584347651,5.50195248323015)) ;
#82557=CARTESIAN_POINT('Ctrl Pts',(0.899528101985093,1.21697598270753,5.48010965575648)) ;
#82558=CARTESIAN_POINT('Ctrl Pts',(1.05394430128351,1.0860013605719,5.46904211895559)) ;
#82559=CARTESIAN_POINT('Ctrl Pts',(1.29606201221943,0.778822370194039,5.44886047542417)) ;
#82560=CARTESIAN_POINT('Ctrl Pts',(1.38444040948578,0.608004917147279,5.44002805095262)) ;
#82561=CARTESIAN_POINT('Ctrl Pts',(1.49377708886147,0.238094230949914,5.41947745727499)) ;
#82562=CARTESIAN_POINT('Ctrl Pts',(1.51204684812289,0.0420157054333175,
5.40858420585741)) ;
#82563=CARTESIAN_POINT('Ctrl Pts',(1.47212613995471,-0.349790423796505,
5.38681719867797)) ;
#82564=CARTESIAN_POINT('Ctrl Pts',(1.41286922649614,-0.541603734889573,
5.37616090361725)) ;
#82565=CARTESIAN_POINT('Ctrl Pts',(1.22713958797241,-0.883327715334427,
5.35717623803698)) ;
#82566=CARTESIAN_POINT('Ctrl Pts',(1.10540567548876,-1.03162909753595,5.34744415820516)) ;
#82567=CARTESIAN_POINT('Ctrl Pts',(0.807403531470688,-1.27947723051666,
5.32622185300559)) ;
#82568=CARTESIAN_POINT('Ctrl Pts',(0.63220846676621,-1.37450981795897,5.31515298242931)) ;
#82569=CARTESIAN_POINT('Ctrl Pts',(0.255900539130508,-1.49102034763574,
5.29381145521729)) ;
#82570=CARTESIAN_POINT('Ctrl Pts',(0.058598105097295,-1.51168064046602,
5.28439376488116)) ;
#82571=CARTESIAN_POINT('Ctrl Pts',(-0.328587791549555,-1.47614852043145,
5.26477827140891)) ;
#82572=CARTESIAN_POINT('Ctrl Pts',(-0.514915163604716,-1.42190993977774,
5.25430696430074)) ;
#82573=CARTESIAN_POINT('Ctrl Pts',(-0.863637689112102,-1.24260683538295,
5.23254840218082)) ;
#82574=CARTESIAN_POINT('Ctrl Pts',(-1.02134589636858,-1.11660552177777,
5.22146062603237)) ;
#82575=CARTESIAN_POINT('Ctrl Pts',(-1.27260482338139,-0.816749981215801,
5.20104260469895)) ;
#82576=CARTESIAN_POINT('Ctrl Pts',(-1.36628395637511,-0.647976112865997,
5.192248672937)) ;
#82577=CARTESIAN_POINT('Ctrl Pts',(-1.4750072213027,-0.315423368644648,
5.17377352048026)) ;
#82578=CARTESIAN_POINT('Ctrl Pts',(-1.5,-0.158084744109952,5.16503248578388)) ;
#82579=CARTESIAN_POINT('Ctrl Pts',(-1.5,-8.67361737988404E-15,5.15624999999999)) ;
#82580=CARTESIAN_POINT('Ctrl Pts',(-1.5,-9.37072593030258E-15,5.09374999999999)) ;
#82581=CARTESIAN_POINT('Ctrl Pts',(-1.5,-0.00344187472693873,5.0939412152626)) ;
#82582=CARTESIAN_POINT('Ctrl Pts',(-1.49998815350225,-0.00688431746682617,
5.09413246208148)) ;
#82583=CARTESIAN_POINT('Ctrl Pts',(-1.49863541206654,-0.203360670571187,
5.10504781503172)) ;
#82584=CARTESIAN_POINT('Ctrl Pts',(-1.46005586441752,-0.394355894599877,
5.11565866081109)) ;
#82585=CARTESIAN_POINT('Ctrl Pts',(-1.31214236584632,-0.752343006402527,
5.13554683368902)) ;
#82586=CARTESIAN_POINT('Ctrl Pts',(-1.20380450774007,-0.915750154214858,
5.14460276623412)) ;
#82587=CARTESIAN_POINT('Ctrl Pts',(-0.927980887698286,-1.19505702468341,
5.16563186052046)) ;
#82588=CARTESIAN_POINT('Ctrl Pts',(-0.762075891344222,-1.30711280946583,
5.17672662906761)) ;
#82589=CARTESIAN_POINT('Ctrl Pts',(-0.403179906210228,-1.4573462967812,
5.19816717262872)) ;
#82590=CARTESIAN_POINT('Ctrl Pts',(-0.214676580361502,-1.49677985789189,
5.20833191981973)) ;
#82591=CARTESIAN_POINT('Ctrl Pts',(0.174895511444021,-1.50296666459241,
5.22724707156747)) ;
#82592=CARTESIAN_POINT('Ctrl Pts',(0.372335002413048,-1.46659980515433,
5.23759175934614)) ;
#82593=CARTESIAN_POINT('Ctrl Pts',(0.738836998698976,-1.32003003331521,
5.25929647741508)) ;
#82594=CARTESIAN_POINT('Ctrl Pts',(0.904703092032137,-1.21238450586634,
5.2702668670916)) ;
#82595=CARTESIAN_POINT('Ctrl Pts',(1.18152734442406,-0.943462455361497,
5.29105563710312)) ;
#82596=CARTESIAN_POINT('Ctrl Pts',(1.29142533718613,-0.786344642180421,
5.30006418654552)) ;
#82597=CARTESIAN_POINT('Ctrl Pts',(1.45034640196986,-0.431344230680077,
5.31978643162887)) ;
#82598=CARTESIAN_POINT('Ctrl Pts',(1.49469098466996,-0.235461288359372,
5.33066881731336)) ;
#82599=CARTESIAN_POINT('Ctrl Pts',(1.50428467728115,0.156896843711251,5.35246649131728)) ;
#82600=CARTESIAN_POINT('Ctrl Pts',(1.47149572243588,0.349575647701331,5.36317086931673)) ;
#82601=CARTESIAN_POINT('Ctrl Pts',(1.33473263596281,0.711123641425198,5.38325686896805)) ;
#82602=CARTESIAN_POINT('Ctrl Pts',(1.232343504703,0.876664118202146,5.39214395987996)) ;
#82603=CARTESIAN_POINT('Ctrl Pts',(0.966352187603716,1.16435852619215,5.4129329844238)) ;
#82604=CARTESIAN_POINT('Ctrl Pts',(0.80360990004434,1.28209565947801,5.42403340230932)) ;
#82605=CARTESIAN_POINT('Ctrl Pts',(0.448532344779636,1.44410974785279,5.445617470496)) ;
#82606=CARTESIAN_POINT('Ctrl Pts',(0.260766569034991,1.48951565285212,5.45591263073244)) ;
#82607=CARTESIAN_POINT('Ctrl Pts',(-0.129850519027224,1.50763748789584,
5.47520958845111)) ;
#82608=CARTESIAN_POINT('Ctrl Pts',(-0.32910134254664,1.47700956127791,5.48522251902366)) ;
#82609=CARTESIAN_POINT('Ctrl Pts',(-0.700944457067442,1.34061643389493,
5.50690152719526)) ;
#82610=CARTESIAN_POINT('Ctrl Pts',(-0.870273581683968,1.23741727326228,
5.51791502185275)) ;
#82611=CARTESIAN_POINT('Ctrl Pts',(-1.15476252292559,0.976012346349693,
5.53886375038982)) ;
#82612=CARTESIAN_POINT('Ctrl Pts',(-1.26891717769988,0.822135710191326,
5.54807579387825)) ;
#82613=CARTESIAN_POINT('Ctrl Pts',(-1.43766062436454,0.471895763218968,
5.56753356871005)) ;
#82614=CARTESIAN_POINT('Ctrl Pts',(-1.48748217415704,0.277360504023277,
5.57834108310981)) ;
#82615=CARTESIAN_POINT('Ctrl Pts',(-1.49931070630541,0.0525329777524311,
5.59083150123597)) ;
#82616=CARTESIAN_POINT('Ctrl Pts',(-1.5,0.0262545598512842,5.59229141334158)) ;
#82617=CARTESIAN_POINT('Ctrl Pts',(-1.5,-1.89645643827552E-14,5.59374999999999)) ;
#82618=CARTESIAN_POINT('Origin',(0.,0.,0.)) ;
#82619=CARTESIAN_POINT('',(-1.5,4.24821278652342E-15,6.15624999999999)) ;
#82620=CARTESIAN_POINT('',(-1.5,-7.2389092309605E-15,6.09374999999999)) ;
#82621=CARTESIAN_POINT('',(-1.5,-1.83697019872103E-16,0.)) ;
#82622=CARTESIAN_POINT('Ctrl Pts',(-1.5,9.81688131253131E-15,6.15624999999999)) ;
#82623=CARTESIAN_POINT('Ctrl Pts',(-1.5,0.0938400860056215,6.15103666188857)) ;
#82624=CARTESIAN_POINT('Ctrl Pts',(-1.49119408246604,0.18769741776628,6.14582236567966)) ;
#82625=CARTESIAN_POINT('Ctrl Pts',(-1.43645284865028,0.475454866950807,
6.12983584072496)) ;
#82626=CARTESIAN_POINT('Ctrl Pts',(-1.36095535503423,0.661232582555009,
6.1200280899777)) ;
#82627=CARTESIAN_POINT('Ctrl Pts',(-1.14580339935446,0.986859460641902,
6.1006313956257)) ;
#82628=CARTESIAN_POINT('Ctrl Pts',(-1.01043659121357,1.12505731080659,6.09027972786117)) ;
#82629=CARTESIAN_POINT('Ctrl Pts',(-0.68888878141633,1.34725938427253,6.06863697183069)) ;
#82630=CARTESIAN_POINT('Ctrl Pts',(-0.504084036591963,1.42673943002813,
6.05753777035093)) ;
#82631=CARTESIAN_POINT('Ctrl Pts',(-0.120923480652032,1.50744063774349,
6.03686124929372)) ;
#82632=CARTESIAN_POINT('Ctrl Pts',(0.0731394438453323,1.51051288213524,
6.02802310137105)) ;
#82633=CARTESIAN_POINT('Ctrl Pts',(0.453451699063325,1.44290958093571,6.00784744998277)) ;
#82634=CARTESIAN_POINT('Ctrl Pts',(0.635984208094232,1.37226742224584,5.99710306836153)) ;
#82635=CARTESIAN_POINT('Ctrl Pts',(0.968198538908579,1.16281092222751,5.97530116280622)) ;
#82636=CARTESIAN_POINT('Ctrl Pts',(1.11366771024356,1.02435463556251,5.96445626607422)) ;
#82637=CARTESIAN_POINT('Ctrl Pts',(1.33699766836063,0.706055532219886,5.94486965669495)) ;
#82638=CARTESIAN_POINT('Ctrl Pts',(1.41557334053027,0.531266268116329,5.93576479267313)) ;
#82639=CARTESIAN_POINT('Ctrl Pts',(1.50474854535445,0.155580242132143,5.91489334678512)) ;
#82640=CARTESIAN_POINT('Ctrl Pts',(1.51217740036442,-0.0423044321232613,
5.90389975377093)) ;
#82641=CARTESIAN_POINT('Ctrl Pts',(1.44975514536609,-0.434115159917777,
5.88213249111568)) ;
#82642=CARTESIAN_POINT('Ctrl Pts',(1.37877799478145,-0.623840646366446,
5.87192424702647)) ;
#82643=CARTESIAN_POINT('Ctrl Pts',(1.17142571722235,-0.956205955623757,
5.8527156362194)) ;
#82644=CARTESIAN_POINT('Ctrl Pts',(1.04012680410663,-1.09757991078438,5.84247146000674)) ;
#82645=CARTESIAN_POINT('Ctrl Pts',(0.725560469845027,-1.32778690799201,
5.82094224138175)) ;
#82646=CARTESIAN_POINT('Ctrl Pts',(0.543539747779754,-1.41210078244945,
5.80984271323995)) ;
#82647=CARTESIAN_POINT('Ctrl Pts',(0.162309679028314,-1.50368453042566,
5.78895678000588)) ;
#82648=CARTESIAN_POINT('Ctrl Pts',(-0.0326899750580471,-1.51206457167333,
5.78001232983263)) ;
#82649=CARTESIAN_POINT('Ctrl Pts',(-0.415190720627786,-1.45431417734196,
5.76000507651066)) ;
#82650=CARTESIAN_POINT('Ctrl Pts',(-0.599048900134903,-1.38871839313835,
5.74933709060796)) ;
#82651=CARTESIAN_POINT('Ctrl Pts',(-0.936397357604732,-1.18857375385767,
5.72754683206703)) ;
#82652=CARTESIAN_POINT('Ctrl Pts',(-1.08557354820172,-1.05408538577059,
5.71663380124812)) ;
#82653=CARTESIAN_POINT('Ctrl Pts',(-1.31757646822544,-0.741728147345655,
5.69679496559784)) ;
#82654=CARTESIAN_POINT('Ctrl Pts',(-1.4009043199849,-0.568897104360946,
5.68785539468672)) ;
#82655=CARTESIAN_POINT('Ctrl Pts',(-1.48317308356884,-0.259166673181986,
5.67064814851011)) ;
#82656=CARTESIAN_POINT('Ctrl Pts',(-1.5,-0.12971522306197,5.66345640128121)) ;
#82657=CARTESIAN_POINT('Ctrl Pts',(-1.5,1.11022302462516E-15,5.65624999999999)) ;
#82658=CARTESIAN_POINT('Ctrl Pts',(-1.5,-1.87697080100691E-14,5.59374999999999)) ;
#82659=CARTESIAN_POINT('Ctrl Pts',(-1.5,-0.167469537432786,5.6030538631907)) ;
#82660=CARTESIAN_POINT('Ctrl Pts',(-1.47195184100008,-0.333968347888134,
5.61230379710489)) ;
#82661=CARTESIAN_POINT('Ctrl Pts',(-1.35382876989179,-0.6737723606495,5.63118179781386)) ;
#82662=CARTESIAN_POINT('Ctrl Pts',(-1.25664401481313,-0.841229768361045,
5.63999051354659)) ;
#82663=CARTESIAN_POINT('Ctrl Pts',(-0.999412713006369,-1.13620944885856,
5.66056044033892)) ;
#82664=CARTESIAN_POINT('Ctrl Pts',(-0.839622037268671,-1.25889663974064,
5.67165635033435)) ;
#82665=CARTESIAN_POINT('Ctrl Pts',(-0.488233431159106,-1.43124403379356,
5.69334997014089)) ;
#82666=CARTESIAN_POINT('Ctrl Pts',(-0.301275547724059,-1.48191920452157,
5.70375262913292)) ;
#82667=CARTESIAN_POINT('Ctrl Pts',(0.0873162328487167,-1.51044673774205,
5.72324119137115)) ;
#82668=CARTESIAN_POINT('Ctrl Pts',(0.285390240297882,-1.48581513460725,
5.73287486837702)) ;
#82669=CARTESIAN_POINT('Ctrl Pts',(0.659969730966546,-1.36134047243951,
5.75435446202922)) ;
#82670=CARTESIAN_POINT('Ctrl Pts',(0.832858396725634,-1.26299416389039,
5.76540441374301)) ;
#82671=CARTESIAN_POINT('Ctrl Pts',(1.12545908186054,-1.00967855059635,5.78651871558404)) ;
#82672=CARTESIAN_POINT('Ctrl Pts',(1.24414979380325,-0.859168050038595,
5.79601844166451)) ;
#82673=CARTESIAN_POINT('Ctrl Pts',(1.4231386145617,-0.514022370003128,5.81519320166649)) ;
#82674=CARTESIAN_POINT('Ctrl Pts',(1.47865917119759,-0.321069586856946,
5.82591280073016)) ;
#82675=CARTESIAN_POINT('Ctrl Pts',(1.51091126307826,0.071098839192046,5.84769993551066)) ;
#82676=CARTESIAN_POINT('Ctrl Pts',(1.48893860924911,0.266419057375733,5.85855105874309)) ;
#82677=CARTESIAN_POINT('Ctrl Pts',(1.37266513433757,0.634268127106245,5.87898711817257)) ;
#82678=CARTESIAN_POINT('Ctrl Pts',(1.28082105809126,0.803741777759219,5.88778596193725)) ;
#82679=CARTESIAN_POINT('Ctrl Pts',(1.03271198358855,1.10613951420092,5.90812305247334)) ;
#82680=CARTESIAN_POINT('Ctrl Pts',(0.87612409845522,1.2338682185265,5.91920491017406)) ;
#82681=CARTESIAN_POINT('Ctrl Pts',(0.528855580859981,1.41680906373381,5.9409945646616)) ;
#82682=CARTESIAN_POINT('Ctrl Pts',(0.342886244098983,1.47291663030694,5.95150056206419)) ;
#82683=CARTESIAN_POINT('Ctrl Pts',(-0.0435503507273721,1.51211432137883,
5.9711818261535)) ;
#82684=CARTESIAN_POINT('Ctrl Pts',(-0.240456802888681,1.49351229186924,
5.98049919743776)) ;
#82685=CARTESIAN_POINT('Ctrl Pts',(-0.617634247619035,1.38114985604414,
6.00176733448129)) ;
#82686=CARTESIAN_POINT('Ctrl Pts',(-0.794007068072516,1.28786509067901,
6.0128443192442)) ;
#82687=CARTESIAN_POINT('Ctrl Pts',(-1.09481650099445,1.04288543426395,6.03412201028953)) ;
#82688=CARTESIAN_POINT('Ctrl Pts',(-1.21814041222709,0.895723138282387,
6.04398760342875)) ;
#82689=CARTESIAN_POINT('Ctrl Pts',(-1.40734887121585,0.555786377324176,
6.06287297903754)) ;
#82690=CARTESIAN_POINT('Ctrl Pts',(-1.46852860805036,0.364591536553745,
6.0734949146359)) ;
#82691=CARTESIAN_POINT('Ctrl Pts',(-1.49689589468376,0.111493134674231,
6.08755593696254)) ;
#82692=CARTESIAN_POINT('Ctrl Pts',(-1.5,0.0557152328261553,6.09065470928742)) ;
#82693=CARTESIAN_POINT('Ctrl Pts',(-1.5,-9.37072593030258E-15,6.09374999999999)) ;
#82694=CARTESIAN_POINT('Origin',(0.,0.,0.)) ;
#82695=CARTESIAN_POINT('',(-1.5,5.23978324035715E-16,6.65624999999999)) ;
#82696=CARTESIAN_POINT('',(-1.5,-5.28734532048659E-15,6.59374999999999)) ;
#82697=CARTESIAN_POINT('',(-1.5,-1.83697019872103E-16,0.)) ;
#82698=CARTESIAN_POINT('Ctrl Pts',(-1.5,-4.5102810375397E-16,6.65624999999999)) ;
#82699=CARTESIAN_POINT('Ctrl Pts',(-1.5,0.124981814104662,6.64930656588306)) ;
#82700=CARTESIAN_POINT('Ctrl Pts',(-1.48437885790166,0.249763345316788,
6.64237425859351)) ;
#82701=CARTESIAN_POINT('Ctrl Pts',(-1.40497923519992,0.560453320344288,
6.62511370442532)) ;
#82702=CARTESIAN_POINT('Ctrl Pts',(-1.32025838181587,0.738229996303097,
6.61593123889224)) ;
#82703=CARTESIAN_POINT('Ctrl Pts',(-1.08887343464721,1.04953098763693,6.59615147567178)) ;
#82704=CARTESIAN_POINT('Ctrl Pts',(-0.94513821388451,1.18061729652795,6.58559472528041)) ;
#82705=CARTESIAN_POINT('Ctrl Pts',(-0.609454725731597,1.385176787341,6.56376193784831)) ;
#82706=CARTESIAN_POINT('Ctrl Pts',(-0.419159520584368,1.45412205074647,
6.55269120931616)) ;
#82707=CARTESIAN_POINT('Ctrl Pts',(-0.0323006526586065,1.51172991041425,
6.53247823503077)) ;
#82708=CARTESIAN_POINT('Ctrl Pts',(0.159932450966637,1.50359436742395,6.52365508990474)) ;
#82709=CARTESIAN_POINT('Ctrl Pts',(0.535293751442473,1.41474059569989,6.50312735058965)) ;
#82710=CARTESIAN_POINT('Ctrl Pts',(0.714483288689404,1.33324259147996,6.49224225650864)) ;
#82711=CARTESIAN_POINT('Ctrl Pts',(1.03468086348225,1.10405900253399,6.47047053270454)) ;
#82712=CARTESIAN_POINT('Ctrl Pts',(1.17174544516121,0.957365362404684,6.45980118660689)) ;
#82713=CARTESIAN_POINT('Ctrl Pts',(1.37609716509034,0.626482797821238,6.44077812754815)) ;
#82714=CARTESIAN_POINT('Ctrl Pts',(1.44435403624083,0.447218209615709,6.43109545608976)) ;
#82715=CARTESIAN_POINT('Ctrl Pts',(1.51149825482502,0.0656056189570403,
6.40989475660872)) ;
#82716=CARTESIAN_POINT('Ctrl Pts',(1.50701414843509,-0.133571729305174,
6.39882934837193)) ;
#82717=CARTESIAN_POINT('Ctrl Pts',(1.42132330124281,-0.518225845657976,
6.37745967524123)) ;
#82718=CARTESIAN_POINT('Ctrl Pts',(1.34117892727577,-0.699958049992881,
6.36800088872471)) ;
#82719=CARTESIAN_POINT('Ctrl Pts',(1.11789709948255,-1.0184613443221,6.34841092304488)) ;
#82720=CARTESIAN_POINT('Ctrl Pts',(0.978319502241427,-1.15318222579219,
6.33795324605904)) ;
#82721=CARTESIAN_POINT('Ctrl Pts',(0.649619225769072,-1.36671320489274,
6.31620723054758)) ;
#82722=CARTESIAN_POINT('Ctrl Pts',(0.462010248026866,-1.44099612190541,
6.30511747503596)) ;
#82723=CARTESIAN_POINT('Ctrl Pts',(0.0769441254254464,-1.51020675207094,
6.28466845506971)) ;
#82724=CARTESIAN_POINT('Ctrl Pts',(-0.116180026277667,-1.50769626983412,
6.27587407115268)) ;
#82725=CARTESIAN_POINT('Ctrl Pts',(-0.494082706878714,-1.42957943689278,
6.25552230792883)) ;
#82726=CARTESIAN_POINT('Ctrl Pts',(-0.675043776732769,-1.35355845111559,
6.2447041203467)) ;
#82727=CARTESIAN_POINT('Ctrl Pts',(-1.0014718743312,-1.13427482675704,6.22290762939067)) ;
#82728=CARTESIAN_POINT('Ctrl Pts',(-1.14285079494042,-0.991685518632995,
6.21214471878683)) ;
#82729=CARTESIAN_POINT('Ctrl Pts',(-1.35683680668118,-0.667122033599381,
6.19283365963467)) ;
#82730=CARTESIAN_POINT('Ctrl Pts',(-1.43032222715605,-0.490163771142688,
6.18348132061904)) ;
#82731=CARTESIAN_POINT('Ctrl Pts',(-1.48960830908396,-0.203858299136244,
6.16757546106313)) ;
#82732=CARTESIAN_POINT('Ctrl Pts',(-1.5,-0.101939325142457,6.16191329584124)) ;
#82733=CARTESIAN_POINT('Ctrl Pts',(-1.5,1.17787724018825E-14,6.15624999999999)) ;
#82734=CARTESIAN_POINT('Ctrl Pts',(-1.5,-9.92261828258734E-15,6.09374999999999)) ;
#82735=CARTESIAN_POINT('Ctrl Pts',(-1.5,-0.138795933253646,6.10146088518074)) ;
#82736=CARTESIAN_POINT('Ctrl Pts',(-1.48073442875306,-0.277202948098713,
6.10915016378326)) ;
#82737=CARTESIAN_POINT('Ctrl Pts',(-1.39032217281161,-0.59437475913241,
6.12677081995179)) ;
#82738=CARTESIAN_POINT('Ctrl Pts',(-1.30371818610947,-0.765891971535818,
6.13563293984562)) ;
#82739=CARTESIAN_POINT('Ctrl Pts',(-1.06468844715775,-1.0755083150188,6.15573371750861)) ;
#82740=CARTESIAN_POINT('Ctrl Pts',(-0.911411885737207,-1.2081353020028,
6.1667923224801)) ;
#82741=CARTESIAN_POINT('Ctrl Pts',(-0.56851446104285,-1.40143879973568,
6.18865952412143)) ;
#82742=CARTESIAN_POINT('Ctrl Pts',(-0.383673635175328,-1.46289104837478,
6.19925968940906)) ;
#82743=CARTESIAN_POINT('Ctrl Pts',(0.000573644848951456,-1.51254780663004,
6.21912614968483)) ;
#82744=CARTESIAN_POINT('Ctrl Pts',(0.196383733168085,-1.49974703911056,
6.22820554345879)) ;
#82745=CARTESIAN_POINT('Ctrl Pts',(0.57591537113953,-1.39914381604468,6.24926030187857)) ;
#82746=CARTESIAN_POINT('Ctrl Pts',(0.755536941194608,-1.31089279521363,
6.26035376594251)) ;
#82747=CARTESIAN_POINT('Ctrl Pts',(1.06417064803916,-1.0742108545428,6.28177741043845)) ;
#82748=CARTESIAN_POINT('Ctrl Pts',(1.19204295342378,-0.930293304306606,
6.29192737932854)) ;
#82749=CARTESIAN_POINT('Ctrl Pts',(1.39103649701779,-0.595407548986935,
6.31080384275084)) ;
#82750=CARTESIAN_POINT('Ctrl Pts',(1.45763241901129,-0.406022035808256,
6.32119322023287)) ;
#82751=CARTESIAN_POINT('Ctrl Pts',(1.51264770441934,-0.0152206621079717,
6.34290440766066)) ;
#82752=CARTESIAN_POINT('Ctrl Pts',(1.50171959659393,0.182147600367653,6.35386931113153)) ;
#82753=CARTESIAN_POINT('Ctrl Pts',(1.4060553413921,0.556010522676409,6.37463947348201)) ;
#82754=CARTESIAN_POINT('Ctrl Pts',(1.3243658414026,0.729509542578257,6.38362890604055)) ;
#82755=CARTESIAN_POINT('Ctrl Pts',(1.09534643232919,1.0439251098773,6.40338137325538)) ;
#82756=CARTESIAN_POINT('Ctrl Pts',(0.947435360849062,1.17979259578049,6.41427184483062)) ;
#82757=CARTESIAN_POINT('Ctrl Pts',(0.611826754406933,1.38316072366324,6.43606793610001)) ;
#82758=CARTESIAN_POINT('Ctrl Pts',(0.428409966272987,1.45049801396441,6.44676306071974)) ;
#82759=CARTESIAN_POINT('Ctrl Pts',(0.046656659607905,1.51164850997432,6.4668288001395)) ;
#82760=CARTESIAN_POINT('Ctrl Pts',(-0.148013323645245,1.50510892206033,
6.47572937985251)) ;
#82761=CARTESIAN_POINT('Ctrl Pts',(-0.529926193154905,1.4172928056006,6.49654350792237)) ;
#82762=CARTESIAN_POINT('Ctrl Pts',(-0.712924645156483,1.3346423648461,6.50764387062591)) ;
#82763=CARTESIAN_POINT('Ctrl Pts',(-1.02993030182321,1.10718331722484,6.52921411927188)) ;
#82764=CARTESIAN_POINT('Ctrl Pts',(-1.16264602587055,0.966895855390792,
6.53949628146208)) ;
#82765=CARTESIAN_POINT('Ctrl Pts',(-1.37270991425259,0.636862577898985,
6.55877057604555)) ;
#82766=CARTESIAN_POINT('Ctrl Pts',(-1.44526608981773,0.448516541760216,
6.56883241434665)) ;
#82767=CARTESIAN_POINT('Ctrl Pts',(-1.4929329537697,0.168179439750475,6.58440669779164)) ;
#82768=CARTESIAN_POINT('Ctrl Pts',(-1.5,0.0840663850849933,6.58907964527304)) ;
#82769=CARTESIAN_POINT('Ctrl Pts',(-1.5,2.97483362866747E-16,6.59374999999999)) ;
#82770=CARTESIAN_POINT('Origin',(0.,0.,0.)) ;
#82771=CARTESIAN_POINT('',(-1.5,-1.70514134259448E-15,7.15624999999999)) ;
#82772=CARTESIAN_POINT('',(-1.5,1.38700325333418E-15,7.09374999999999)) ;
#82773=CARTESIAN_POINT('',(-1.5,-1.83697019872103E-16,0.)) ;
#82774=CARTESIAN_POINT('Ctrl Pts',(-1.5,-7.11236625150491E-15,7.15624999999999)) ;
#82775=CARTESIAN_POINT('Ctrl Pts',(-1.5,0.155970879159808,7.14758495115777)) ;
#82776=CARTESIAN_POINT('Ctrl Pts',(-1.47567100304807,0.311268816362477,
7.13895728797986)) ;
#82777=CARTESIAN_POINT('Ctrl Pts',(-1.36859153902948,0.643438650998488,
7.12050340827786)) ;
#82778=CARTESIAN_POINT('Ctrl Pts',(-1.27483150901209,0.81354728074605,7.11165349066535)) ;
#82779=CARTESIAN_POINT('Ctrl Pts',(-1.02723184549473,1.11012268705131,7.0915026405694)) ;
#82780=CARTESIAN_POINT('Ctrl Pts',(-0.875333730341766,1.23343240344003,
7.08076916919696)) ;
#82781=CARTESIAN_POINT('Ctrl Pts',(-0.52863446093955,1.41777460586891,7.05896797608639)) ;
#82782=CARTESIAN_POINT('Ctrl Pts',(-0.336219533923613,1.47530195769444,
7.04811242659884)) ;
#82783=CARTESIAN_POINT('Ctrl Pts',(0.0509867626765902,1.51112099286464,
7.02848798176849)) ;
#82784=CARTESIAN_POINT('Ctrl Pts',(0.241744219449288,1.49253459485981,7.01941170345382)) ;
#82785=CARTESIAN_POINT('Ctrl Pts',(0.612067889516041,1.38340728828563,6.99856318349895)) ;
#82786=CARTESIAN_POINT('Ctrl Pts',(0.78745746631049,1.29164622821851,6.98757583021581)) ;
#82787=CARTESIAN_POINT('Ctrl Pts',(1.09675715651085,1.04282559728137,6.96578295773999)) ;
#82788=CARTESIAN_POINT('Ctrl Pts',(1.22636394567284,0.886764146108135,6.95551467478378)) ;
#82789=CARTESIAN_POINT('Ctrl Pts',(1.41185802272716,0.541478724633405,6.93633215136852)) ;
#82790=CARTESIAN_POINT('Ctrl Pts',(1.46929070030764,0.357357376336164,6.92610318757423)) ;
#82791=CARTESIAN_POINT('Ctrl Pts',(1.51279019148619,-0.0298681335906356,
6.90459065924496)) ;
#82792=CARTESIAN_POINT('Ctrl Pts',(1.49555855397567,-0.229648748802826,
6.89349173617762)) ;
#82793=CARTESIAN_POINT('Ctrl Pts',(1.38568178600204,-0.606101868472665,
6.87257767397374)) ;
#82794=CARTESIAN_POINT('Ctrl Pts',(1.29600326945513,-0.779644091130765,
6.86361387273169)) ;
#82795=CARTESIAN_POINT('Ctrl Pts',(1.05575279960783,-1.08294642667726,6.84362975173546)) ;
#82796=CARTESIAN_POINT('Ctrl Pts',(0.907525210975976,-1.20986361353978,
6.83297267113945)) ;
#82797=CARTESIAN_POINT('Ctrl Pts',(0.566284158502573,-1.40316465850384,
6.81118522987622)) ;
#82798=CARTESIAN_POINT('Ctrl Pts',(0.375451337987938,-1.46581143000135,
6.8002635934212)) ;
#82799=CARTESIAN_POINT('Ctrl Pts',(-0.0109415681523102,-1.51197434190153,
6.78039095294844)) ;
#82800=CARTESIAN_POINT('Ctrl Pts',(-0.202378019607965,-1.49841150830115,
6.77146895822236)) ;
#82801=CARTESIAN_POINT('Ctrl Pts',(-0.575174916429631,-1.39907699561318,
6.75077346714216)) ;
#82802=CARTESIAN_POINT('Ctrl Pts',(-0.752473738342542,-1.31225762170762,
6.73983152432047)) ;
#82803=CARTESIAN_POINT('Ctrl Pts',(-1.06628383312216,-1.07356112140703,
6.71810287075417)) ;
#82804=CARTESIAN_POINT('Ctrl Pts',(-1.19900989580016,-0.922982733540992,
6.70753435208992)) ;
#82805=CARTESIAN_POINT('Ctrl Pts',(-1.3938697751391,-0.586005200031803,
6.68879866473212)) ;
#82806=CARTESIAN_POINT('Ctrl Pts',(-1.45698248258737,-0.404394641375286,
6.67871636896529)) ;
#82807=CARTESIAN_POINT('Ctrl Pts',(-1.49480995094287,-0.14415235976927,
6.66425846443162)) ;
#82808=CARTESIAN_POINT('Ctrl Pts',(-1.5,-0.0720429060650724,6.66025238367027)) ;
#82809=CARTESIAN_POINT('Ctrl Pts',(-1.5,0.,6.65624999999999)) ;
#82810=CARTESIAN_POINT('Ctrl Pts',(-1.5,-1.21430643318376E-15,6.59374999999999)) ;
#82811=CARTESIAN_POINT('Ctrl Pts',(-1.5,-0.111361082712955,6.59993672681737)) ;
#82812=CARTESIAN_POINT('Ctrl Pts',(-1.48759844499926,-0.222640270679804,
6.60611890392665)) ;
#82813=CARTESIAN_POINT('Ctrl Pts',(-1.42084385215368,-0.516992673569965,
6.62247181519833)) ;
#82814=CARTESIAN_POINT('Ctrl Pts',(-1.34404671761395,-0.692531276762383,
6.6316548353919)) ;
#82815=CARTESIAN_POINT('Ctrl Pts',(-1.12397619152421,-1.01303129154334,
6.65114576170348)) ;
#82816=CARTESIAN_POINT('Ctrl Pts',(-0.97992280872646,-1.15294615050247,
6.66196305717479)) ;
#82817=CARTESIAN_POINT('Ctrl Pts',(-0.649697411365527,-1.36585525071345,
6.68376517568562)) ;
#82818=CARTESIAN_POINT('Ctrl Pts',(-0.467696385807258,-1.4383808020701,
6.69453630275932)) ;
#82819=CARTESIAN_POINT('Ctrl Pts',(-0.0882190491870855,-1.509663036695,
6.71477397670299)) ;
#82820=CARTESIAN_POINT('Ctrl Pts',(0.105509085441113,-1.5085533975611,6.72358871386342)) ;
#82821=CARTESIAN_POINT('Ctrl Pts',(0.489353528451194,-1.43188764015323,
6.74418604261076)) ;
#82822=CARTESIAN_POINT('Ctrl Pts',(0.67515914264358,-1.35422220285163,6.75528299265005)) ;
#82823=CARTESIAN_POINT('Ctrl Pts',(0.999244984673385,-1.13504027758486,
6.77696396680771)) ;
#82824=CARTESIAN_POINT('Ctrl Pts',(1.13610075771986,-0.998049285255926,
6.78735374860089)) ;
#82825=CARTESIAN_POINT('Ctrl Pts',(1.35411996744601,-0.674923104365787,
6.8068189299665)) ;
#82826=CARTESIAN_POINT('Ctrl Pts',(1.43126335112967,-0.490580595220442,
6.81649552248775)) ;
#82827=CARTESIAN_POINT('Ctrl Pts',(1.5093267236132,-0.103499418996943,6.83800003227795)) ;
#82828=CARTESIAN_POINT('Ctrl Pts',(1.50986472630013,0.0953286944885322,
6.84904603858269)) ;
#82829=CARTESIAN_POINT('Ctrl Pts',(1.43542715550702,0.47502528955843,6.87014029386435)) ;
#82830=CARTESIAN_POINT('Ctrl Pts',(1.36379416565911,0.65279156298978,6.87960085491672)) ;
#82831=CARTESIAN_POINT('Ctrl Pts',(1.15321846841009,0.97960764740451,6.89881040744143)) ;
#82832=CARTESIAN_POINT('Ctrl Pts',(1.01335589122013,1.1236681895384,6.90954123054988)) ;
#82833=CARTESIAN_POINT('Ctrl Pts',(0.68910323787394,1.34648368114626,6.93133116281912)) ;
#82834=CARTESIAN_POINT('Ctrl Pts',(0.508751931396615,1.42445173175803,6.9421740982814)) ;
#82835=CARTESIAN_POINT('Ctrl Pts',(0.131741837294639,1.50638091622421,6.96258881557077)) ;
#82836=CARTESIAN_POINT('Ctrl Pts',(-0.0610573145705921,1.51089691893831,
6.97138492922422)) ;
#82837=CARTESIAN_POINT('Ctrl Pts',(-0.446777479089504,1.44582129502042,
6.99175055551223)) ;
#82838=CARTESIAN_POINT('Ctrl Pts',(-0.63536076460844,1.37343070700381,7.00283462273427)) ;
#82839=CARTESIAN_POINT('Ctrl Pts',(-0.966577871508148,1.16307287847368,
7.02461358623473)) ;
#82840=CARTESIAN_POINT('Ctrl Pts',(-1.10764838590662,1.02963334093072,7.03510749834392)) ;
#82841=CARTESIAN_POINT('Ctrl Pts',(-1.33383010390516,0.713695777908442,
7.05476571474223)) ;
#82842=CARTESIAN_POINT('Ctrl Pts',(-1.41561801260082,0.533388227676851,
7.06411732068462)) ;
#82843=CARTESIAN_POINT('Ctrl Pts',(-1.48677251611317,0.22991157572445,7.08097713468198)) ;
#82844=CARTESIAN_POINT('Ctrl Pts',(-1.5,0.115009252399373,7.08736059708891)) ;
#82845=CARTESIAN_POINT('Ctrl Pts',(-1.5,1.13450915328883E-14,7.09374999999999)) ;
#82846=CARTESIAN_POINT('Origin',(0.,0.,0.)) ;
#82847=CARTESIAN_POINT('',(-1.5,-2.17351668110822E-15,7.65624999999999)) ;
#82848=CARTESIAN_POINT('',(-1.5,2.87452863398429E-15,7.59374999999998)) ;
#82849=CARTESIAN_POINT('',(-1.5,-1.83697019872103E-16,0.)) ;
#82850=CARTESIAN_POINT('Ctrl Pts',(-1.5,-7.63278329429795E-15,7.65624999999999)) ;
#82851=CARTESIAN_POINT('Ctrl Pts',(-1.5,0.1861458861506,7.64590856188051)) ;
#82852=CARTESIAN_POINT('Ctrl Pts',(-1.4653476410335,0.370821775569803,7.63564879024612)) ;
#82853=CARTESIAN_POINT('Ctrl Pts',(-1.32841052256855,0.722308822181751,
7.61612173210102)) ;
#82854=CARTESIAN_POINT('Ctrl Pts',(-1.22588013089401,0.885226385993034,
7.60730723013069)) ;
#82855=CARTESIAN_POINT('Ctrl Pts',(-0.962395644933833,1.16695931533222,
7.58680441218545)) ;
#82856=CARTESIAN_POINT('Ctrl Pts',(-0.802767042430613,1.28201247368992,
7.57592835640116)) ;
#82857=CARTESIAN_POINT('Ctrl Pts',(-0.444952562952282,1.44621235819178,
7.55415189132776)) ;
#82858=CARTESIAN_POINT('Ctrl Pts',(-0.249569090721813,1.4923983972716,7.54346855410715)) ;
#82859=CARTESIAN_POINT('Ctrl Pts',(0.139072625428861,1.50557896499573,7.52440389393943)) ;
#82860=CARTESIAN_POINT('Ctrl Pts',(0.328533048250181,1.47587651637286,7.51477334957883)) ;
#82861=CARTESIAN_POINT('Ctrl Pts',(0.693038358340403,1.3448401171827,7.49359617969286)) ;
#82862=CARTESIAN_POINT('Ctrl Pts',(0.863667549151541,1.24216627735557,7.48253472781602)) ;
#82863=CARTESIAN_POINT('Ctrl Pts',(1.15526329027305,0.976824102726417,7.46113470521818)) ;
#82864=CARTESIAN_POINT('Ctrl Pts',(1.27341103702043,0.81683896816719,7.45162994267596)) ;
#82865=CARTESIAN_POINT('Ctrl Pts',(1.43908475574544,0.464718579020663,7.43206769883448)) ;
#82866=CARTESIAN_POINT('Ctrl Pts',(1.48671418225868,0.276748660010704,7.42162492555615)) ;
#82867=CARTESIAN_POINT('Ctrl Pts',(1.50890089335789,-0.114429023727044,
7.39989283201516)) ;
#82868=CARTESIAN_POINT('Ctrl Pts',(1.48028463544928,-0.314079750787138,
7.38880112495627)) ;
#82869=CARTESIAN_POINT('Ctrl Pts',(1.34926843422165,-0.682763372048332,
7.36831870155287)) ;
#82870=CARTESIAN_POINT('Ctrl Pts',(1.25116644086583,-0.849278719452466,
7.35952236457923)) ;
#82871=CARTESIAN_POINT('Ctrl Pts',(0.995713855764172,-1.13856859594314,
7.33919606644558)) ;
#82872=CARTESIAN_POINT('Ctrl Pts',(0.839956299406488,-1.25787404469203,
7.32838813727827)) ;
#82873=CARTESIAN_POINT('Ctrl Pts',(0.487639817921922,-1.43238773447714,
7.30658970016548)) ;
#82874=CARTESIAN_POINT('Ctrl Pts',(0.293678011497376,-1.48435269459901,
7.29581423728834)) ;
#82875=CARTESIAN_POINT('Ctrl Pts',(-0.0942923383214878,-1.50902769141779,
7.27646258855124)) ;
#82876=CARTESIAN_POINT('Ctrl Pts',(-0.284378782084336,-1.48499391784799,
7.26715098385231)) ;
#82877=CARTESIAN_POINT('Ctrl Pts',(-0.651911110962182,-1.36516501901101,
7.24613949591127)) ;
#82878=CARTESIAN_POINT('Ctrl Pts',(-0.825058919774653,-1.26804586784891,
7.23511116387671)) ;
#82879=CARTESIAN_POINT('Ctrl Pts',(-1.12574676982119,-1.01106851517849,
7.21350605314977)) ;
#82880=CARTESIAN_POINT('Ctrl Pts',(-1.24971616502101,-0.853080854350677,
7.20364338079726)) ;
#82881=CARTESIAN_POINT('Ctrl Pts',(-1.42557846088632,-0.504435403451394,
7.18427418908063)) ;
#82882=CARTESIAN_POINT('Ctrl Pts',(-1.47828940988115,-0.318383776178807,
7.17393798756549)) ;
#82883=CARTESIAN_POINT('Ctrl Pts',(-1.49819523775879,-0.0850159091993737,
7.16097310606663)) ;
#82884=CARTESIAN_POINT('Ctrl Pts',(-1.5,-0.0424829919454561,7.15861016621918)) ;
#82885=CARTESIAN_POINT('Ctrl Pts',(-1.5,-9.66814085323954E-15,7.15624999999999)) ;
#82886=CARTESIAN_POINT('Ctrl Pts',(-1.5,1.00028780763944E-14,7.09374999999999)) ;
#82887=CARTESIAN_POINT('Ctrl Pts',(-1.5,-0.0815960447684402,7.09828311359823)) ;
#82888=CARTESIAN_POINT('Ctrl Pts',(-1.49334221031576,-0.163245912606358,
7.10281921736702)) ;
#82889=CARTESIAN_POINT('Ctrl Pts',(-1.44902861703293,-0.431890594248862,
7.11774392190272)) ;
#82890=CARTESIAN_POINT('Ctrl Pts',(-1.382619826531,-0.611989318737896,7.12756170921206)) ;
#82891=CARTESIAN_POINT('Ctrl Pts',(-1.18167785850058,-0.945075901262501,
7.14648193922668)) ;
#82892=CARTESIAN_POINT('Ctrl Pts',(-1.0461622008619,-1.09318335400795,7.15711603525437)) ;
#82893=CARTESIAN_POINT('Ctrl Pts',(-0.728231481697741,-1.32581226318711,
7.17887439825599)) ;
#82894=CARTESIAN_POINT('Ctrl Pts',(-0.5497048048325,-1.4092307172552,7.18978094628113)) ;
#82895=CARTESIAN_POINT('Ctrl Pts',(-0.175257719464432,-1.50186036307312,
7.21036958579283)) ;
#82896=CARTESIAN_POINT('Ctrl Pts',(0.0166800168265415,-1.51195786524259,
7.21922035476033)) ;
#82897=CARTESIAN_POINT('Ctrl Pts',(0.404133880099292,-1.45839867267581,
7.23934949279767)) ;
#82898=CARTESIAN_POINT('Ctrl Pts',(0.595331248838867,-1.39133561973484,
7.25041134307188)) ;
#82899=CARTESIAN_POINT('Ctrl Pts',(0.93339288951111,-1.18995502000163,7.27227024689042)) ;
#82900=CARTESIAN_POINT('Ctrl Pts',(1.07855535558916,-1.0601651251158,7.2828596541539)) ;
#82901=CARTESIAN_POINT('Ctrl Pts',(1.31274322598517,-0.751379456456309,
7.30270440300672)) ;
#82902=CARTESIAN_POINT('Ctrl Pts',(1.39903638673437,-0.574952294707854,
7.31180820584957)) ;
#82903=CARTESIAN_POINT('Ctrl Pts',(1.50034365131131,-0.195507154400685,
7.33288849142218)) ;
#82904=CARTESIAN_POINT('Ctrl Pts',(1.51302058012752,0.00414932182816016,
7.34398051787934)) ;
#82905=CARTESIAN_POINT('Ctrl Pts',(1.46105430473585,0.389466756601615,7.36538704203342)) ;
#82906=CARTESIAN_POINT('Ctrl Pts',(1.39975717137317,0.571898589845439,7.3755221438803)) ;
#82907=CARTESIAN_POINT('Ctrl Pts',(1.20814359709347,0.910975961757015,7.39435977565317)) ;
#82908=CARTESIAN_POINT('Ctrl Pts',(1.07693060012791,1.06290383237179,7.40479459213124)) ;
#82909=CARTESIAN_POINT('Ctrl Pts',(0.76524656804414,1.30487847604685,7.42651201499658)) ;
#82910=CARTESIAN_POINT('Ctrl Pts',(0.588625691888289,1.39349738551153,7.43747132723668)) ;
#82911=CARTESIAN_POINT('Ctrl Pts',(0.21671876678619,1.49639045746761,7.45822284840112)) ;
#82912=CARTESIAN_POINT('Ctrl Pts',(0.0255363238703203,1.51178362234739,
7.46719406020196)) ;
#82913=CARTESIAN_POINT('Ctrl Pts',(-0.361165341329922,1.46939576911905,
7.48697669311104)) ;
#82914=CARTESIAN_POINT('Ctrl Pts',(-0.552591732084792,1.40861203393721,
7.49787513671878)) ;
#82915=CARTESIAN_POINT('Ctrl Pts',(-0.895851526154825,1.21856151679165,
7.51966941229296)) ;
#82916=CARTESIAN_POINT('Ctrl Pts',(-1.04542819758655,1.0929484300856,7.5303551756611)) ;
#82917=CARTESIAN_POINT('Ctrl Pts',(-1.28836769275067,0.792097162750906,
7.5504005872201)) ;
#82918=CARTESIAN_POINT('Ctrl Pts',(-1.37954201897998,0.619819417571374,
7.5593155879127)) ;
#82919=CARTESIAN_POINT('Ctrl Pts',(-1.47836564920042,0.293655230972509,
7.57743582050153)) ;
#82920=CARTESIAN_POINT('Ctrl Pts',(-1.5,0.147080497195422,7.5855788612669)) ;
#82921=CARTESIAN_POINT('Ctrl Pts',(-1.5,1.02348685082632E-14,7.59374999999998)) ;
#82922=CARTESIAN_POINT('Origin',(0.,0.,0.)) ;
#82923=CARTESIAN_POINT('',(-1.17524047358084,1.05150989506409E-10,0.406249999985091)) ;
#82924=CARTESIAN_POINT('',(-1.17524047358084,2.87273037626067E-15,0.343750000000002)) ;
#82925=CARTESIAN_POINT('',(-1.17524047358084,-1.4392544841992E-16,0.)) ;
#82926=CARTESIAN_POINT('',(-0.45578786625158,-1.08325786021627,0.)) ;
#82927=CARTESIAN_POINT('Ctrl Pts',(-1.17524047358084,2.10302814174179E-10,
0.406249999985091)) ;
#82928=CARTESIAN_POINT('Ctrl Pts',(-1.17524047358083,3.33428712385673E-5,
0.406247635741228)) ;
#82929=CARTESIAN_POINT('Ctrl Pts',(-1.17524047216194,6.66856023358135E-5,
0.406245271492423)) ;
#82930=CARTESIAN_POINT('Ctrl Pts',(-1.17522757665485,0.151576869489721,
0.395502067066514)) ;
#82931=CARTESIAN_POINT('Ctrl Pts',(-1.145929008722,0.301658245186112,0.38486017582027)) ;
#82932=CARTESIAN_POINT('Ctrl Pts',(-1.03172938875857,0.582968732539079,
0.364913159750174)) ;
#82933=CARTESIAN_POINT('Ctrl Pts',(-0.947742468184635,0.711412293797784,
0.355893102642213)) ;
#82934=CARTESIAN_POINT('Ctrl Pts',(-0.732986343659152,0.931732084592661,
0.334894268679289)) ;
#82935=CARTESIAN_POINT('Ctrl Pts',(-0.603354347417427,1.0204657587481,0.323787928991981)) ;
#82936=CARTESIAN_POINT('Ctrl Pts',(-0.322468561346593,1.14000796889925,
0.302301168183816)) ;
#82937=CARTESIAN_POINT('Ctrl Pts',(-0.174733803845013,1.17179163907959,
0.292102270501326)) ;
#82938=CARTESIAN_POINT('Ctrl Pts',(0.130808108867636,1.17828656423486,0.273109383022199)) ;
#82939=CARTESIAN_POINT('Ctrl Pts',(0.285781753044923,1.15058516116786,0.262826684366474)) ;
#82940=CARTESIAN_POINT('Ctrl Pts',(0.573856810241372,1.03705912960264,0.241111743155458)) ;
#82941=CARTESIAN_POINT('Ctrl Pts',(0.704399560267853,0.953220128037648,
0.230123010631557)) ;
#82942=CARTESIAN_POINT('Ctrl Pts',(0.922471833417844,0.743267926701739,
0.209288109485642)) ;
#82943=CARTESIAN_POINT('Ctrl Pts',(1.00916274464,0.620467650978295,0.200245793834457)) ;
#82944=CARTESIAN_POINT('Ctrl Pts',(1.13495314535437,0.342640116918902,0.180545745184494)) ;
#82945=CARTESIAN_POINT('Ctrl Pts',(1.17034734576148,0.18917786967726,0.16966412487703)) ;
#82946=CARTESIAN_POINT('Ctrl Pts',(1.17907453998758,-0.118511772839143,
0.147846629547835)) ;
#82947=CARTESIAN_POINT('Ctrl Pts',(1.15390583968203,-0.269771473464922,
0.137121186257288)) ;
#82948=CARTESIAN_POINT('Ctrl Pts',(1.04763953904311,-0.553611342601334,
0.116994818114125)) ;
#82949=CARTESIAN_POINT('Ctrl Pts',(0.967863217709318,-0.683576658879517,
0.108115548345547)) ;
#82950=CARTESIAN_POINT('Ctrl Pts',(0.760092353676459,-0.909832915906859,
0.0873351930678865)) ;
#82951=CARTESIAN_POINT('Ctrl Pts',(0.632728327525695,-1.00258751053419,
0.0762255674912086)) ;
#82952=CARTESIAN_POINT('Ctrl Pts',(0.354593874883976,-1.13048305812118,
0.0546116026402439)) ;
#82953=CARTESIAN_POINT('Ctrl Pts',(0.20739856690986,-1.16650602409258,0.0442955324203148)) ;
#82954=CARTESIAN_POINT('Ctrl Pts',(-0.0285609865855068,-1.1780396392425,
0.0293968953689426)) ;
#82955=CARTESIAN_POINT('Ctrl Pts',(-0.114694549034007,-1.17279463536867,
0.0241201604405704)) ;
#82956=CARTESIAN_POINT('Ctrl Pts',(-0.287536914348188,-1.14301640971954,
0.0124505634703877)) ;
#82957=CARTESIAN_POINT('Ctrl Pts',(-0.373501658918062,-1.11788032291883,
0.00628050026599479)) ;
#82958=CARTESIAN_POINT('Ctrl Pts',(-0.455787866252675,-1.08325786021582,
-8.27188350007229E-14)) ;
#82959=CARTESIAN_POINT('',(0.455787866251495,-1.08325786021631,0.)) ;
#82960=CARTESIAN_POINT('Origin',(0.,0.,1.91347191551875E-17)) ;
#82961=CARTESIAN_POINT('',(0.,1.17524047358084,0.218750000000004)) ;
#82962=CARTESIAN_POINT('Ctrl Pts',(0.455787866251497,-1.08325786021631,
8.88950230295211E-16)) ;
#82963=CARTESIAN_POINT('Ctrl Pts',(0.555456626337732,-1.04132157416659,
0.00760722476484358)) ;
#82964=CARTESIAN_POINT('Ctrl Pts',(0.648808587897722,-0.985853182093984,
0.0153063133539367)) ;
#82965=CARTESIAN_POINT('Ctrl Pts',(0.73322905633996,-0.918458121899505,
0.0228797846822488)) ;
#82966=CARTESIAN_POINT('Ctrl Pts',(0.742719106373334,-0.910881967620221,
0.0237311495604381)) ;
#82967=CARTESIAN_POINT('Ctrl Pts',(0.752096210069285,-0.903155153397013,
0.0245809201248136)) ;
#82968=CARTESIAN_POINT('Ctrl Pts',(0.761356502140137,-0.895280094380157,
0.0254287733909492)) ;
#82969=CARTESIAN_POINT('Ctrl Pts',(0.807820971065409,-0.855766174929913,
0.0296829644505966)) ;
#82970=CARTESIAN_POINT('Ctrl Pts',(0.851070642967234,-0.812754819245497,
0.0338637394877002)) ;
#82971=CARTESIAN_POINT('Ctrl Pts',(0.89075805595094,-0.766642195879478,
0.0379357160198994)) ;
#82972=CARTESIAN_POINT('Ctrl Pts',(0.916698449836841,-0.736502171037903,
0.0405972317801421)) ;
#82973=CARTESIAN_POINT('Ctrl Pts',(0.941116361855842,-0.705036795841439,
0.0432122440934423)) ;
#82974=CARTESIAN_POINT('Ctrl Pts',(0.963905565511381,-0.672366143942861,
0.045769972778043)) ;
#82975=CARTESIAN_POINT('Ctrl Pts',(0.970921870664855,-0.662307553623158,
0.0465574423720755)) ;
#82976=CARTESIAN_POINT('Ctrl Pts',(0.977783737726072,-0.652134817790821,
0.0473394751670997)) ;
#82977=CARTESIAN_POINT('Ctrl Pts',(0.984487934328163,-0.641851756955354,
0.0481157372196471)) ;
#82978=CARTESIAN_POINT('Ctrl Pts',(0.987004204195475,-0.637992240646428,
0.048407089775053)) ;
#82979=CARTESIAN_POINT('Ctrl Pts',(0.989499607468229,-0.634115061770119,
0.0486977871654455)) ;
#82980=CARTESIAN_POINT('Ctrl Pts',(0.991969521565222,-0.630227450235288,
0.0489872892015786)) ;
#82981=CARTESIAN_POINT('Ctrl Pts',(1.00094420270959,-0.616101422945214,
0.050039223950282)) ;
#82982=CARTESIAN_POINT('Ctrl Pts',(1.00954934528882,-0.601890188375154,
0.0510714871118151)) ;
#82983=CARTESIAN_POINT('Ctrl Pts',(1.01778810567736,-0.587620236790823,
0.052083333332872)) ;
#82984=CARTESIAN_POINT('Ctrl Pts',(1.03588297104925,-0.556279010610585,
0.0543056605136163)) ;
#82985=CARTESIAN_POINT('Ctrl Pts',(1.05265649617207,-0.523875077122629,
0.0566033415851627)) ;
#82986=CARTESIAN_POINT('Ctrl Pts',(1.06794121459765,-0.490603437521713,
0.0589625495053588)) ;
#82987=CARTESIAN_POINT('Ctrl Pts',(1.0831560161713,-0.457483992304385,0.0613109657062566)) ;
#82988=CARTESIAN_POINT('Ctrl Pts',(1.09689501026764,-0.423505381285014,
0.0637203031839332)) ;
#82989=CARTESIAN_POINT('Ctrl Pts',(1.10903206965691,-0.38889335198346,0.0661745547519881)) ;
#82990=CARTESIAN_POINT('Ctrl Pts',(1.12110084630513,-0.354476048946159,
0.0686149987725218)) ;
#82991=CARTESIAN_POINT('Ctrl Pts',(1.13158529026317,-0.319433203135218,
0.0710997984510217)) ;
#82992=CARTESIAN_POINT('Ctrl Pts',(1.14040729558434,-0.284009455691929,
0.0736116069021118)) ;
#82993=CARTESIAN_POINT('Ctrl Pts',(1.14639361115526,-0.259972094209997,
0.0753160354866054)) ;
#82994=CARTESIAN_POINT('Ctrl Pts',(1.15161504008478,-0.235761997361788,
0.0770327122995954)) ;
#82995=CARTESIAN_POINT('Ctrl Pts',(1.15606152093929,-0.211451958013961,
0.0787564757827807)) ;
#82996=CARTESIAN_POINT('Ctrl Pts',(1.16293619560641,-0.173866366817296,
0.0814215751136272)) ;
#82997=CARTESIAN_POINT('Ctrl Pts',(1.16796201959779,-0.136032559741066,
0.0841042748055188)) ;
#82998=CARTESIAN_POINT('Ctrl Pts',(1.17114009049391,-0.0980869980277225,
0.0867948987364481)) ;
#82999=CARTESIAN_POINT('Ctrl Pts',(1.17750913668542,-0.0220417985293885,
0.0921870717433521)) ;
#83000=CARTESIAN_POINT('Ctrl Pts',(1.1764575549977,0.0544503015484298,0.0976109333415215)) ;
#83001=CARTESIAN_POINT('Ctrl Pts',(1.16799326335438,0.130314648071384,0.102990282520794)) ;
#83002=CARTESIAN_POINT('Ctrl Pts',(1.1645137386421,0.161501176091812,0.105201640445828)) ;
#83003=CARTESIAN_POINT('Ctrl Pts',(1.15978139602167,0.192581525329594,0.107405469501587)) ;
#83004=CARTESIAN_POINT('Ctrl Pts',(1.15379723626192,0.223477310564639,0.10959621159011)) ;
#83005=CARTESIAN_POINT('Ctrl Pts',(1.15113866660766,0.237203313941591,0.1105694878178)) ;
#83006=CARTESIAN_POINT('Ctrl Pts',(1.14823292643457,0.250893708838873,0.111540239138144)) ;
#83007=CARTESIAN_POINT('Ctrl Pts',(1.14507883494787,0.264546087661879,0.112508294834686)) ;
#83008=CARTESIAN_POINT('Ctrl Pts',(1.13736632444846,0.297929429729847,0.114875423294677)) ;
#83009=CARTESIAN_POINT('Ctrl Pts',(1.12816921570323,0.331063129141963,0.117224850224537)) ;
#83010=CARTESIAN_POINT('Ctrl Pts',(1.11754564321342,0.363705796045817,0.119539459279577)) ;
#83011=CARTESIAN_POINT('Ctrl Pts',(1.10685168558726,0.396564732812124,0.121869403484268)) ;
#83012=CARTESIAN_POINT('Ctrl Pts',(1.09471263728511,0.428925268436663,0.124164007322948)) ;
#83013=CARTESIAN_POINT('Ctrl Pts',(1.08123676383361,0.460561864766466,0.126407278454903)) ;
#83014=CARTESIAN_POINT('Ctrl Pts',(1.06776089038211,0.492198461096268,0.128650549586858)) ;
#83015=CARTESIAN_POINT('Ctrl Pts',(1.05294880728718,0.523110465237353,0.13084244171702)) ;
#83016=CARTESIAN_POINT('Ctrl Pts',(1.03695027890869,0.553104230515107,0.132969223848851)) ;
#83017=CARTESIAN_POINT('Ctrl Pts',(1.03073801379148,0.564750878091717,0.133795058209168)) ;
#83018=CARTESIAN_POINT('Ctrl Pts',(1.0243472497762,0.576259465955854,0.13461110310401)) ;
#83019=CARTESIAN_POINT('Ctrl Pts',(1.01778810567666,0.58762023679042,0.135416666666671)) ;
#83020=CARTESIAN_POINT('Ctrl Pts',(1.01147691905926,0.598551532667805,0.136191777244968)) ;
#83021=CARTESIAN_POINT('Ctrl Pts',(1.00495532187839,0.609440442024016,0.136978305885939)) ;
#83022=CARTESIAN_POINT('Ctrl Pts',(0.998223622886107,0.620273947102929,
0.137775772101735)) ;
#83023=CARTESIAN_POINT('Ctrl Pts',(0.994230328960125,0.626700462916888,
0.138248834994084)) ;
#83024=CARTESIAN_POINT('Ctrl Pts',(0.990163120027323,0.633107478035257,
0.138725745462529)) ;
#83025=CARTESIAN_POINT('Ctrl Pts',(0.986022228864173,0.639492247746788,
0.139206391902537)) ;
#83026=CARTESIAN_POINT('Ctrl Pts',(0.982391378490878,0.645090594232399,
0.139627836281867)) ;
#83027=CARTESIAN_POINT('Ctrl Pts',(0.978701509136287,0.650675207237517,
0.140052417976343)) ;
#83028=CARTESIAN_POINT('Ctrl Pts',(0.974968401333292,0.65622159911429,0.140478299761523)) ;
#83029=CARTESIAN_POINT('Ctrl Pts',(0.94517954247386,0.700479813319558,0.143876683376199)) ;
#83030=CARTESIAN_POINT('Ctrl Pts',(0.912465254098321,0.742576356849108,
0.147378071508724)) ;
#83031=CARTESIAN_POINT('Ctrl Pts',(0.877105627658379,0.782224960399829,
0.150955115078013)) ;
#83032=CARTESIAN_POINT('Ctrl Pts',(0.831750620023092,0.833081343733677,
0.155543309432169)) ;
#83033=CARTESIAN_POINT('Ctrl Pts',(0.782044785587662,0.879913760162883,
0.160256013274919)) ;
#83034=CARTESIAN_POINT('Ctrl Pts',(0.728524264359262,0.92219443014058,0.165041591738334)) ;
#83035=CARTESIAN_POINT('Ctrl Pts',(0.706132108701109,0.939884006432844,
0.167043803514445)) ;
#83036=CARTESIAN_POINT('Ctrl Pts',(0.683071546470738,0.95677716846021,0.169058824721421)) ;
#83037=CARTESIAN_POINT('Ctrl Pts',(0.659380441035754,0.972834829106157,
0.171082944473584)) ;
#83038=CARTESIAN_POINT('Ctrl Pts',(0.649585211206294,0.979473965341576,
0.171919828941859)) ;
#83039=CARTESIAN_POINT('Ctrl Pts',(0.639687548158731,0.985966464245742,
0.1727578047544)) ;
#83040=CARTESIAN_POINT('Ctrl Pts',(0.629702276471932,0.992302984853204,
0.173595630396174)) ;
#83041=CARTESIAN_POINT('Ctrl Pts',(0.557229399416611,1.03829330873695,0.17967655003808)) ;
#83042=CARTESIAN_POINT('Ctrl Pts',(0.479966401464458,1.07618734135146,0.185764576080157)) ;
#83043=CARTESIAN_POINT('Ctrl Pts',(0.399297087258105,1.10532891342338,0.191751468645449)) ;
#83044=CARTESIAN_POINT('Ctrl Pts',(0.390512697340452,1.10850225057657,0.192403404256976)) ;
#83045=CARTESIAN_POINT('Ctrl Pts',(0.381687975012754,1.11157177312558,0.19305413597231)) ;
#83046=CARTESIAN_POINT('Ctrl Pts',(0.372824787348853,1.11453660715151,0.193703518155098)) ;
#83047=CARTESIAN_POINT('Ctrl Pts',(0.360834972624344,1.11854733241287,0.194581979985341)) ;
#83048=CARTESIAN_POINT('Ctrl Pts',(0.34877476153917,1.12236648064852,0.19545797257085)) ;
#83049=CARTESIAN_POINT('Ctrl Pts',(0.336648882234719,1.12599187423029,0.196331128362409)) ;
#83050=CARTESIAN_POINT('Ctrl Pts',(0.326768217427892,1.12894599391718,0.19704261158634)) ;
#83051=CARTESIAN_POINT('Ctrl Pts',(0.316853206965907,1.13176869706379,0.197751544689599)) ;
#83052=CARTESIAN_POINT('Ctrl Pts',(0.306906979259801,1.1344594646016,0.198457717160829)) ;
#83053=CARTESIAN_POINT('Ctrl Pts',(0.253270239805225,1.14896989022454,0.202265873375283)) ;
#83054=CARTESIAN_POINT('Ctrl Pts',(0.198716886494649,1.15964686582265,0.205994406585413)) ;
#83055=CARTESIAN_POINT('Ctrl Pts',(0.143643430230035,1.16642905300505,0.209616793303918)) ;
#83056=CARTESIAN_POINT('Ctrl Pts',(0.0960555021956946,1.17228941219517,
0.212746828899368)) ;
#83057=CARTESIAN_POINT('Ctrl Pts',(0.0480783523083568,1.17524047358084,
0.215797620224182)) ;
#83058=CARTESIAN_POINT('Ctrl Pts',(-5.2787093272888E-18,1.17524047358084,
0.218750000000004)) ;
#83059=CARTESIAN_POINT('Ctrl Pts',(1.69773917146898E-12,1.17524047358084,
0.218749999999899)) ;
#83060=CARTESIAN_POINT('Ctrl Pts',(-0.126600692090499,1.17524047358102,
0.226524254003875)) ;
#83061=CARTESIAN_POINT('Ctrl Pts',(-0.252329587007292,1.15478626807222,
0.234970150993983)) ;
#83062=CARTESIAN_POINT('Ctrl Pts',(-0.4964174014379,1.07325253106312,0.252849691552136)) ;
#83063=CARTESIAN_POINT('Ctrl Pts',(-0.612698810244334,1.01138495191746,
0.262183699254262)) ;
#83064=CARTESIAN_POINT('Ctrl Pts',(-0.84002034410012,0.836587015392715,
0.282340225925395)) ;
#83065=CARTESIAN_POINT('Ctrl Pts',(-0.943423576788923,0.717916941119984,
0.292844323157757)) ;
#83066=CARTESIAN_POINT('Ctrl Pts',(-1.09478665341015,0.45276593025062,0.311645511569115)) ;
#83067=CARTESIAN_POINT('Ctrl Pts',(-1.14343934987247,0.309962728219041,
0.321771325905397)) ;
#83068=CARTESIAN_POINT('Ctrl Pts',(-1.17151191967199,0.10815275245462,0.336081161516424)) ;
#83069=CARTESIAN_POINT('Ctrl Pts',(-1.17524047358084,0.0540497505340984,
0.339917468718878)) ;
#83070=CARTESIAN_POINT('Ctrl Pts',(-1.17524047358084,5.94966725733499E-15,
0.343750000000002)) ;
#83071=CARTESIAN_POINT('Origin',(0.,0.,0.)) ;
#83072=CARTESIAN_POINT('',(-1.17524047358084,1.36204092907257E-16,0.906250000000002)) ;
#83073=CARTESIAN_POINT('',(-1.17524047358084,-1.69338707316203E-15,0.843750000000002)) ;
#83074=CARTESIAN_POINT('',(-1.17524047358084,-1.4392544841992E-16,0.)) ;
#83075=CARTESIAN_POINT('Ctrl Pts',(-1.17524047358084,1.04119177003363E-15,
0.906250000000002)) ;
#83076=CARTESIAN_POINT('Ctrl Pts',(-1.17524047358084,0.0202793012904351,
0.904812045970855)) ;
#83077=CARTESIAN_POINT('Ctrl Pts',(-1.17471558743293,0.0405774738555247,
0.903372753827319)) ;
#83078=CARTESIAN_POINT('Ctrl Pts',(-1.16585586118875,0.211393740268767,
0.891260603856515)) ;
#83079=CARTESIAN_POINT('Ctrl Pts',(-1.12916400813093,0.359047310690368,
0.880790862149689)) ;
#83080=CARTESIAN_POINT('Ctrl Pts',(-1.00050354246883,0.635582556545377,
0.861182446391989)) ;
#83081=CARTESIAN_POINT('Ctrl Pts',(-0.908572250758423,0.761238895462286,
0.85172121147626)) ;
#83082=CARTESIAN_POINT('Ctrl Pts',(-0.680988460715921,0.970251111909413,
0.830335556180614)) ;
#83083=CARTESIAN_POINT('Ctrl Pts',(-0.547470900446216,1.05138296722918,
0.819260125930664)) ;
#83084=CARTESIAN_POINT('Ctrl Pts',(-0.261932318018029,1.15534724208175,
0.798039943742627)) ;
#83085=CARTESIAN_POINT('Ctrl Pts',(-0.11341618306421,1.17920917547203,0.788355329287387)) ;
#83086=CARTESIAN_POINT('Ctrl Pts',(0.19139296078578,1.16998813394558,0.769310788426688)) ;
#83087=CARTESIAN_POINT('Ctrl Pts',(0.344719843502962,1.13430450684253,0.758630223295995)) ;
#83088=CARTESIAN_POINT('Ctrl Pts',(0.6257620144399,1.00647439980544,0.736840022340475)) ;
#83089=CARTESIAN_POINT('Ctrl Pts',(0.751272026900972,0.916606473578397,
0.725946590613973)) ;
#83090=CARTESIAN_POINT('Ctrl Pts',(0.958534826557889,0.696258186516551,
0.705406894001169)) ;
#83091=CARTESIAN_POINT('Ctrl Pts',(1.03925302012441,0.568782956917435,0.696580962733728)) ;
#83092=CARTESIAN_POINT('Ctrl Pts',(1.15135135229401,0.283314574452573,0.676339120824057)) ;
#83093=CARTESIAN_POINT('Ctrl Pts',(1.17886389517849,0.127048431846906,0.665258683378948)) ;
#83094=CARTESIAN_POINT('Ctrl Pts',(1.17100472484766,-0.181027472991394,
0.643413799164202)) ;
#83095=CARTESIAN_POINT('Ctrl Pts',(1.13805352029235,-0.329961447770428,
0.632853267218683)) ;
#83096=CARTESIAN_POINT('Ctrl Pts',(1.01675529018029,-0.608954557836807,
0.6130705705183)) ;
#83097=CARTESIAN_POINT('Ctrl Pts',(0.928913126162766,-0.736034408769977,
0.603863890560589)) ;
#83098=CARTESIAN_POINT('Ctrl Pts',(0.707873747457054,-0.950883999345414,
0.582673155614445)) ;
#83099=CARTESIAN_POINT('Ctrl Pts',(0.576292200247247,-1.03592879950197,
0.571577882905812)) ;
#83100=CARTESIAN_POINT('Ctrl Pts',(0.292999335820162,-1.14790387139071,
0.550211592344942)) ;
#83101=CARTESIAN_POINT('Ctrl Pts',(0.144866780735161,-1.17579331214599,
0.540165532210261)) ;
#83102=CARTESIAN_POINT('Ctrl Pts',(-0.160315813799847,-1.17464616911588,
0.521384308485598)) ;
#83103=CARTESIAN_POINT('Ctrl Pts',(-0.3145033932383,-1.14304656608018,0.510795683886598)) ;
#83104=CARTESIAN_POINT('Ctrl Pts',(-0.599172761887689,-1.0225856529898,
0.48904401062123)) ;
#83105=CARTESIAN_POINT('Ctrl Pts',(-0.72731437612933,-0.935793429643947,
0.478098023512044)) ;
#83106=CARTESIAN_POINT('Ctrl Pts',(-0.940171384116082,-0.72078997858306,
0.457404293988808)) ;
#83107=CARTESIAN_POINT('Ctrl Pts',(-1.02397644071054,-0.595756300398089,
0.448493574385486)) ;
#83108=CARTESIAN_POINT('Ctrl Pts',(-1.14360031635853,-0.31333144758319,
0.428467541475363)) ;
#83109=CARTESIAN_POINT('Ctrl Pts',(-1.17524047360901,-0.157447947684027,
0.417414236257988)) ;
#83110=CARTESIAN_POINT('Ctrl Pts',(-1.17524047358084,2.10302920911065E-10,
0.406249999985091)) ;
#83111=CARTESIAN_POINT('Ctrl Pts',(-1.17524047358084,5.96744875736022E-15,
0.343750000000002)) ;
#83112=CARTESIAN_POINT('Ctrl Pts',(-1.17524047358084,-0.10056073900197,
0.350880507986989)) ;
#83113=CARTESIAN_POINT('Ctrl Pts',(-1.16233296013586,-0.200937146127487,
0.357997945466203)) ;
#83114=CARTESIAN_POINT('Ctrl Pts',(-1.09785564047115,-0.446351823951105,
0.375399680355109)) ;
#83115=CARTESIAN_POINT('Ctrl Pts',(-1.03064731215459,-0.585043083983595,
0.384535643011968)) ;
#83116=CARTESIAN_POINT('Ctrl Pts',(-0.84776435181588,-0.827873160197687,
0.404375293844389)) ;
#83117=CARTESIAN_POINT('Ctrl Pts',(-0.734282924849944,-0.929994728118301,
0.414964515506367)) ;
#83118=CARTESIAN_POINT('Ctrl Pts',(-0.469784373122341,-1.08867274565634,
0.436832484995882)) ;
#83119=CARTESIAN_POINT('Ctrl Pts',(-0.320081111277505,-1.14169623565684,
0.447905294936889)) ;
#83120=CARTESIAN_POINT('Ctrl Pts',(-0.0164013647280398,-1.18458870108195,
0.468074259944006)) ;
#83121=CARTESIAN_POINT('Ctrl Pts',(0.134153473501831,-1.17708405685267,
0.476922690824644)) ;
#83122=CARTESIAN_POINT('Ctrl Pts',(0.427990911138155,-1.10518837239671,
0.497515535036282)) ;
#83123=CARTESIAN_POINT('Ctrl Pts',(0.568123902524849,-1.04011790080108,
0.508427767447896)) ;
#83124=CARTESIAN_POINT('Ctrl Pts',(0.817806327670518,-0.858293519786357,
0.530206538152454)) ;
#83125=CARTESIAN_POINT('Ctrl Pts',(0.924317628413691,-0.742386396552834,
0.540856490029454)) ;
#83126=CARTESIAN_POINT('Ctrl Pts',(1.0823830905674,-0.481525143101595,0.559811428644212)) ;
#83127=CARTESIAN_POINT('Ctrl Pts',(1.13471881974578,-0.340406375375874,
0.569612643785922)) ;
#83128=CARTESIAN_POINT('Ctrl Pts',(1.18471102264315,-0.0404316039914042,
0.590883097090857)) ;
#83129=CARTESIAN_POINT('Ctrl Pts',(1.17972508402808,0.115872602932994,0.601966233580656)) ;
#83130=CARTESIAN_POINT('Ctrl Pts',(1.10966180879066,0.416545840309742,0.623286213344783)) ;
#83131=CARTESIAN_POINT('Ctrl Pts',(1.04568659395149,0.558019808731794,0.632654039607303)) ;
#83132=CARTESIAN_POINT('Ctrl Pts',(0.868552388088852,0.805966324916247,
0.652322069717154)) ;
#83133=CARTESIAN_POINT('Ctrl Pts',(0.758009163999587,0.910696733028636,
0.662823356309342)) ;
#83134=CARTESIAN_POINT('Ctrl Pts',(0.498423053649437,1.0758012021434,0.684617505925215)) ;
#83135=CARTESIAN_POINT('Ctrl Pts',(0.350593694266161,1.13263935614624,0.69571048796941)) ;
#83136=CARTESIAN_POINT('Ctrl Pts',(0.0481602798510692,1.18378120089601,
0.716095389944385)) ;
#83137=CARTESIAN_POINT('Ctrl Pts',(-0.103009693180801,1.18027462929666,
0.724897106005194)) ;
#83138=CARTESIAN_POINT('Ctrl Pts',(-0.39867718968897,1.11604386548558,0.745330579794386)) ;
#83139=CARTESIAN_POINT('Ctrl Pts',(-0.540113184163221,1.05487699393238,
0.7561844293853)) ;
#83140=CARTESIAN_POINT('Ctrl Pts',(-0.794319299722647,0.880080649233699,
0.777991819243996)) ;
#83141=CARTESIAN_POINT('Ctrl Pts',(-0.903942617574611,0.767070080997107,
0.788730179153422)) ;
#83142=CARTESIAN_POINT('Ctrl Pts',(-1.06890822958908,0.510689481693172,
0.807949983986318)) ;
#83143=CARTESIAN_POINT('Ctrl Pts',(-1.12497808721731,0.37124377155117,0.817426041918157)) ;
#83144=CARTESIAN_POINT('Ctrl Pts',(-1.16799649676227,0.150680192339373,
0.833065648178182)) ;
#83145=CARTESIAN_POINT('Ctrl Pts',(-1.17524047358084,0.0753367271238741,
0.838408062979634)) ;
#83146=CARTESIAN_POINT('Ctrl Pts',(-1.17524047358084,-3.71854203583437E-15,
0.843750000000002)) ;
#83147=CARTESIAN_POINT('Origin',(0.,0.,0.)) ;
#83148=CARTESIAN_POINT('',(-1.17524047358084,1.0382603004152E-15,1.40625)) ;
#83149=CARTESIAN_POINT('',(-1.17524047358084,7.52030926879024E-16,1.34375)) ;
#83150=CARTESIAN_POINT('',(-1.17524047358084,-1.4392544841992E-16,0.)) ;
#83151=CARTESIAN_POINT('Ctrl Pts',(-1.17524047358084,1.93364185863387E-15,
1.40625)) ;
#83152=CARTESIAN_POINT('Ctrl Pts',(-1.17524047358084,0.04022257400546,1.40339791887918)) ;
#83153=CARTESIAN_POINT('Ctrl Pts',(-1.17317560429429,0.0804927572900409,
1.40054246190466)) ;
#83154=CARTESIAN_POINT('Ctrl Pts',(-1.15363384185356,0.269838964882093,
1.38711640061135)) ;
#83155=CARTESIAN_POINT('Ctrl Pts',(-1.10981617409642,0.414746302173939,
1.3768413873588)) ;
#83156=CARTESIAN_POINT('Ctrl Pts',(-0.966822628308877,0.686334315935149,
1.35758376733219)) ;
#83157=CARTESIAN_POINT('Ctrl Pts',(-0.866656139323778,0.809163180776926,
1.34744814557029)) ;
#83158=CARTESIAN_POINT('Ctrl Pts',(-0.626271893489302,1.00630816652666,
1.32569718173687)) ;
#83159=CARTESIAN_POINT('Ctrl Pts',(-0.489259202086931,1.0795836502592,1.31468566134647)) ;
#83160=CARTESIAN_POINT('Ctrl Pts',(-0.199493226876555,1.16772697093534,
1.29376679674992)) ;
#83161=CARTESIAN_POINT('Ctrl Pts',(-0.0500767687957025,1.18357945674508,
1.28462074599962)) ;
#83162=CARTESIAN_POINT('Ctrl Pts',(0.253749602960034,1.15807119453095,1.26505911204832)) ;
#83163=CARTESIAN_POINT('Ctrl Pts',(0.404998008215433,1.11421428515519,1.25421640798347)) ;
#83164=CARTESIAN_POINT('Ctrl Pts',(0.678131728877579,0.971835826442956,
1.23239605312863)) ;
#83165=CARTESIAN_POINT('Ctrl Pts',(0.798109033041594,0.875991959562471,
1.22163050272023)) ;
#83166=CARTESIAN_POINT('Ctrl Pts',(0.993951951775847,0.644955162106818,
1.2014131267936)) ;
#83167=CARTESIAN_POINT('Ctrl Pts',(1.06836977023306,0.512342277031657,1.19257889669174)) ;
#83168=CARTESIAN_POINT('Ctrl Pts',(1.16482435595196,0.22089396801138,1.17191303329527)) ;
#83169=CARTESIAN_POINT('Ctrl Pts',(1.18383776080121,0.0642437159595267,
1.16080535961959)) ;
#83170=CARTESIAN_POINT('Ctrl Pts',(1.15996489664612,-0.241400433726271,
1.13913290502011)) ;
#83171=CARTESIAN_POINT('Ctrl Pts',(1.11960234743318,-0.387690749984452,
1.12875982822244)) ;
#83172=CARTESIAN_POINT('Ctrl Pts',(0.983613341401883,-0.661723584428254,
1.10932885213684)) ;
#83173=CARTESIAN_POINT('Ctrl Pts',(0.887517303054449,-0.785946092176641,
1.09955231366117)) ;
#83174=CARTESIAN_POINT('Ctrl Pts',(0.65339647872034,-0.988975611380567,
1.0779773432707)) ;
#83175=CARTESIAN_POINT('Ctrl Pts',(0.518044727734835,-1.06612844449193,
1.06693035084248)) ;
#83176=CARTESIAN_POINT('Ctrl Pts',(0.230321117048486,-1.16204066071992,
1.04586146672072)) ;
#83177=CARTESIAN_POINT('Ctrl Pts',(0.0813714242245326,-1.18183751648957,
1.03648071970046)) ;
#83178=CARTESIAN_POINT('Ctrl Pts',(-0.222980227030622,-1.16438441904261,
1.01717241525019)) ;
#83179=CARTESIAN_POINT('Ctrl Pts',(-0.375313403061051,-1.12455686395351,
1.0064059536026)) ;
#83180=CARTESIAN_POINT('Ctrl Pts',(-0.652455471206262,-0.989317123906594,
0.98459254970711)) ;
#83181=CARTESIAN_POINT('Ctrl Pts',(-0.775205273694797,-0.896389255418135,
0.973760129666063)) ;
#83182=CARTESIAN_POINT('Ctrl Pts',(-0.976718230171345,-0.670624059163199,
0.953381467873824)) ;
#83183=CARTESIAN_POINT('Ctrl Pts',(-1.05426732657947,-0.54058712396737,
0.944581667441689)) ;
#83184=CARTESIAN_POINT('Ctrl Pts',(-1.15162322837993,-0.271198393744022,
0.925479993055387)) ;
#83185=CARTESIAN_POINT('Ctrl Pts',(-1.17524047358084,-0.136023713315906,
0.915895097916393)) ;
#83186=CARTESIAN_POINT('Ctrl Pts',(-1.17524047358084,8.67361737988404E-16,
0.906250000000002)) ;
#83187=CARTESIAN_POINT('Ctrl Pts',(-1.17524047358084,-3.71854203583437E-15,
0.843750000000002)) ;
#83188=CARTESIAN_POINT('Ctrl Pts',(-1.17524047358084,-0.078372892307368,
0.849307223824201)) ;
#83189=CARTESIAN_POINT('Ctrl Pts',(-1.16740080636849,-0.156738492471966,
0.854863930580949)) ;
#83190=CARTESIAN_POINT('Ctrl Pts',(-1.12085118653128,-0.385937684285252,
0.871115866317054)) ;
#83191=CARTESIAN_POINT('Ctrl Pts',(-1.06019873478228,-0.530294701065063,
0.880779924121279)) ;
#83192=CARTESIAN_POINT('Ctrl Pts',(-0.888915438186115,-0.783377667817373,
0.900270769870976)) ;
#83193=CARTESIAN_POINT('Ctrl Pts',(-0.781390210104203,-0.890651624122545,
0.910676906637472)) ;
#83194=CARTESIAN_POINT('Ctrl Pts',(-0.5269036707543,-1.06208047624785,0.932382126472764)) ;
#83195=CARTESIAN_POINT('Ctrl Pts',(-0.381055225059466,-1.12269807590544,
0.943487460687598)) ;
#83196=CARTESIAN_POINT('Ctrl Pts',(-0.0799626681969364,-1.18213557941063,
0.964084135823149)) ;
#83197=CARTESIAN_POINT('Ctrl Pts',(0.071867518770716,-1.18265521488411,
0.972900336861989)) ;
#83198=CARTESIAN_POINT('Ctrl Pts',(0.369300845634156,-1.12605315656733,
0.993171780067366)) ;
#83199=CARTESIAN_POINT('Ctrl Pts',(0.511924838644523,-1.0687843688582,1.00396038024544)) ;
#83200=CARTESIAN_POINT('Ctrl Pts',(0.770425194894299,-0.901076654851032,
1.02578015098746)) ;
#83201=CARTESIAN_POINT('Ctrl Pts',(0.883058018607359,-0.791027335171729,
1.03659833032357)) ;
#83202=CARTESIAN_POINT('Ctrl Pts',(1.05483070655924,-0.539159838753598,
1.05607613549244)) ;
#83203=CARTESIAN_POINT('Ctrl Pts',(1.11459544966178,-0.401318682169378,
1.06529350597521)) ;
#83204=CARTESIAN_POINT('Ctrl Pts',(1.18057883902678,-0.105594918914387,
1.0862625310317)) ;
#83205=CARTESIAN_POINT('Ctrl Pts',(1.18424105822213,0.0498773760115757,
1.09728667874309)) ;
#83206=CARTESIAN_POINT('Ctrl Pts',(1.13096504430472,0.355816569528943,1.11898005415539)) ;
#83207=CARTESIAN_POINT('Ctrl Pts',(1.07359647263153,0.503036071445992,1.12899077992006)) ;
#83208=CARTESIAN_POINT('Ctrl Pts',(0.908029028731414,0.761068349354,1.14830610002792)) ;
#83209=CARTESIAN_POINT('Ctrl Pts',(0.803473383957124,0.870718346127371,
1.15861412110518)) ;
#83210=CARTESIAN_POINT('Ctrl Pts',(0.55405468980877,1.04811272561393,1.18021963659358)) ;
#83211=CARTESIAN_POINT('Ctrl Pts',(0.410207640003824,1.11232003373639,1.19132933832228)) ;
#83212=CARTESIAN_POINT('Ctrl Pts',(0.11049155378206,1.17976547217851,1.21212539881691)) ;
#83213=CARTESIAN_POINT('Ctrl Pts',(-0.0420042747174427,1.18418253655367,
1.2210123552515)) ;
#83214=CARTESIAN_POINT('Ctrl Pts',(-0.341078428303618,1.13487089602653,
1.24112608525408)) ;
#83215=CARTESIAN_POINT('Ctrl Pts',(-0.484735956272483,1.08133427966265,
1.25184583298843)) ;
#83216=CARTESIAN_POINT('Ctrl Pts',(-0.747142454712865,0.920478081773251,
1.27366255898542)) ;
#83217=CARTESIAN_POINT('Ctrl Pts',(-0.862566052875092,0.813327180918138,
1.28454935350987)) ;
#83218=CARTESIAN_POINT('Ctrl Pts',(-1.04078647908616,0.565824186520556,
1.30426836137977)) ;
#83219=CARTESIAN_POINT('Ctrl Pts',(-1.1040680687744,0.429463242089193,1.31329784632424)) ;
#83220=CARTESIAN_POINT('Ctrl Pts',(-1.16352312203673,0.191486738352365,
1.33017215907742)) ;
#83221=CARTESIAN_POINT('Ctrl Pts',(-1.17524047358084,0.0958129055313116,
1.33695614889143)) ;
#83222=CARTESIAN_POINT('Ctrl Pts',(-1.17524047358084,3.04920446938418E-15,
1.34375)) ;
#83223=CARTESIAN_POINT('Origin',(0.,0.,0.)) ;
#83224=CARTESIAN_POINT('',(-1.17524047358084,-1.51178320927071E-15,1.90625)) ;
#83225=CARTESIAN_POINT('',(-1.17524047358084,-3.66865715126017E-16,1.84375)) ;
#83226=CARTESIAN_POINT('',(-1.17524047358084,-1.4392544841992E-16,0.)) ;
#83227=CARTESIAN_POINT('Ctrl Pts',(-1.17524047358084,-1.93364185863387E-15,
1.90625)) ;
#83228=CARTESIAN_POINT('Ctrl Pts',(-1.17524047358084,0.0620702449181597,
1.90184875572181)) ;
#83229=CARTESIAN_POINT('Ctrl Pts',(-1.17032322149779,0.124185902335723,
1.89744429135801)) ;
#83230=CARTESIAN_POINT('Ctrl Pts',(-1.13686603480775,0.333198273001777,
1.8826237521177)) ;
#83231=CARTESIAN_POINT('Ctrl Pts',(-1.08539661824635,0.474712480263841,
1.87273801672552)) ;
#83232=CARTESIAN_POINT('Ctrl Pts',(-0.928933450973058,0.736601141370628,
1.85384504587131)) ;
#83233=CARTESIAN_POINT('Ctrl Pts',(-0.823153083206283,0.853165552137381,
1.84321667558877)) ;
#83234=CARTESIAN_POINT('Ctrl Pts',(-0.574544799352632,1.03659861296798,
1.82144683169118)) ;
#83235=CARTESIAN_POINT('Ctrl Pts',(-0.434728280900438,1.10256826143134,
1.81052215396611)) ;
#83236=CARTESIAN_POINT('Ctrl Pts',(-0.141321704421145,1.17623437512204,
1.78989299960338)) ;
#83237=CARTESIAN_POINT('Ctrl Pts',(0.00909819868139983,1.1846564506662,
1.78102513235836)) ;
#83238=CARTESIAN_POINT('Ctrl Pts',(0.313051975628829,1.14365715711825,1.76090645979978)) ;
#83239=CARTESIAN_POINT('Ctrl Pts',(0.463171539465951,1.0915165113851,1.7498393858503)) ;
#83240=CARTESIAN_POINT('Ctrl Pts',(0.728774489075423,0.934331756521546,
1.72795653959804)) ;
#83241=CARTESIAN_POINT('Ctrl Pts',(0.842920959693578,0.832819718037304,
1.71734808924873)) ;
#83242=CARTESIAN_POINT('Ctrl Pts',(1.0271136198994,0.591165030054373,1.69746968469931)) ;
#83243=CARTESIAN_POINT('Ctrl Pts',(1.09505484350283,0.453100495453474,1.6883782116043)) ;
#83244=CARTESIAN_POINT('Ctrl Pts',(1.17518605745325,0.155812781552446,1.66729829075803)) ;
#83245=CARTESIAN_POINT('Ctrl Pts',(1.18546762072542,-0.000766465150745417,
1.65619565189226)) ;
#83246=CARTESIAN_POINT('Ctrl Pts',(1.14530292216298,-0.303048152507463,
1.63476162100299)) ;
#83247=CARTESIAN_POINT('Ctrl Pts',(1.09748010274341,-0.446226863218259,
1.62460918029479)) ;
#83248=CARTESIAN_POINT('Ctrl Pts',(0.947630262761121,-0.712359381071128,
1.60573839570251)) ;
#83249=CARTESIAN_POINT('Ctrl Pts',(0.844917717132733,-0.831641643055628,
1.59531629414138)) ;
#83250=CARTESIAN_POINT('Ctrl Pts',(0.600700962335393,-1.02172106265588,
1.57358048557175)) ;
#83251=CARTESIAN_POINT('Ctrl Pts',(0.462244563371156,-1.09137091714145,
1.5626088525641)) ;
#83252=CARTESIAN_POINT('Ctrl Pts',(0.170639783454818,-1.17230698850336,
1.54183259516968)) ;
#83253=CARTESIAN_POINT('Ctrl Pts',(0.0207459066617789,-1.18447520582619,
1.5328513636375)) ;
#83254=CARTESIAN_POINT('Ctrl Pts',(-0.282514133918315,-1.15139421754003,
1.51305602532775)) ;
#83255=CARTESIAN_POINT('Ctrl Pts',(-0.432642605518342,-1.10377731834681,
1.50214878809337)) ;
#83256=CARTESIAN_POINT('Ctrl Pts',(-0.701839874216317,-0.954796873471342,
1.48033609651557)) ;
#83257=CARTESIAN_POINT('Ctrl Pts',(-0.819149554004533,-0.856285326726335,
1.46963977949436)) ;
#83258=CARTESIAN_POINT('Ctrl Pts',(-1.00962200101427,-0.620317325344421,
1.44957736213647)) ;
#83259=CARTESIAN_POINT('Ctrl Pts',(-1.08106222403007,-0.485219252727698,
1.44065567155089)) ;
#83260=CARTESIAN_POINT('Ctrl Pts',(-1.15834765003112,-0.229692427266968,
1.42253690981624)) ;
#83261=CARTESIAN_POINT('Ctrl Pts',(-1.17524047358084,-0.115040940888189,
1.41440726252586)) ;
#83262=CARTESIAN_POINT('Ctrl Pts',(-1.17524047358084,1.76941794549634E-15,
1.40625)) ;
#83263=CARTESIAN_POINT('Ctrl Pts',(-1.17524047358084,3.04920446938418E-15,
1.34375)) ;
#83264=CARTESIAN_POINT('Ctrl Pts',(-1.17524047358084,-0.0571461524468516,
1.34780208931927)) ;
#83265=CARTESIAN_POINT('Ctrl Pts',(-1.17107246744237,-0.11434177785293,
1.35185768664109)) ;
#83266=CARTESIAN_POINT('Ctrl Pts',(-1.14000361664372,-0.325435712949174,
1.36682582435713)) ;
#83267=CARTESIAN_POINT('Ctrl Pts',(-1.08681495493178,-0.473604338824473,
1.37713559876278)) ;
#83268=CARTESIAN_POINT('Ctrl Pts',(-0.928983299727095,-0.735260713248269,
1.39610436984653)) ;
#83269=CARTESIAN_POINT('Ctrl Pts',(-0.827849738352091,-0.8475019580805,
1.40629411816986)) ;
#83270=CARTESIAN_POINT('Ctrl Pts',(-0.584329250040727,-1.03147256612151,
1.4277705904358)) ;
#83271=CARTESIAN_POINT('Ctrl Pts',(-0.44284916566883,-1.09966702637141,
1.43887630176619)) ;
#83272=CARTESIAN_POINT('Ctrl Pts',(-0.144797673821169,-1.17617198619236,
1.45989133728082)) ;
#83273=CARTESIAN_POINT('Ctrl Pts',(0.0084922086471124,-1.18501871018999,
1.4689248117494)) ;
#83274=CARTESIAN_POINT('Ctrl Pts',(0.309344866126974,-1.14387388278698,
1.48885821149429)) ;
#83275=CARTESIAN_POINT('Ctrl Pts',(0.454041837088111,-1.09451906300235,
1.49949352868873)) ;
#83276=CARTESIAN_POINT('Ctrl Pts',(0.721892420234701,-0.940665283792315,
1.52139630135329)) ;
#83277=CARTESIAN_POINT('Ctrl Pts',(0.841303444694949,-0.835587345031483,
1.53245446019827)) ;
#83278=CARTESIAN_POINT('Ctrl Pts',(1.02663502806333,-0.591169448394882,
1.55250076944265)) ;
#83279=CARTESIAN_POINT('Ctrl Pts',(1.09332082134992,-0.456198563499785,
1.56140211221623)) ;
#83280=CARTESIAN_POINT('Ctrl Pts',(1.17371744524374,-0.164538408549839,
1.58208299707245)) ;
#83281=CARTESIAN_POINT('Ctrl Pts',(1.18514751286619,-0.0102269767388764,
1.59302483091269)) ;
#83282=CARTESIAN_POINT('Ctrl Pts',(1.14782573398913,0.296588702875181,1.61478035574011)) ;
#83283=CARTESIAN_POINT('Ctrl Pts',(1.09843102085877,0.446032345250234,1.62537702692745)) ;
#83284=CARTESIAN_POINT('Ctrl Pts',(0.94743739780899,0.711217516993629,1.64418063760009)) ;
#83285=CARTESIAN_POINT('Ctrl Pts',(0.849498492656227,0.825756775880921,
1.65419377055637)) ;
#83286=CARTESIAN_POINT('Ctrl Pts',(0.611371103160633,1.01561578403287,1.67554783095833)) ;
#83287=CARTESIAN_POINT('Ctrl Pts',(0.472131147139452,1.08735755872389,1.68664174677093)) ;
#83288=CARTESIAN_POINT('Ctrl Pts',(0.175693143720339,1.17208665320142,1.70784927802165)) ;
#83289=CARTESIAN_POINT('Ctrl Pts',(0.0216498618195364,1.18497964669672,
1.71707524226508)) ;
#83290=CARTESIAN_POINT('Ctrl Pts',(-0.280748676962267,1.15117800427482,
1.73684322763561)) ;
#83291=CARTESIAN_POINT('Ctrl Pts',(-0.426273891349944,1.10557843348025,
1.74739626772215)) ;
#83292=CARTESIAN_POINT('Ctrl Pts',(-0.69727449409683,0.958988168389735,
1.7692349570435)) ;
#83293=CARTESIAN_POINT('Ctrl Pts',(-0.819053205034701,0.857331536334873,
1.78031721189922)) ;
#83294=CARTESIAN_POINT('Ctrl Pts',(-1.01078815793964,0.617964087801939,
1.80057767991255)) ;
#83295=CARTESIAN_POINT('Ctrl Pts',(-1.08114979329975,0.484448938981724,
1.80939894945103)) ;
#83296=CARTESIAN_POINT('Ctrl Pts',(-1.15823561048095,0.230432003852988,
1.82741064867621)) ;
#83297=CARTESIAN_POINT('Ctrl Pts',(-1.17524047358084,0.11542194896722,1.83556572115368)) ;
#83298=CARTESIAN_POINT('Ctrl Pts',(-1.17524047358084,-2.0122792321331E-15,
1.84375)) ;
#83299=CARTESIAN_POINT('Origin',(0.,0.,0.)) ;
#83300=CARTESIAN_POINT('',(-1.17524047358084,1.46543595637449E-15,2.40625)) ;
#83301=CARTESIAN_POINT('',(-1.17524047358084,-2.10740602288104E-16,2.34375)) ;
#83302=CARTESIAN_POINT('',(-1.17524047358084,-1.4392544841992E-16,0.)) ;
#83303=CARTESIAN_POINT('Ctrl Pts',(-1.17524047358084,3.86728371726775E-15,
2.40625)) ;
#83304=CARTESIAN_POINT('Ctrl Pts',(-1.17524047358084,0.0834495761747775,
2.40033280134642)) ;
#83305=CARTESIAN_POINT('Ctrl Pts',(-1.16635217935271,0.166862378997987,
2.39441821019833)) ;
#83306=CARTESIAN_POINT('Ctrl Pts',(-1.11706459718736,0.394393758538108,
2.37828453481763)) ;
#83307=CARTESIAN_POINT('Ctrl Pts',(-1.05815594704201,0.532602159607403,
2.36901282500718)) ;
#83308=CARTESIAN_POINT('Ctrl Pts',(-0.887957895915845,0.785522102144264,
2.34959440147497)) ;
#83309=CARTESIAN_POINT('Ctrl Pts',(-0.776015636887052,0.89626550280217,
2.33879402034525)) ;
#83310=CARTESIAN_POINT('Ctrl Pts',(-0.518493345242722,1.0656264026718,2.31697569865871)) ;
#83311=CARTESIAN_POINT('Ctrl Pts',(-0.376135411641797,1.12380087866683,
2.30617132653577)) ;
#83312=CARTESIAN_POINT('Ctrl Pts',(-0.0791076040610528,1.1821736635866,
2.28586200645094)) ;
#83313=CARTESIAN_POINT('Ctrl Pts',(0.0725661795061427,1.18259313534048,
2.27705455905564)) ;
#83314=CARTESIAN_POINT('Ctrl Pts',(0.37397870511359,1.12508890452228,2.25650677712517)) ;
#83315=CARTESIAN_POINT('Ctrl Pts',(0.520297290338154,1.06534672146473,2.24540360952536)) ;
#83316=CARTESIAN_POINT('Ctrl Pts',(0.775986170953501,0.895378863462734,
2.22367635441125)) ;
#83317=CARTESIAN_POINT('Ctrl Pts',(0.884220168238866,0.788690305821157,
2.21324744834696)) ;
#83318=CARTESIAN_POINT('Ctrl Pts',(1.05687330065032,0.536803523834036,2.19371489338642)) ;
#83319=CARTESIAN_POINT('Ctrl Pts',(1.11830696198107,0.393125915306599,2.1841255656214)) ;
#83320=CARTESIAN_POINT('Ctrl Pts',(1.18190897774897,0.0903690543124847,
2.16265784136978)) ;
#83321=CARTESIAN_POINT('Ctrl Pts',(1.18353793976289,-0.0656690731964901,
2.15159357189922)) ;
#83322=CARTESIAN_POINT('Ctrl Pts',(1.12733899954514,-0.364026815236812,
2.13043777806047)) ;
#83323=CARTESIAN_POINT('Ctrl Pts',(1.07214749838274,-0.503861438847376,
2.12089097958312)) ;
#83324=CARTESIAN_POINT('Ctrl Pts',(0.908803610461331,-0.761303455262943,
2.10173312985122)) ;
#83325=CARTESIAN_POINT('Ctrl Pts',(0.799906337408573,-0.875004375116867,
2.09101487911931)) ;
#83326=CARTESIAN_POINT('Ctrl Pts',(0.546748269139941,-1.05146697417733,
2.06921277246286)) ;
#83327=CARTESIAN_POINT('Ctrl Pts',(0.405609687779362,-1.11355576229213,
2.0583445009321)) ;
#83328=CARTESIAN_POINT('Ctrl Pts',(0.110368603997391,-1.17959403248063,
2.03787312930077)) ;
#83329=CARTESIAN_POINT('Ctrl Pts',(-0.0406517881214192,-1.18404743083405,
2.02906590780156)) ;
#83330=CARTESIAN_POINT('Ctrl Pts',(-0.343388059821988,-1.13485866192171,
2.00873165190228)) ;
#83331=CARTESIAN_POINT('Ctrl Pts',(-0.491669810186357,-1.07891875610629,
1.99764273583528)) ;
#83332=CARTESIAN_POINT('Ctrl Pts',(-0.752433496068832,-0.915323715049072,
1.97582978891062)) ;
#83333=CARTESIAN_POINT('Ctrl Pts',(-0.863678168296611,-0.811203927399449,
1.96530707679724)) ;
#83334=CARTESIAN_POINT('Ctrl Pts',(-1.04217961452683,-0.564467980662324,
1.9455980068477)) ;
#83335=CARTESIAN_POINT('Ctrl Pts',(-1.10692635915049,-0.423660441951649,
1.93629069177583)) ;
#83336=CARTESIAN_POINT('Ctrl Pts',(-1.16439348800968,-0.184272101586651,
1.91931626925363)) ;
#83337=CARTESIAN_POINT('Ctrl Pts',(-1.17524047358084,-0.0921861360282586,
1.9127866860443)) ;
#83338=CARTESIAN_POINT('Ctrl Pts',(-1.17524047358084,-1.93364185863387E-15,
1.90625)) ;
#83339=CARTESIAN_POINT('Ctrl Pts',(-1.17524047358084,-1.97082727899222E-15,
1.84375)) ;
#83340=CARTESIAN_POINT('Ctrl Pts',(-1.17524047358084,-0.0369227145432839,
1.84636809642177)) ;
#83341=CARTESIAN_POINT('Ctrl Pts',(-1.17350050494735,-0.0738875789323789,
1.84898918158263)) ;
#83342=CARTESIAN_POINT('Ctrl Pts',(-1.15531888768442,-0.265927879751574,
1.86260627422142)) ;
#83343=CARTESIAN_POINT('Ctrl Pts',(-1.10990808627486,-0.416663234139651,
1.87329453744474)) ;
#83344=CARTESIAN_POINT('Ctrl Pts',(-0.966120197721852,-0.685568682193822,
1.8923619435132)) ;
#83345=CARTESIAN_POINT('Ctrl Pts',(-0.871483293981198,-0.802462772346145,
1.90201787557277)) ;
#83346=CARTESIAN_POINT('Ctrl Pts',(-0.639185790066518,-0.998278888114406,
1.92322513798936)) ;
#83347=CARTESIAN_POINT('Ctrl Pts',(-0.502379855421458,-1.07365518346609,
1.93429844355089)) ;
#83348=CARTESIAN_POINT('Ctrl Pts',(-0.207738743852656,-1.16699033977343,
1.95570074890575)) ;
#83349=CARTESIAN_POINT('Ctrl Pts',(-0.0528796569725674,-1.18414916102219,
1.96518693701189)) ;
#83350=CARTESIAN_POINT('Ctrl Pts',(0.251069176422445,-1.15796405987137,
1.98478008751724)) ;
#83351=CARTESIAN_POINT('Ctrl Pts',(0.397347839176802,-1.11624903803342,
1.99524167333822)) ;
#83352=CARTESIAN_POINT('Ctrl Pts',(0.671396769691305,-0.977212386910812,
2.01699974953374)) ;
#83353=CARTESIAN_POINT('Ctrl Pts',(0.795518854725933,-0.879136203929369,
2.0280989652418)) ;
#83354=CARTESIAN_POINT('Ctrl Pts',(0.993804818622206,-0.645043587864466,
2.04857470307815)) ;
#83355=CARTESIAN_POINT('Ctrl Pts',(1.06797519504685,-0.512990391897107,
2.05737514712029)) ;
#83356=CARTESIAN_POINT('Ctrl Pts',(1.16338541714191,-0.225789755613562,
2.07773981877259)) ;
#83357=CARTESIAN_POINT('Ctrl Pts',(1.18283238528975,-0.0731000063795935,
2.08856666319766)) ;
#83358=CARTESIAN_POINT('Ctrl Pts',(1.16209969672046,0.234549305736465,2.11038129880004)) ;
#83359=CARTESIAN_POINT('Ctrl Pts',(1.12077669646272,0.386486048632133,2.12115474944774)) ;
#83360=CARTESIAN_POINT('Ctrl Pts',(0.984348216925391,0.659104502713493,
2.14048543539456)) ;
#83361=CARTESIAN_POINT('Ctrl Pts',(0.893009466813732,0.778407601930865,
2.14984315768763)) ;
#83362=CARTESIAN_POINT('Ctrl Pts',(0.666587026440478,0.980128001727854,
2.17089897505181)) ;
#83363=CARTESIAN_POINT('Ctrl Pts',(0.53231423687697,1.05907036021218,2.18194315633091)) ;
#83364=CARTESIAN_POINT('Ctrl Pts',(0.239593499292404,1.16104702568118,2.20353390977969)) ;
#83365=CARTESIAN_POINT('Ctrl Pts',(0.0838932043262317,1.1825275122596,2.21333996072108)) ;
#83366=CARTESIAN_POINT('Ctrl Pts',(-0.221545121912344,1.16392516257651,
2.23275574064081)) ;
#83367=CARTESIAN_POINT('Ctrl Pts',(-0.368468205679511,1.12606139499527,
2.24312035750159)) ;
#83368=CARTESIAN_POINT('Ctrl Pts',(-0.645330677917689,0.994553419131068,
2.26478428707692)) ;
#83369=CARTESIAN_POINT('Ctrl Pts',(-0.771671046636979,0.900068111178731,
2.27589241248701)) ;
#83370=CARTESIAN_POINT('Ctrl Pts',(-0.976388228670599,0.671262250230045,
2.29657564124344)) ;
#83371=CARTESIAN_POINT('Ctrl Pts',(-1.05434711077808,0.540627456958495,
2.3054154726478)) ;
#83372=CARTESIAN_POINT('Ctrl Pts',(-1.15169317363573,0.270768039187681,
2.32455052229915)) ;
#83373=CARTESIAN_POINT('Ctrl Pts',(-1.17524047358084,0.135823181646263,
2.33411912127776)) ;
#83374=CARTESIAN_POINT('Ctrl Pts',(-1.17524047358084,-2.04697370165263E-15,
2.34375)) ;
#83375=CARTESIAN_POINT('Origin',(0.,0.,0.)) ;
#83376=CARTESIAN_POINT('',(-1.17524047358084,-1.87607513922584E-15,2.90625)) ;
#83377=CARTESIAN_POINT('',(-1.17524047358084,1.76684416032546E-15,2.84375)) ;
#83378=CARTESIAN_POINT('',(-1.17524047358084,-1.4392544841992E-16,0.)) ;
#83379=CARTESIAN_POINT('Ctrl Pts',(-1.17524047358084,-3.33066907387547E-15,
2.90625)) ;
#83380=CARTESIAN_POINT('Ctrl Pts',(-1.17524047358084,0.102796714931198,
2.89896094460793)) ;
#83381=CARTESIAN_POINT('Ctrl Pts',(-1.16175251768774,0.205374231616836,
2.89168743200976)) ;
#83382=CARTESIAN_POINT('Ctrl Pts',(-1.09622846694473,0.449144165446436,
2.87440232176286)) ;
#83383=CARTESIAN_POINT('Ctrl Pts',(-1.03044749565387,0.584480502606388,
2.8654720323337)) ;
#83384=CARTESIAN_POINT('Ctrl Pts',(-0.847669471907953,0.828843250210975,
2.84558448648495)) ;
#83385=CARTESIAN_POINT('Ctrl Pts',(-0.73031054313643,0.933891377908787,
2.83465339897623)) ;
#83386=CARTESIAN_POINT('Ctrl Pts',(-0.465241211512785,1.0898268629092,2.81284761224835)) ;
#83387=CARTESIAN_POINT('Ctrl Pts',(-0.320908177432949,1.14070369228232,
2.80218068264354)) ;
#83388=CARTESIAN_POINT('Ctrl Pts',(-0.0206957133140149,1.1848215140349,
2.78218119192395)) ;
#83389=CARTESIAN_POINT('Ctrl Pts',(0.132299481600214,1.17759557215243,2.77320929363418)) ;
#83390=CARTESIAN_POINT('Ctrl Pts',(0.430972390015288,1.10439932805368,2.75227340471072)) ;
#83391=CARTESIAN_POINT('Ctrl Pts',(0.573329363895275,1.03765163917832,2.74116513908726)) ;
#83392=CARTESIAN_POINT('Ctrl Pts',(0.819023758124217,0.856061032113319,
2.71963955224451)) ;
#83393=CARTESIAN_POINT('Ctrl Pts',(0.921414527925757,0.744754050742277,
2.70940572480726)) ;
#83394=CARTESIAN_POINT('Ctrl Pts',(1.08283436189426,0.48317272917608,2.69021927291669)) ;
#83395=CARTESIAN_POINT('Ctrl Pts',(1.1377932318867,0.33385005147702,2.67992246384761)) ;
#83396=CARTESIAN_POINT('Ctrl Pts',(1.18496375441424,0.0261162310963888,
2.65810183597765)) ;
#83397=CARTESIAN_POINT('Ctrl Pts',(1.17821842944344,-0.128942780920343,
2.6471069931134)) ;
#83398=CARTESIAN_POINT('Ctrl Pts',(1.10652469798646,-0.423082410616588,
2.62625029496606)) ;
#83399=CARTESIAN_POINT('Ctrl Pts',(1.04404604218016,-0.5597773011796,2.6171829082496)) ;
#83400=CARTESIAN_POINT('Ctrl Pts',(0.867294413301401,-0.808282445052659,
2.59751856586323)) ;
#83401=CARTESIAN_POINT('Ctrl Pts',(0.752501217679453,-0.916101525685282,
2.58664679342224)) ;
#83402=CARTESIAN_POINT('Ctrl Pts',(0.490970385683506,-1.07852996685889,
2.56482809816473)) ;
#83403=CARTESIAN_POINT('Ctrl Pts',(0.347540328044389,-1.13292001959081,
2.55409206134565)) ;
#83404=CARTESIAN_POINT('Ctrl Pts',(0.0488368145967983,-1.1838982236926,
2.53394200558513)) ;
#83405=CARTESIAN_POINT('Ctrl Pts',(-0.103503123360973,-1.18037661342213,
2.5250762093136)) ;
#83406=CARTESIAN_POINT('Ctrl Pts',(-0.403542762412943,-1.11476842320377,
2.50432541750764)) ;
#83407=CARTESIAN_POINT('Ctrl Pts',(-0.547856624339745,-1.05137942574436,
2.49321606210347)) ;
#83408=CARTESIAN_POINT('Ctrl Pts',(-0.798450359446747,-0.875341296917099,
2.47158647423735)) ;
#83409=CARTESIAN_POINT('Ctrl Pts',(-0.903692038123453,-0.76622942971059,
2.46125540411813)) ;
#83410=CARTESIAN_POINT('Ctrl Pts',(-1.07057692923121,-0.509331921162476,
2.44189941445632)) ;
#83411=CARTESIAN_POINT('Ctrl Pts',(-1.12870603757051,-0.362776011402504,
2.43197353059918)) ;
#83412=CARTESIAN_POINT('Ctrl Pts',(-1.16899556970882,-0.139924281782822,
2.41617167737358)) ;
#83413=CARTESIAN_POINT('Ctrl Pts',(-1.17524047358084,-0.0699492221345031,
2.41120992265036)) ;
#83414=CARTESIAN_POINT('Ctrl Pts',(-1.17524047358084,3.86728371726775E-15,
2.40625)) ;
#83415=CARTESIAN_POINT('Ctrl Pts',(-1.17524047358084,-1.97082727899222E-15,
2.34375)) ;
#83416=CARTESIAN_POINT('Ctrl Pts',(-1.17524047358084,-0.0159893943237037,
2.34488376756241)) ;
#83417=CARTESIAN_POINT('Ctrl Pts',(-1.17491416755614,-0.031990960902034,
2.34601839822863)) ;
#83418=CARTESIAN_POINT('Ctrl Pts',(-1.16789302334604,-0.203772957593621,
2.35819902569405)) ;
#83419=CARTESIAN_POINT('Ctrl Pts',(-1.13058937576196,-0.35677151180435,
2.36904776669998)) ;
#83420=CARTESIAN_POINT('Ctrl Pts',(-1.00137560583638,-0.632943406666202,
2.38863041815657)) ;
#83421=CARTESIAN_POINT('Ctrl Pts',(-0.91320344982542,-0.754615858669875,
2.39775958595751)) ;
#83422=CARTESIAN_POINT('Ctrl Pts',(-0.692462386878117,-0.961956822065874,
2.41866579313358)) ;
#83423=CARTESIAN_POINT('Ctrl Pts',(-0.560711658947958,-1.04425308901793,
2.42967400906333)) ;
#83424=CARTESIAN_POINT('Ctrl Pts',(-0.269955844015801,-1.15455632123922,
2.45143930909058)) ;
#83425=CARTESIAN_POINT('Ctrl Pts',(-0.113430199319369,-1.1802422369551,
2.46160718411688)) ;
#83426=CARTESIAN_POINT('Ctrl Pts',(0.193381317443829,-1.16888890246322,
2.48085028379429)) ;
#83427=CARTESIAN_POINT('Ctrl Pts',(0.340823271976921,-1.13468702620785,
2.4911169355698)) ;
#83428=CARTESIAN_POINT('Ctrl Pts',(0.620169972116385,-1.0103740433884,2.51267832641062)) ;
#83429=CARTESIAN_POINT('Ctrl Pts',(0.748523511011231,-0.919340734146067,
2.52378768966377)) ;
#83430=CARTESIAN_POINT('Ctrl Pts',(0.95930284898831,-0.695623131354465,
2.54466278354844)) ;
#83431=CARTESIAN_POINT('Ctrl Pts',(1.0408833027931,-0.566314536431026,2.55359406672777)) ;
#83432=CARTESIAN_POINT('Ctrl Pts',(1.15057221143423,-0.283558081993978,
2.5736436126713)) ;
#83433=CARTESIAN_POINT('Ctrl Pts',(1.17752841498523,-0.132793104251016,
2.5843339764119)) ;
#83434=CARTESIAN_POINT('Ctrl Pts',(1.17258071781568,0.174811322933465,2.60614542933716)) ;
#83435=CARTESIAN_POINT('Ctrl Pts',(1.13906811408573,0.328705172668025,2.61705765348718)) ;
#83436=CARTESIAN_POINT('Ctrl Pts',(1.01665018435854,0.608144314357815,2.6368719771633)) ;
#83437=CARTESIAN_POINT('Ctrl Pts',(0.931405988739206,0.732058253005227,
2.64584205896672)) ;
#83438=CARTESIAN_POINT('Ctrl Pts',(0.715945908723865,0.944548908495419,
2.66660654909468)) ;
#83439=CARTESIAN_POINT('Ctrl Pts',(0.586599278267999,1.02987735240299,2.67757463699525)) ;
#83440=CARTESIAN_POINT('Ctrl Pts',(0.300150572994426,1.14691880914246,2.69931434267748)) ;
#83441=CARTESIAN_POINT('Ctrl Pts',(0.14555775932464,1.17654992989502,2.70976521147525)) ;
#83442=CARTESIAN_POINT('Ctrl Pts',(-0.159812805757192,1.17389589616134,
2.72861140294063)) ;
#83443=CARTESIAN_POINT('Ctrl Pts',(-0.307753050386385,1.14404354082301,
2.73875444678115)) ;
#83444=CARTESIAN_POINT('Ctrl Pts',(-0.589810317143855,1.02832259298039,
2.76017766746428)) ;
#83445=CARTESIAN_POINT('Ctrl Pts',(-0.720434359265456,0.941436947348458,
2.77127940686414)) ;
#83446=CARTESIAN_POINT('Ctrl Pts',(-0.938352564545528,0.72385413908037,
2.79237538059191)) ;
#83447=CARTESIAN_POINT('Ctrl Pts',(-1.02427130333543,0.596096991198836,
2.80148226809044)) ;
#83448=CARTESIAN_POINT('Ctrl Pts',(-1.14204739775072,0.315947654532678,
2.82134694989839)) ;
#83449=CARTESIAN_POINT('Ctrl Pts',(-1.17319161754045,0.166433527854817,
2.8319486189496)) ;
#83450=CARTESIAN_POINT('Ctrl Pts',(-1.17520791360152,0.0101030964659361,
2.84303361494994)) ;
#83451=CARTESIAN_POINT('Ctrl Pts',(-1.17524047358084,0.00505079841659654,
2.84339186064256)) ;
#83452=CARTESIAN_POINT('Ctrl Pts',(-1.17524047358084,3.8300982969094E-15,
2.84375)) ;
#83453=CARTESIAN_POINT('Origin',(0.,0.,0.)) ;
#83454=CARTESIAN_POINT('',(-1.17524047358084,1.11632285683415E-15,3.40625)) ;
#83455=CARTESIAN_POINT('',(-1.17524047358084,3.12860208896725E-15,3.34375)) ;
#83456=CARTESIAN_POINT('',(-1.17524047358084,-1.4392544841992E-16,0.)) ;
#83457=CARTESIAN_POINT('Ctrl Pts',(-1.17524047358084,4.40619762898109E-15,
3.40625)) ;
#83458=CARTESIAN_POINT('Ctrl Pts',(-1.17524047358084,0.123092062062834,
3.39752185280871)) ;
#83459=CARTESIAN_POINT('Ctrl Pts',(-1.15590038001192,0.245621219624255,
3.38883361975373)) ;
#83460=CARTESIAN_POINT('Ctrl Pts',(-1.07142376848625,0.505704859705224,
3.37039174580484)) ;
#83461=CARTESIAN_POINT('Ctrl Pts',(-0.998235456447153,0.638130708170466,
3.3615918656591)) ;
#83462=CARTESIAN_POINT('Ctrl Pts',(-0.801629981464181,0.873587217586578,
3.3411709676216)) ;
#83463=CARTESIAN_POINT('Ctrl Pts',(-0.678101194694549,0.972589508504834,
3.33007535099264)) ;
#83464=CARTESIAN_POINT('Ctrl Pts',(-0.40481703820335,1.11357539151809,3.30829513023606)) ;
#83465=CARTESIAN_POINT('Ctrl Pts',(-0.258722442497593,1.15629084316166,
3.29780937856914)) ;
#83466=CARTESIAN_POINT('Ctrl Pts',(0.0448317785119429,1.18444011834994,
3.27817082298269)) ;
#83467=CARTESIAN_POINT('Ctrl Pts',(0.199477442066073,1.16838838479748,3.26875762215172)) ;
#83468=CARTESIAN_POINT('Ctrl Pts',(0.494594327588301,1.07727980730025,3.24740504116467)) ;
#83469=CARTESIAN_POINT('Ctrl Pts',(0.632038624059815,1.00283603509006,3.23632559671853)) ;
#83470=CARTESIAN_POINT('Ctrl Pts',(0.865846472707079,0.808553580002312,
3.21507996154768)) ;
#83471=CARTESIAN_POINT('Ctrl Pts',(0.961335813428651,0.692272716898223,
3.20533730967976)) ;
#83472=CARTESIAN_POINT('Ctrl Pts',(1.10699956285693,0.424327747474994,3.18633800872487)) ;
#83473=CARTESIAN_POINT('Ctrl Pts',(1.1534495275018,0.273917693398749,3.17567281172495)) ;
#83474=CARTESIAN_POINT('Ctrl Pts',(1.18468568302401,-0.0333087329033022,
3.15388816188743)) ;
#83475=CARTESIAN_POINT('Ctrl Pts',(1.17029961616188,-0.187073114751344,
3.14298511797822)) ;
#83476=CARTESIAN_POINT('Ctrl Pts',(1.08438834604793,-0.477121901343889,
3.12241849118191)) ;
#83477=CARTESIAN_POINT('Ctrl Pts',(1.01498853020898,-0.611013566767672,
3.11358203694755)) ;
#83478=CARTESIAN_POINT('Ctrl Pts',(0.824921751742507,-0.851706530322419,
3.09337701318501)) ;
#83479=CARTESIAN_POINT('Ctrl Pts',(0.703752672949174,-0.95426200692336,
3.08230032702302)) ;
#83480=CARTESIAN_POINT('Ctrl Pts',(0.433556743847305,-1.10275613565874,
3.06044355175743)) ;
#83481=CARTESIAN_POINT('Ctrl Pts',(0.288238670419427,-1.14933810079984,
3.04986840216459)) ;
#83482=CARTESIAN_POINT('Ctrl Pts',(-0.0137600089507247,-1.18506222361528,
3.03005681211611)) ;
#83483=CARTESIAN_POINT('Ctrl Pts',(-0.167602700280939,-1.17323466445312,
3.02088679462236)) ;
#83484=CARTESIAN_POINT('Ctrl Pts',(-0.464474152133334,-1.09066572219718,
2.99972923178039)) ;
#83485=CARTESIAN_POINT('Ctrl Pts',(-0.604310753179328,-1.01984881684707,
2.9886314674591)) ;
#83486=CARTESIAN_POINT('Ctrl Pts',(-0.843789761265557,-0.831582903172137,
2.96725088845622)) ;
#83487=CARTESIAN_POINT('Ctrl Pts',(-0.942598090975861,-0.717666170959262,
2.95714452491155)) ;
#83488=CARTESIAN_POINT('Ctrl Pts',(-1.09538049653803,-0.453420168177252,
2.93839400450008)) ;
#83489=CARTESIAN_POINT('Ctrl Pts',(-1.14581664734383,-0.30432730260374,
2.92782908029924)) ;
#83490=CARTESIAN_POINT('Ctrl Pts',(-1.17205840686471,-0.0999155125112192,
2.91333475660637)) ;
#83491=CARTESIAN_POINT('Ctrl Pts',(-1.17524047358084,-0.0499318976710169,
2.90979054473627)) ;
#83492=CARTESIAN_POINT('Ctrl Pts',(-1.17524047358084,-3.79291287655106E-15,
2.90625)) ;
#83493=CARTESIAN_POINT('Ctrl Pts',(-1.17524047358084,3.92047505570758E-15,
2.84375)) ;
#83494=CARTESIAN_POINT('Ctrl Pts',(-1.17524047358084,-0.152126593682685,
2.85453691248745)) ;
#83495=CARTESIAN_POINT('Ctrl Pts',(-1.14570195523154,-0.30289276073012,
2.86522736055861)) ;
#83496=CARTESIAN_POINT('Ctrl Pts',(-1.03177105272725,-0.582195023770608,
2.88503197851547)) ;
#83497=CARTESIAN_POINT('Ctrl Pts',(-0.949525466818209,-0.70845542441791,
2.89389257548998)) ;
#83498=CARTESIAN_POINT('Ctrl Pts',(-0.739493191168034,-0.926167026186486,
2.91450885883425)) ;
#83499=CARTESIAN_POINT('Ctrl Pts',(-0.612673416800777,-1.01452432539374,
2.92542916261959)) ;
#83500=CARTESIAN_POINT('Ctrl Pts',(-0.329814365549704,-1.13872553130698,
2.94720227586273)) ;
#83501=CARTESIAN_POINT('Ctrl Pts',(-0.176048087867001,-1.1723934496705,
2.95783835880861)) ;
#83502=CARTESIAN_POINT('Ctrl Pts',(0.128954723639944,-1.17762545861859,
2.97675336623768)) ;
#83503=CARTESIAN_POINT('Ctrl Pts',(0.27727628357567,-1.15177912605721,2.98660868402162)) ;
#83504=CARTESIAN_POINT('Ctrl Pts',(0.561718479925036,-1.04387119659527,
3.00790135698431)) ;
#83505=CARTESIAN_POINT('Ctrl Pts',(0.69429664646387,-0.960806993799944,
3.01898761018966)) ;
#83506=CARTESIAN_POINT('Ctrl Pts',(0.918663492912159,-0.748906987703286,
3.04027810339717)) ;
#83507=CARTESIAN_POINT('Ctrl Pts',(1.00857503310541,-0.62254998347992,3.04960655322784)) ;
#83508=CARTESIAN_POINT('Ctrl Pts',(1.13362015305737,-0.34480079881445,3.06930104632019)) ;
#83509=CARTESIAN_POINT('Ctrl Pts',(1.16848146009738,-0.196507126553218,
3.07981617603158)) ;
#83510=CARTESIAN_POINT('Ctrl Pts',(1.18045210584942,0.111025344536259,3.1016225267319)) ;
#83511=CARTESIAN_POINT('Ctrl Pts',(1.15511396970844,0.267432180839338,3.1127129404117)) ;
#83512=CARTESIAN_POINT('Ctrl Pts',(1.04700014446727,0.554458555440088,3.13306525560825)) ;
#83513=CARTESIAN_POINT('Ctrl Pts',(0.967898515283207,0.683233687816861,
3.14187012450672)) ;
#83514=CARTESIAN_POINT('Ctrl Pts',(0.763568577207577,0.906354575428315,
3.16232801996293)) ;
#83515=CARTESIAN_POINT('Ctrl Pts',(0.639459802292681,0.99779626387338,3.17319120070305)) ;
#83516=CARTESIAN_POINT('Ctrl Pts',(0.360385805909782,1.12942715567709,3.19499529266108)) ;
#83517=CARTESIAN_POINT('Ctrl Pts',(0.207552209614602,1.16723163352072,3.20572075830446)) ;
#83518=CARTESIAN_POINT('Ctrl Pts',(-0.0970329583631905,1.18066001159202,
3.22490071113121)) ;
#83519=CARTESIAN_POINT('Ctrl Pts',(-0.24576523956688,1.15888046266532,3.23442189518927)) ;
#83520=CARTESIAN_POINT('Ctrl Pts',(-0.532433326707437,1.0590459441693,3.25556502233849)) ;
#83521=CARTESIAN_POINT('Ctrl Pts',(-0.666905793461843,0.979949453657754,
3.26662692988576)) ;
#83522=CARTESIAN_POINT('Ctrl Pts',(-0.897847745957213,0.773991028819708,
3.28811053380133)) ;
#83523=CARTESIAN_POINT('Ctrl Pts',(-0.991908182729067,0.649069202730488,
3.29772614237813)) ;
#83524=CARTESIAN_POINT('Ctrl Pts',(-1.12433615609302,0.373813399472767,
3.31724383609312)) ;
#83525=CARTESIAN_POINT('Ctrl Pts',(-1.16292193409571,0.226849787736784,
3.32766465457238)) ;
#83526=CARTESIAN_POINT('Ctrl Pts',(-1.17440830644317,0.0510959910084378,
3.34012691234566)) ;
#83527=CARTESIAN_POINT('Ctrl Pts',(-1.17524047358084,0.025534463780991,
3.34193941567314)) ;
#83528=CARTESIAN_POINT('Ctrl Pts',(-1.17524047358084,3.8300982969094E-15,
3.34375)) ;
#83529=CARTESIAN_POINT('Origin',(0.,0.,0.)) ;
#83530=CARTESIAN_POINT('',(-1.17524047358084,-8.87282757919059E-16,3.90625)) ;
#83531=CARTESIAN_POINT('',(-1.17524047358084,-7.65852114600683E-16,3.84375)) ;
#83532=CARTESIAN_POINT('',(-1.17524047358084,-1.4392544841992E-16,0.)) ;
#83533=CARTESIAN_POINT('Ctrl Pts',(-1.17524047358084,-4.61436444609831E-15,
3.90625)) ;
#83534=CARTESIAN_POINT('Ctrl Pts',(-1.17524047358084,0.142946901613543,
3.89611399628934)) ;
#83535=CARTESIAN_POINT('Ctrl Pts',(-1.1491589245173,0.284799858846186,3.88605556141144)) ;
#83536=CARTESIAN_POINT('Ctrl Pts',(-1.04428959141748,0.559955417645546,
3.86654497577778)) ;
#83537=CARTESIAN_POINT('Ctrl Pts',(-0.963615569038733,0.68959302865811,
3.85764140732964)) ;
#83538=CARTESIAN_POINT('Ctrl Pts',(-0.754344875320265,0.914587047104567,
3.83681370207455)) ;
#83539=CARTESIAN_POINT('Ctrl Pts',(-0.626485163312983,1.0064855174128,3.82570399038894)) ;
#83540=CARTESIAN_POINT('Ctrl Pts',(-0.3477412494646,1.13259792905656,3.80411581877577)) ;
#83541=CARTESIAN_POINT('Ctrl Pts',(-0.200420290895077,1.16771393451668,
3.7938241877845)) ;
#83542=CARTESIAN_POINT('Ctrl Pts',(0.106052340955811,1.18088096493308,3.77453759594294)) ;
#83543=CARTESIAN_POINT('Ctrl Pts',(0.262369877053113,1.15625423255477,3.7644653429766)) ;
#83544=CARTESIAN_POINT('Ctrl Pts',(0.55362950714163,1.04804009767492,3.74274317114028)) ;
#83545=CARTESIAN_POINT('Ctrl Pts',(0.686020312601358,0.966577589927002,
3.73172520941794)) ;
#83546=CARTESIAN_POINT('Ctrl Pts',(0.908188754124144,0.760640735684068,
3.71078113116053)) ;
#83547=CARTESIAN_POINT('Ctrl Pts',(0.997154657087659,0.639567498828977,
3.70160011579944)) ;
#83548=CARTESIAN_POINT('Ctrl Pts',(1.12819030460119,0.364284748481715,3.6820805113344)) ;
#83549=CARTESIAN_POINT('Ctrl Pts',(1.16650968655984,0.21154349106954,3.67125001459453)) ;
#83550=CARTESIAN_POINT('Ctrl Pts',(1.18114170999137,-0.0961853876034204,
3.64942973712858)) ;
#83551=CARTESIAN_POINT('Ctrl Pts',(1.15877886932711,-0.248175324724643,
3.63865251461271)) ;
#83552=CARTESIAN_POINT('Ctrl Pts',(1.05785413346947,-0.533682336843727,
3.61840793357184)) ;
#83553=CARTESIAN_POINT('Ctrl Pts',(0.980856866002174,-0.664674810720661,
3.60958359921497)) ;
#83554=CARTESIAN_POINT('Ctrl Pts',(0.777764588059354,-0.894826428636171,
3.58895243992535)) ;
#83555=CARTESIAN_POINT('Ctrl Pts',(0.651976704282397,-0.990225850296007,
3.57784583258341)) ;
#83556=CARTESIAN_POINT('Ctrl Pts',(0.375807896236073,-1.12364601950554,
3.55615670491253)) ;
#83557=CARTESIAN_POINT('Ctrl Pts',(0.229038560342614,-1.16248604997788,
3.54576691718324)) ;
#83558=CARTESIAN_POINT('Ctrl Pts',(-0.0760266080667465,-1.18301413991114,
3.52630577732941)) ;
#83559=CARTESIAN_POINT('Ctrl Pts',(-0.231510867798561,-1.16263852629176,
3.51658667002208)) ;
#83560=CARTESIAN_POINT('Ctrl Pts',(-0.524732102727574,-1.06286326271082,
3.49504323011921)) ;
#83561=CARTESIAN_POINT('Ctrl Pts',(-0.65965851366554,-0.984821206774737,
3.48399083056172)) ;
#83562=CARTESIAN_POINT('Ctrl Pts',(-0.887579615110947,-0.78459783705296,
3.46289605921784)) ;
#83563=CARTESIAN_POINT('Ctrl Pts',(-0.979757190311564,-0.665913011896129,
3.45346820958247)) ;
#83564=CARTESIAN_POINT('Ctrl Pts',(-1.11807259121496,-0.394238123750088,
3.43420442951269)) ;
#83565=CARTESIAN_POINT('Ctrl Pts',(-1.16044512750511,-0.242598028979702,
3.42345201343422)) ;
#83566=CARTESIAN_POINT('Ctrl Pts',(-1.17416414971479,-0.0581108873613505,
3.41037049623514)) ;
#83567=CARTESIAN_POINT('Ctrl Pts',(-1.17524047358084,-0.0290397786505206,
3.40830913734985)) ;
#83568=CARTESIAN_POINT('Ctrl Pts',(-1.17524047358084,3.86728371726775E-15,
3.40625)) ;
#83569=CARTESIAN_POINT('Ctrl Pts',(-1.17524047358084,3.22658566531686E-15,
3.34375)) ;
#83570=CARTESIAN_POINT('Ctrl Pts',(-1.17524047358084,-0.130483209475118,
3.35300223478431)) ;
#83571=CARTESIAN_POINT('Ctrl Pts',(-1.15350790037109,-0.260259712787548,
3.36220435881975)) ;
#83572=CARTESIAN_POINT('Ctrl Pts',(-1.06162271654697,-0.526085279377952,
3.38105337827336)) ;
#83573=CARTESIAN_POINT('Ctrl Pts',(-0.985684775170123,-0.657445115209627,
3.38986361039039)) ;
#83574=CARTESIAN_POINT('Ctrl Pts',(-0.787094018328788,-0.88593423012538,
3.41015939979644)) ;
#83575=CARTESIAN_POINT('Ctrl Pts',(-0.665766803792927,-0.980377255471268,
3.42095817999328)) ;
#83576=CARTESIAN_POINT('Ctrl Pts',(-0.390670514530027,-1.11931648336967,
3.44277711803581)) ;
#83577=CARTESIAN_POINT('Ctrl Pts',(-0.238883506616201,-1.16122754663595,
3.45358390892082)) ;
#83578=CARTESIAN_POINT('Ctrl Pts',(0.0652067499452988,-1.1828388016687,
3.47302358395648)) ;
#83579=CARTESIAN_POINT('Ctrl Pts',(0.21439210539306,-1.1650817465961,3.48227548530999)) ;
#83580=CARTESIAN_POINT('Ctrl Pts',(0.503181454485975,-1.073193310475,3.50326715590652)) ;
#83581=CARTESIAN_POINT('Ctrl Pts',(0.639406917105912,-0.998044366447435,
3.51429675557723)) ;
#83582=CARTESIAN_POINT('Ctrl Pts',(0.876777484238287,-0.798048737993809,
3.53596372234866)) ;
#83583=CARTESIAN_POINT('Ctrl Pts',(0.974975375041977,-0.674546337411974,
3.54591962311291)) ;
#83584=CARTESIAN_POINT('Ctrl Pts',(1.11460032262829,-0.401776023878272,
3.56526107702989)) ;
#83585=CARTESIAN_POINT('Ctrl Pts',(1.15676310438279,-0.256194006053251,
3.57558393017482)) ;
#83586=CARTESIAN_POINT('Ctrl Pts',(1.18455103405537,0.0487251835052672,
3.59720497968292)) ;
#83587=CARTESIAN_POINT('Ctrl Pts',(1.16762799416042,0.205401534263999,3.60831450395198)) ;
#83588=CARTESIAN_POINT('Ctrl Pts',(1.07505395344607,0.498276653639495,3.62908153886662)) ;
#83589=CARTESIAN_POINT('Ctrl Pts',(1.00218359127923,0.632176154534591,3.63795457738639)) ;
#83590=CARTESIAN_POINT('Ctrl Pts',(0.809134037081688,0.865785758313647,
3.65809163489348)) ;
#83591=CARTESIAN_POINT('Ctrl Pts',(0.690539621904492,0.963028817488338,
3.66882187190168)) ;
#83592=CARTESIAN_POINT('Ctrl Pts',(0.419437138478927,1.10886120636148,3.69063994793443)) ;
#83593=CARTESIAN_POINT('Ctrl Pts',(0.268760300407346,1.15468110020436,3.70151714852314)) ;
#83594=CARTESIAN_POINT('Ctrl Pts',(-0.0347798880424834,1.18413544278438,
3.72120111191882)) ;
#83595=CARTESIAN_POINT('Ctrl Pts',(-0.18444046516192,1.17020530514855,3.7302545754592)) ;
#83596=CARTESIAN_POINT('Ctrl Pts',(-0.475174156686655,1.08582907581352,
3.75109930779784)) ;
#83597=CARTESIAN_POINT('Ctrl Pts',(-0.612953208086329,1.01444551153309,
3.76209081295829)) ;
#83598=CARTESIAN_POINT('Ctrl Pts',(-0.854990498523108,0.821285178496173,
3.7838020155861)) ;
#83599=CARTESIAN_POINT('Ctrl Pts',(-0.956258019499858,0.700744194359125,
3.79406199925237)) ;
#83600=CARTESIAN_POINT('Ctrl Pts',(-1.10294642971048,0.432602098744818,
3.81307527792753)) ;
#83601=CARTESIAN_POINT('Ctrl Pts',(-1.14903783149158,0.288659253487398,
3.82328190148623)) ;
#83602=CARTESIAN_POINT('Ctrl Pts',(-1.17245792453858,0.093437291591936,
3.83712459767508)) ;
#83603=CARTESIAN_POINT('Ctrl Pts',(-1.17524047358084,0.0466922986522145,
3.84043916704695)) ;
#83604=CARTESIAN_POINT('Ctrl Pts',(-1.17524047358084,-3.71854203583437E-15,
3.84375)) ;
#83605=CARTESIAN_POINT('Origin',(0.,0.,0.)) ;
#83606=CARTESIAN_POINT('',(-1.17524047358084,9.68871361376125E-16,4.40624999999999)) ;
#83607=CARTESIAN_POINT('',(-1.17524047358084,-2.37914494725911E-15,4.34374999999999)) ;
#83608=CARTESIAN_POINT('',(-1.17524047358084,-1.4392544841992E-16,0.)) ;
#83609=CARTESIAN_POINT('Ctrl Pts',(-1.17524047358084,1.90683135537553E-30,
4.40624999999999)) ;
#83610=CARTESIAN_POINT('Ctrl Pts',(-1.17524047358084,0.0128716194911538,
4.40533730597549)) ;
#83611=CARTESIAN_POINT('Ctrl Pts',(-1.17502901344671,0.0257515459259134,
4.40442402292659)) ;
#83612=CARTESIAN_POINT('Ctrl Pts',(-1.16947972214485,0.194466094770272,
4.39246090043968)) ;
#83613=CARTESIAN_POINT('Ctrl Pts',(-1.1333934290327,0.347763277250189,4.38159098445752)) ;
#83614=CARTESIAN_POINT('Ctrl Pts',(-1.00636237929119,0.624993082444022,
4.36193331925155)) ;
#83615=CARTESIAN_POINT('Ctrl Pts',(-0.919136169074253,0.747384332887866,
4.35286111314413)) ;
#83616=CARTESIAN_POINT('Ctrl Pts',(-0.700098714093276,0.956394260739641,
4.33200034954346)) ;
#83617=CARTESIAN_POINT('Ctrl Pts',(-0.569117427224042,1.03967776490008,
4.32100438195105)) ;
#83618=CARTESIAN_POINT('Ctrl Pts',(-0.278971950167976,1.1524718093816,4.2991882527502)) ;
#83619=CARTESIAN_POINT('Ctrl Pts',(-0.122197490070545,1.1794242883068,4.28890219547748)) ;
#83620=CARTESIAN_POINT('Ctrl Pts',(0.185013179439947,1.1702291438196,4.2697111006592)) ;
#83621=CARTESIAN_POINT('Ctrl Pts',(0.332591497936668,1.13711307177577,4.25947457090684)) ;
#83622=CARTESIAN_POINT('Ctrl Pts',(0.612639221476556,1.01494031829922,4.23794601097797)) ;
#83623=CARTESIAN_POINT('Ctrl Pts',(0.741571806097502,0.924937605955755,
4.22683762838516)) ;
#83624=CARTESIAN_POINT('Ctrl Pts',(0.954139258068047,0.70274177553902,4.2059066830972)) ;
#83625=CARTESIAN_POINT('Ctrl Pts',(1.03679863747558,0.573822476343852,4.19693830232643)) ;
#83626=CARTESIAN_POINT('Ctrl Pts',(1.14851756853483,0.291714221415981,4.17693471857275)) ;
#83627=CARTESIAN_POINT('Ctrl Pts',(1.17652988979183,0.141252473189452,4.16626585607121)) ;
#83628=CARTESIAN_POINT('Ctrl Pts',(1.17382180480569,-0.166279287440103,
4.1444595557478)) ;
#83629=CARTESIAN_POINT('Ctrl Pts',(1.14142759470212,-0.320417855077137,
4.13352997926948)) ;
#83630=CARTESIAN_POINT('Ctrl Pts',(1.02101421940899,-0.600805711523604,
4.11364838462641)) ;
#83631=CARTESIAN_POINT('Ctrl Pts',(0.936624318794625,-0.725382913496972,
4.10471505227448)) ;
#83632=CARTESIAN_POINT('Ctrl Pts',(0.722708975269278,-0.93936673538121,
4.08399248249237)) ;
#83633=CARTESIAN_POINT('Ctrl Pts',(0.594075891314688,-1.02556630487159,
4.07303732716529)) ;
#83634=CARTESIAN_POINT('Ctrl Pts',(0.308605328998943,-1.14467192257802,
4.0512845047467)) ;
#83635=CARTESIAN_POINT('Ctrl Pts',(0.154247834183575,-1.17543888794573,
4.04072903521798)) ;
#83636=CARTESIAN_POINT('Ctrl Pts',(-0.150998891746284,-1.17504814395324,
4.02197069050609)) ;
#83637=CARTESIAN_POINT('Ctrl Pts',(-0.299048572172097,-1.14633511102661,
4.01186131970491)) ;
#83638=CARTESIAN_POINT('Ctrl Pts',(-0.580235062583513,-1.03349017525507,
3.99059353674741)) ;
#83639=CARTESIAN_POINT('Ctrl Pts',(-0.710182219725325,-0.948904884149489,
3.97961491944388)) ;
#83640=CARTESIAN_POINT('Ctrl Pts',(-0.926950131953632,-0.737683011794045,
3.95881510148556)) ;
#83641=CARTESIAN_POINT('Ctrl Pts',(-1.01291829531872,-0.614327874904145,
3.94981043782202)) ;
#83642=CARTESIAN_POINT('Ctrl Pts',(-1.13702740411321,-0.335694479443153,
3.93005324757567)) ;
#83643=CARTESIAN_POINT('Ctrl Pts',(-1.17148359162314,-0.182013941692096,
3.91915614883959)) ;
#83644=CARTESIAN_POINT('Ctrl Pts',(-1.17514374548819,-0.0174150947011532,
3.90748486037486)) ;
#83645=CARTESIAN_POINT('Ctrl Pts',(-1.17524047358084,-0.00870551871022769,
3.90686728634167)) ;
#83646=CARTESIAN_POINT('Ctrl Pts',(-1.17524047358084,-3.79291287655106E-15,
3.90625)) ;
#83647=CARTESIAN_POINT('Ctrl Pts',(-1.17524047358084,-3.12250225675825E-15,
3.84375)) ;
#83648=CARTESIAN_POINT('Ctrl Pts',(-1.17524047358084,-0.108258895333412,
3.85142636480696)) ;
#83649=CARTESIAN_POINT('Ctrl Pts',(-1.16028088637367,-0.216234520909998,
3.85908264367101)) ;
#83650=CARTESIAN_POINT('Ctrl Pts',(-1.08910194938674,-0.467076363318089,
3.87686920509162)) ;
#83651=CARTESIAN_POINT('Ctrl Pts',(-1.01964084687618,-0.603846833868942,
3.88587818764472)) ;
#83652=CARTESIAN_POINT('Ctrl Pts',(-0.832725477793128,-0.843046352796263,
3.90583674249475)) ;
#83653=CARTESIAN_POINT('Ctrl Pts',(-0.71720215641018,-0.943273281852801,
3.91648418011504)) ;
#83654=CARTESIAN_POINT('Ctrl Pts',(-0.449321885193019,-1.09731938696322,
3.93839559452685)) ;
#83655=CARTESIAN_POINT('Ctrl Pts',(-0.298349998552315,-1.14760859635405,
3.94944936729988)) ;
#83656=CARTESIAN_POINT('Ctrl Pts',(0.00616172932227222,-1.18465574205611,
3.96946218391667)) ;
#83657=CARTESIAN_POINT('Ctrl Pts',(0.156307571630098,-1.17431790910372,
3.97838119273087)) ;
#83658=CARTESIAN_POINT('Ctrl Pts',(0.448801251791293,-1.0969418842604,3.99908581846858)) ;
#83659=CARTESIAN_POINT('Ctrl Pts',(0.58793583219071,-1.0290916116714,4.0100352951173)) ;
#83660=CARTESIAN_POINT('Ctrl Pts',(0.834258197193588,-0.842306532240701,
4.03178360764163)) ;
#83661=CARTESIAN_POINT('Ctrl Pts',(0.93849259450696,-0.724379572815127,
4.04236535091666)) ;
#83662=CARTESIAN_POINT('Ctrl Pts',(1.09158794225778,-0.460347016038917,
4.06112752092142)) ;
#83663=CARTESIAN_POINT('Ctrl Pts',(1.14123666714252,-0.317992959561192,
4.07120192248525)) ;
#83664=CARTESIAN_POINT('Ctrl Pts',(1.18532600445379,-0.0165202074694624,
4.09257859381825)) ;
#83665=CARTESIAN_POINT('Ctrl Pts',(1.17715057099471,0.139970764168848,4.10367497298973)) ;
#83666=CARTESIAN_POINT('Ctrl Pts',(1.10197749426139,0.434810365215498,4.12458130498915)) ;
#83667=CARTESIAN_POINT('Ctrl Pts',(1.03802033559752,0.57089215321861,4.13358117941572)) ;
#83668=CARTESIAN_POINT('Ctrl Pts',(0.858565778431052,0.817549425241584,
4.15334598837812)) ;
#83669=CARTESIAN_POINT('Ctrl Pts',(0.74261499275234,0.924135312990195,4.16424512443554)) ;
#83670=CARTESIAN_POINT('Ctrl Pts',(0.479479286439668,1.08366531170208,4.18605961067483)) ;
#83671=CARTESIAN_POINT('Ctrl Pts',(0.33563429935706,1.1364834116783,4.19676539574625)) ;
#83672=CARTESIAN_POINT('Ctrl Pts',(0.0362501517362821,1.18439204189214,
4.21684841980273)) ;
#83673=CARTESIAN_POINT('Ctrl Pts',(-0.116378575296644,1.17921896890736,
4.22575548506318)) ;
#83674=CARTESIAN_POINT('Ctrl Pts',(-0.415818103686213,1.11022378891706,
4.24658950691394)) ;
#83675=CARTESIAN_POINT('Ctrl Pts',(-0.559267897367201,1.04532872852346,
4.25769919745631)) ;
#83676=CARTESIAN_POINT('Ctrl Pts',(-0.807689818907504,0.86679618491432,
4.279283855629)) ;
#83677=CARTESIAN_POINT('Ctrl Pts',(-0.911664654473727,0.75669555126946,
4.28957218732499)) ;
#83678=CARTESIAN_POINT('Ctrl Pts',(-1.0761179660709,0.49770643017,4.30885301482668)) ;
#83679=CARTESIAN_POINT('Ctrl Pts',(-1.13284157540801,0.349924032353012,
4.31893777077122)) ;
#83680=CARTESIAN_POINT('Ctrl Pts',(-1.16979960242193,0.130620444338645,
4.33448803423816)) ;
#83681=CARTESIAN_POINT('Ctrl Pts',(-1.17524047358084,0.065291328614083,
4.33912035681335)) ;
#83682=CARTESIAN_POINT('Ctrl Pts',(-1.17524047358084,-3.71854203583437E-15,
4.34374999999999)) ;
#83683=CARTESIAN_POINT('Origin',(0.,0.,0.)) ;
#83684=CARTESIAN_POINT('',(-1.17524047358084,-2.89956199005216E-15,4.90624999999999)) ;
#83685=CARTESIAN_POINT('',(-1.17524047358084,-1.37300533119257E-15,4.84374999999999)) ;
#83686=CARTESIAN_POINT('',(-1.17524047358084,-1.4392544841992E-16,0.)) ;
#83687=CARTESIAN_POINT('Ctrl Pts',(-1.17524047358084,-7.58582575310211E-15,
4.90624999999999)) ;
#83688=CARTESIAN_POINT('Ctrl Pts',(-1.17524047358084,0.0336064111452372,
4.90386705427522)) ;
#83689=CARTESIAN_POINT('Ctrl Pts',(-1.17379902465408,0.0672506944046495,
4.90148142313449)) ;
#83690=CARTESIAN_POINT('Ctrl Pts',(-1.15753280327446,0.256125621332427,
4.88808877916264)) ;
#83691=CARTESIAN_POINT('Ctrl Pts',(-1.11339784493106,0.407249272087715,
4.87737298282475)) ;
#83692=CARTESIAN_POINT('Ctrl Pts',(-0.97191001713831,0.677324635980341,
4.85822262097939)) ;
#83693=CARTESIAN_POINT('Ctrl Pts',(-0.878311667224519,0.794970991004644,
4.84866705058936)) ;
#83694=CARTESIAN_POINT('Ctrl Pts',(-0.647858954275702,0.992651478855324,
4.82750697353716)) ;
#83695=CARTESIAN_POINT('Ctrl Pts',(-0.511839952604746,1.06915809467643,
4.81644191761435)) ;
#83696=CARTESIAN_POINT('Ctrl Pts',(-0.217789837788617,1.16521007102824,
4.79497958257196)) ;
#83697=CARTESIAN_POINT('Ctrl Pts',(-0.0626683588253212,1.18372319582663,
4.78539906234046)) ;
#83698=CARTESIAN_POINT('Ctrl Pts',(0.241755923350193,1.15992886988465,4.76586147754698)) ;
#83699=CARTESIAN_POINT('Ctrl Pts',(0.388249083467121,1.11943010005734,4.75542984062084)) ;
#83700=CARTESIAN_POINT('Ctrl Pts',(0.66320889718637,0.982766788481499,4.73369997296271)) ;
#83701=CARTESIAN_POINT('Ctrl Pts',(0.78804277392843,0.885820221574825,4.7225970968929)) ;
#83702=CARTESIAN_POINT('Ctrl Pts',(0.988365812490969,0.653391146675087,
4.70205524579088)) ;
#83703=CARTESIAN_POINT('Ctrl Pts',(1.06373156815355,0.521787684346926,4.69324864666541)) ;
#83704=CARTESIAN_POINT('Ctrl Pts',(1.16148270650949,0.235303024827453,4.6729347431169)) ;
#83705=CARTESIAN_POINT('Ctrl Pts',(1.18216976652638,0.0829036082278015,
4.66212848544556)) ;
#83706=CARTESIAN_POINT('Ctrl Pts',(1.16402721483696,-0.224794388844498,
4.64031039771591)) ;
#83707=CARTESIAN_POINT('Ctrl Pts',(1.1239771417896,-0.377080091451739,4.62951220321653)) ;
#83708=CARTESIAN_POINT('Ctrl Pts',(0.98983529323125,-0.650834129120896,
4.61010099590598)) ;
#83709=CARTESIAN_POINT('Ctrl Pts',(0.899507015930689,-0.770887185367275,
4.6008224685601)) ;
#83710=CARTESIAN_POINT('Ctrl Pts',(0.67489360591369,-0.974406537661227,
4.57981395995323)) ;
#83711=CARTESIAN_POINT('Ctrl Pts',(0.541416377616256,-1.05442702615244,
4.56878040850312)) ;
#83712=CARTESIAN_POINT('Ctrl Pts',(0.249309634015072,-1.15905825563868,
4.54713324478207)) ;
#83713=CARTESIAN_POINT('Ctrl Pts',(0.0933474980749243,-1.18187483724993,
4.53721746569737)) ;
#83714=CARTESIAN_POINT('Ctrl Pts',(-0.212535149674799,-1.16558942260184,
4.51785654503261)) ;
#83715=CARTESIAN_POINT('Ctrl Pts',(-0.359634330439741,-1.12889840454129,
4.50752269281791)) ;
#83716=CARTESIAN_POINT('Ctrl Pts',(-0.637312589759921,-0.999690819910851,
4.48589022512135)) ;
#83717=CARTESIAN_POINT('Ctrl Pts',(-0.764307844796796,-0.906307054685691,
4.47478093847204)) ;
#83718=CARTESIAN_POINT('Ctrl Pts',(-0.970971990849064,-0.679123640590144,
4.45403567298827)) ;
#83719=CARTESIAN_POINT('Ctrl Pts',(-1.05008805783472,-0.548916067448755,
4.44517225178508)) ;
#83720=CARTESIAN_POINT('Ctrl Pts',(-1.15062478854163,-0.276774697313999,
4.4258753946558)) ;
#83721=CARTESIAN_POINT('Ctrl Pts',(-1.17524047358084,-0.138870815676883,
4.41609697875304)) ;
#83722=CARTESIAN_POINT('Ctrl Pts',(-1.17524047358084,4.85722573273506E-16,
4.40624999999999)) ;
#83723=CARTESIAN_POINT('Ctrl Pts',(-1.17524047358084,-3.71854203583437E-15,
4.34374999999999)) ;
#83724=CARTESIAN_POINT('Ctrl Pts',(-1.17524047358084,-0.0879429296864962,
4.3499858110009)) ;
#83725=CARTESIAN_POINT('Ctrl Pts',(-1.16536913559801,-0.175817305099971,
4.35621676099149)) ;
#83726=CARTESIAN_POINT('Ctrl Pts',(-1.11247180243315,-0.407170807428106,
4.37262145344443)) ;
#83727=CARTESIAN_POINT('Ctrl Pts',(-1.05198089044729,-0.544702587945109,
4.38179537625786)) ;
#83728=CARTESIAN_POINT('Ctrl Pts',(-0.878873963396262,-0.795674243273616,
4.40132335303172)) ;
#83729=CARTESIAN_POINT('Ctrl Pts',(-0.765658722969771,-0.905131200820453,
4.41215629577215)) ;
#83730=CARTESIAN_POINT('Ctrl Pts',(-0.506336955375604,-1.07143189443511,
4.4339766233431)) ;
#83731=CARTESIAN_POINT('Ctrl Pts',(-0.363491689914812,-1.12793145483258,
4.44475153936484)) ;
#83732=CARTESIAN_POINT('Ctrl Pts',(-0.0657158903894447,-1.18303025212162,
4.4649907167986)) ;
#83733=CARTESIAN_POINT('Ctrl Pts',(0.0862480431561069,-1.18171108530207,
4.47381688433456)) ;
#83734=CARTESIAN_POINT('Ctrl Pts',(0.387064954368621,-1.12062857541088,
4.49445495433573)) ;
#83735=CARTESIAN_POINT('Ctrl Pts',(0.532509355951195,-1.05926876454441,
4.50556179130252)) ;
#83736=CARTESIAN_POINT('Ctrl Pts',(0.785966327506931,-0.886603103199955,
4.52724763728332)) ;
#83737=CARTESIAN_POINT('Ctrl Pts',(0.892885955994929,-0.778834630601013,
4.53763411803812)) ;
#83738=CARTESIAN_POINT('Ctrl Pts',(1.06300065633516,-0.524734283547396,
4.55708927294375)) ;
#83739=CARTESIAN_POINT('Ctrl Pts',(1.12298496714204,-0.379795602326755,
4.56681965319974)) ;
#83740=CARTESIAN_POINT('Ctrl Pts',(1.18290300104997,-0.0758824019829007,
4.58836937055374)) ;
#83741=CARTESIAN_POINT('Ctrl Pts',(1.18263352169829,0.0799734538844092,
4.59942071560261)) ;
#83742=CARTESIAN_POINT('Ctrl Pts',(1.12292510957113,0.377398239203149,4.62051035583687)) ;
#83743=CARTESIAN_POINT('Ctrl Pts',(1.06610382786025,0.516513514215964,4.6299287115176)) ;
#83744=CARTESIAN_POINT('Ctrl Pts',(0.899751763152944,0.771982532616731,
4.64920133623562)) ;
#83745=CARTESIAN_POINT('Ctrl Pts',(0.789510436318703,0.884398262703763,
4.65995655740372)) ;
#83746=CARTESIAN_POINT('Ctrl Pts',(0.534415846616042,1.05776313639872,4.6817677553963)) ;
#83747=CARTESIAN_POINT('Ctrl Pts',(0.392729941126095,1.11813973013556,4.69260893313949)) ;
#83748=CARTESIAN_POINT('Ctrl Pts',(0.0966996952851368,1.1808222055235,4.71300978991082)) ;
#83749=CARTESIAN_POINT('Ctrl Pts',(-0.0546006167114424,1.18351564863586,
4.72180951098071)) ;
#83750=CARTESIAN_POINT('Ctrl Pts',(-0.356770105579204,1.13069703761872,
4.74223765353203)) ;
#83751=CARTESIAN_POINT('Ctrl Pts',(-0.504206792548302,1.07309022025021,
4.75333377446551)) ;
#83752=CARTESIAN_POINT('Ctrl Pts',(-0.762774838742479,0.906695985440486,
4.77511113414352)) ;
#83753=CARTESIAN_POINT('Ctrl Pts',(-0.872713039004967,0.801444885450279,
4.78559372810281)) ;
#83754=CARTESIAN_POINT('Ctrl Pts',(-1.04867033163315,0.552459444916847,
4.80522632045929)) ;
#83755=CARTESIAN_POINT('Ctrl Pts',(-1.11198000105894,0.410409566754714,
4.81464889431279)) ;
#83756=CARTESIAN_POINT('Ctrl Pts',(-1.16550862440625,0.17457751663472,4.83137114927687)) ;
#83757=CARTESIAN_POINT('Ctrl Pts',(-1.17524047358084,0.0873194511436137,
4.83755839828765)) ;
#83758=CARTESIAN_POINT('Ctrl Pts',(-1.17524047358084,0.,4.84374999999999)) ;
#83759=CARTESIAN_POINT('Origin',(0.,0.,0.)) ;
#83760=CARTESIAN_POINT('',(-1.17524047358084,-3.06002391158001E-15,5.40624999999999)) ;
#83761=CARTESIAN_POINT('',(-1.17524047358084,4.2243346644343E-16,5.34374999999999)) ;
#83762=CARTESIAN_POINT('',(-1.17524047358084,-1.4392544841992E-16,0.)) ;
#83763=CARTESIAN_POINT('Ctrl Pts',(-1.17524047358084,-1.50972806654875E-14,
5.40625)) ;
#83764=CARTESIAN_POINT('Ctrl Pts',(-1.17524047358084,0.054156322179546,
5.40240991199269)) ;
#83765=CARTESIAN_POINT('Ctrl Pts',(-1.17149719619506,0.108363865139321,
5.39856619204925)) ;
#83766=CARTESIAN_POINT('Ctrl Pts',(-1.14245991904882,0.316700694650271,
5.38379355372584)) ;
#83767=CARTESIAN_POINT('Ctrl Pts',(-1.09041023303251,0.465258281745517,
5.37338107781476)) ;
#83768=CARTESIAN_POINT('Ctrl Pts',(-0.934665993484623,0.727999724774848,
5.3545020203338)) ;
#83769=CARTESIAN_POINT('Ctrl Pts',(-0.834492771222264,0.840941110532362,
5.34434642158922)) ;
#83770=CARTESIAN_POINT('Ctrl Pts',(-0.592638212946615,1.02670227320812,
5.32290876835838)) ;
#83771=CARTESIAN_POINT('Ctrl Pts',(-0.451833533797191,1.09598812006894,
5.3118058383577)) ;
#83772=CARTESIAN_POINT('Ctrl Pts',(-0.154264542505518,1.1750060408126,5.29073133822417)) ;
#83773=CARTESIAN_POINT('Ctrl Pts',(-0.000747491529236952,1.18508632964804,
5.28164497410758)) ;
#83774=CARTESIAN_POINT('Ctrl Pts',(0.300584332058249,1.14619222074689,5.26176194626849)) ;
#83775=CARTESIAN_POINT('Ctrl Pts',(0.445545839603115,1.09798914509645,5.25115121813143)) ;
#83776=CARTESIAN_POINT('Ctrl Pts',(0.714383924244483,0.94635903855499,5.22926664280317)) ;
#83777=CARTESIAN_POINT('Ctrl Pts',(0.834531897528456,0.842326220849121,
5.21820028309222)) ;
#83778=CARTESIAN_POINT('Ctrl Pts',(1.02183521132734,0.599452713433834,5.19808764883802)) ;
#83779=CARTESIAN_POINT('Ctrl Pts',(1.08964832106457,0.464933155992749,5.18921723567391)) ;
#83780=CARTESIAN_POINT('Ctrl Pts',(1.17234517244266,0.173941348274813,5.16858374163167)) ;
#83781=CARTESIAN_POINT('Ctrl Pts',(1.18500959824535,0.0198512012903376,
5.15765759853952)) ;
#83782=CARTESIAN_POINT('Ctrl Pts',(1.15022464875196,-0.287150503762624,
5.13588888311813)) ;
#83783=CARTESIAN_POINT('Ctrl Pts',(1.10205516619926,-0.437004301439408,
5.12526312885439)) ;
#83784=CARTESIAN_POINT('Ctrl Pts',(0.953281888395458,-0.70334467726024,
5.10637760557866)) ;
#83785=CARTESIAN_POINT('Ctrl Pts',(0.856368474205286,-0.818609396179132,
5.09648150034986)) ;
#83786=CARTESIAN_POINT('Ctrl Pts',(0.620045591679404,-1.01032312726072,
5.07517249366432)) ;
#83787=CARTESIAN_POINT('Ctrl Pts',(0.481550303729629,-1.08319994735702,
5.06408406458446)) ;
#83788=CARTESIAN_POINT('Ctrl Pts',(0.185657123836112,-1.17059619417369,
5.0428154291615)) ;
#83789=CARTESIAN_POINT('Ctrl Pts',(0.0313637348566941,-1.18480750453488,
5.03351516099886)) ;
#83790=CARTESIAN_POINT('Ctrl Pts',(-0.27152252717408,-1.15337354604257,
5.01380116892149)) ;
#83791=CARTESIAN_POINT('Ctrl Pts',(-0.417293433366323,-1.10898293008958,
5.00327590343977)) ;
#83792=CARTESIAN_POINT('Ctrl Pts',(-0.689265529178068,-0.964739169361853,
4.98146074933774)) ;
#83793=CARTESIAN_POINT('Ctrl Pts',(-0.811785020904053,-0.864192363580381,
4.97037235234583)) ;
#83794=CARTESIAN_POINT('Ctrl Pts',(-1.00556637310702,-0.626460634302472,
4.9500442120722)) ;
#83795=CARTESIAN_POINT('Ctrl Pts',(-1.07711222144063,-0.493404919958927,
4.9412360965373)) ;
#83796=CARTESIAN_POINT('Ctrl Pts',(-1.15727203498349,-0.236821733408562,
4.92304243090614)) ;
#83797=CARTESIAN_POINT('Ctrl Pts',(-1.17524047358084,-0.118646891707225,
4.91466295138983)) ;
#83798=CARTESIAN_POINT('Ctrl Pts',(-1.17524047358084,-5.27355936696949E-15,
4.90624999999999)) ;
#83799=CARTESIAN_POINT('Ctrl Pts',(-1.17524047358084,0.,4.84374999999999)) ;
#83800=CARTESIAN_POINT('Ctrl Pts',(-1.17524047358084,-0.0667390125405247,
4.84848229479701)) ;
#83801=CARTESIAN_POINT('Ctrl Pts',(-1.16955564460581,-0.133513884598031,
4.8532171323018)) ;
#83802=CARTESIAN_POINT('Ctrl Pts',(-1.13283143136164,-0.346611060159256,
4.86832731473904)) ;
#83803=CARTESIAN_POINT('Ctrl Pts',(-1.07974815915801,-0.487390792329828,
4.87805833554934)) ;
#83804=CARTESIAN_POINT('Ctrl Pts',(-0.920300351277828,-0.747361772037844,
4.89706659726841)) ;
#83805=CARTESIAN_POINT('Ctrl Pts',(-0.813160901989492,-0.86269717468872,
4.9077348526552)) ;
#83806=CARTESIAN_POINT('Ctrl Pts',(-0.562558857002137,-1.04312657461033,
4.92952063778222)) ;
#83807=CARTESIAN_POINT('Ctrl Pts',(-0.422157008304024,-1.10741905073089,
4.94042179724895)) ;
#83808=CARTESIAN_POINT('Ctrl Pts',(-0.127949644136201,-1.17778450934342,
4.96098310556376)) ;
#83809=CARTESIAN_POINT('Ctrl Pts',(0.022723984492035,-1.18449444420266,
4.96981733918665)) ;
#83810=CARTESIAN_POINT('Ctrl Pts',(0.326162761302332,-1.13996195065271,
4.99002965192844)) ;
#83811=CARTESIAN_POINT('Ctrl Pts',(0.475501214059982,-1.08617584423663,
5.00110709739386)) ;
#83812=CARTESIAN_POINT('Ctrl Pts',(0.739036042438915,-0.92620970159878,
5.02296155572285)) ;
#83813=CARTESIAN_POINT('Ctrl Pts',(0.85193851793381,-0.823563331821022,
5.03353383150877)) ;
#83814=CARTESIAN_POINT('Ctrl Pts',(1.03368402663923,-0.579715396745444,
5.0533397209827)) ;
#83815=CARTESIAN_POINT('Ctrl Pts',(1.10025481630781,-0.44047762754836,5.06251684407359)) ;
#83816=CARTESIAN_POINT('Ctrl Pts',(1.17691073218495,-0.142002365400373,
5.08368097096632)) ;
#83817=CARTESIAN_POINT('Ctrl Pts',(1.18535584236089,0.0145014606441104,
5.09477826194369)) ;
#83818=CARTESIAN_POINT('Ctrl Pts',(1.14176601862325,0.316099164561747,5.11616379329503)) ;
#83819=CARTESIAN_POINT('Ctrl Pts',(1.09234347057307,0.458558371862131,5.12626266972199)) ;
#83820=CARTESIAN_POINT('Ctrl Pts',(0.939666462827153,0.722855780487681,
5.145008540428)) ;
#83821=CARTESIAN_POINT('Ctrl Pts',(0.835624990096788,0.840950188579383,
5.15558437333414)) ;
#83822=CARTESIAN_POINT('Ctrl Pts',(0.589589205037277,1.02814885579379,5.1773297508833)) ;
#83823=CARTESIAN_POINT('Ctrl Pts',(0.450540903554148,1.09623183439873,5.18828217964236)) ;
#83824=CARTESIAN_POINT('Ctrl Pts',(0.158161311409111,1.17406763505529,5.20899610027115)) ;
#83825=CARTESIAN_POINT('Ctrl Pts',(0.00804861590346991,1.18464228572274,
5.21792242384493)) ;
#83826=CARTESIAN_POINT('Ctrl Pts',(-0.296530748862871,1.14808352384729,
5.23792207885416)) ;
#83827=CARTESIAN_POINT('Ctrl Pts',(-0.447606380953899,1.09802387470485,
5.24897408362528)) ;
#83828=CARTESIAN_POINT('Ctrl Pts',(-0.715765400545716,0.94436759315512,
5.27088879462436)) ;
#83829=CARTESIAN_POINT('Ctrl Pts',(-0.831457772948567,0.844300644444529,
5.28154094137343)) ;
#83830=CARTESIAN_POINT('Ctrl Pts',(-1.01870853473459,0.605404657890455,
5.30150933055223)) ;
#83831=CARTESIAN_POINT('Ctrl Pts',(-1.08835654108605,0.468792762534213,
5.31050908937556)) ;
#83832=CARTESIAN_POINT('Ctrl Pts',(-1.1601035158885,0.217504967293211,5.32832727218508)) ;
#83833=CARTESIAN_POINT('Ctrl Pts',(-1.17524047358084,0.108898732755448,
5.33602826593765)) ;
#83834=CARTESIAN_POINT('Ctrl Pts',(-1.17524047358084,6.17561557447743E-15,
5.34374999999999)) ;
#83835=CARTESIAN_POINT('Origin',(0.,0.,0.)) ;
#83836=CARTESIAN_POINT('',(-1.17524047358084,-2.2495827876471E-15,5.90624999999999)) ;
#83837=CARTESIAN_POINT('',(-1.17524047358084,1.83623309936453E-15,5.84374999999999)) ;
#83838=CARTESIAN_POINT('',(-1.17524047358084,-1.4392544841992E-16,0.)) ;
#83839=CARTESIAN_POINT('Ctrl Pts',(-1.17524047358084,-7.58582575310211E-15,
5.90624999999999)) ;
#83840=CARTESIAN_POINT('Ctrl Pts',(-1.17524047358084,0.0749412078928489,
5.90093610824922)) ;
#83841=CARTESIAN_POINT('Ctrl Pts',(-1.16807236315843,0.149890538220418,
5.89562164055712)) ;
#83842=CARTESIAN_POINT('Ctrl Pts',(-1.12410951984973,0.37651515556659,5.87955226139312)) ;
#83843=CARTESIAN_POINT('Ctrl Pts',(-1.06448232899237,0.521764927946688,
5.86978553376752)) ;
#83844=CARTESIAN_POINT('Ctrl Pts',(-0.894991089303138,0.776406902522572,
5.85034946141045)) ;
#83845=CARTESIAN_POINT('Ctrl Pts',(-0.788394897908854,0.88443736721281,
5.8399735535765)) ;
#83846=CARTESIAN_POINT('Ctrl Pts',(-0.535488632620262,1.05775927797598,
5.81829825869221)) ;
#83847=CARTESIAN_POINT('Ctrl Pts',(-0.390260895491309,1.11951332927642,
5.80719074928886)) ;
#83848=CARTESIAN_POINT('Ctrl Pts',(-0.0895922589655112,1.18147183035352,
5.78653072733016)) ;
#83849=CARTESIAN_POINT('Ctrl Pts',(0.0624435431070185,1.18321696626138,
5.77769828374712)) ;
#83850=CARTESIAN_POINT('Ctrl Pts',(0.360400561462412,1.1289174745997,5.75747631645805)) ;
#83851=CARTESIAN_POINT('Ctrl Pts',(0.503361754371328,1.07282701451939,5.74670878573645)) ;
#83852=CARTESIAN_POINT('Ctrl Pts',(0.763116910540795,0.907275709569743,
5.72488841340987)) ;
#83853=CARTESIAN_POINT('Ctrl Pts',(0.876640368697243,0.798134855960196,
5.71404775080149)) ;
#83854=CARTESIAN_POINT('Ctrl Pts',(1.05045573515797,0.547640396735084,5.69449318879659)) ;
#83855=CARTESIAN_POINT('Ctrl Pts',(1.11133252962224,0.410272222105063,5.68534136692503)) ;
#83856=CARTESIAN_POINT('Ctrl Pts',(1.17966470128619,0.115195906161128,5.66441825072192)) ;
#83857=CARTESIAN_POINT('Ctrl Pts',(1.18459572722913,-0.0401138114626467,
5.65340563095636)) ;
#83858=CARTESIAN_POINT('Ctrl Pts',(1.13382399717879,-0.346797007312973,
5.63165950021797)) ;
#83859=CARTESIAN_POINT('Ctrl Pts',(1.07744306071906,-0.494878503776931,
5.6215346463652)) ;
#83860=CARTESIAN_POINT('Ctrl Pts',(0.913580515513978,-0.754373946827181,
5.60227214544814)) ;
#83861=CARTESIAN_POINT('Ctrl Pts',(0.809913879086464,-0.864711878274894,
5.59199432645043)) ;
#83862=CARTESIAN_POINT('Ctrl Pts',(0.56202160582472,-1.04384466298271,5.57042091195641)) ;
#83863=CARTESIAN_POINT('Ctrl Pts',(0.418783365136616,-1.1091028100288,5.55931133961254)) ;
#83864=CARTESIAN_POINT('Ctrl Pts',(0.119491572437825,-1.17891825992327,
5.53845730823343)) ;
#83865=CARTESIAN_POINT('Ctrl Pts',(-0.033208005507292,-1.18449175161955,
5.52953876600849)) ;
#83866=CARTESIAN_POINT('Ctrl Pts',(-0.332755258580171,-1.13732471487981,
5.50947201828561)) ;
#83867=CARTESIAN_POINT('Ctrl Pts',(-0.476697840529487,-1.08488640619213,
5.49877370516092)) ;
#83868=CARTESIAN_POINT('Ctrl Pts',(-0.740216032869487,-0.926058330823341,
5.47696061715002)) ;
#83869=CARTESIAN_POINT('Ctrl Pts',(-0.85644416733711,-0.819772004395771,
5.46605507031694)) ;
#83870=CARTESIAN_POINT('Ctrl Pts',(-1.03655016378708,-0.573562522277988,
5.44626613380904)) ;
#83871=CARTESIAN_POINT('Ctrl Pts',(-1.1008642792567,-0.437627573512256,
5.43728106579391)) ;
#83872=CARTESIAN_POINT('Ctrl Pts',(-1.16280481815703,-0.197241280534875,
5.42023588097279)) ;
#83873=CARTESIAN_POINT('Ctrl Pts',(-1.17524047358084,-0.0987057153674117,
5.41324897294683)) ;
#83874=CARTESIAN_POINT('Ctrl Pts',(-1.17524047358084,-1.50972806654875E-14,
5.40625)) ;
#83875=CARTESIAN_POINT('Ctrl Pts',(-1.17524047358084,7.69738201417715E-15,
5.34374999999999)) ;
#83876=CARTESIAN_POINT('Ctrl Pts',(-1.17524047358084,-0.0460814382391025,
5.34701751838417)) ;
#83877=CARTESIAN_POINT('Ctrl Pts',(-1.17253025465147,-0.0922152521519931,
5.35028875059508)) ;
#83878=CARTESIAN_POINT('Ctrl Pts',(-1.14948489675735,-0.286885631866481,
5.36409233548477)) ;
#83879=CARTESIAN_POINT('Ctrl Pts',(-1.10360733284383,-0.430921057723322,
5.37430552369991)) ;
#83880=CARTESIAN_POINT('Ctrl Pts',(-0.957309780951295,-0.699307780007639,
5.39333614823432)) ;
#83881=CARTESIAN_POINT('Ctrl Pts',(-0.85622111678967,-0.820002489146776,
5.40357693887794)) ;
#83882=CARTESIAN_POINT('Ctrl Pts',(-0.614454492851251,-1.01354027017214,
5.42528490244742)) ;
#83883=CARTESIAN_POINT('Ctrl Pts',(-0.476760246395516,-1.08513670825354,
5.43627874710529)) ;
#83884=CARTESIAN_POINT('Ctrl Pts',(-0.186134534229494,-1.16993609825664,
5.45713185130973)) ;
#83885=CARTESIAN_POINT('Ctrl Pts',(-0.0365019681565856,-1.18408252796803,
5.46619501517522)) ;
#83886=CARTESIAN_POINT('Ctrl Pts',(0.267071427811465,-1.15507276534244,
5.48586525574657)) ;
#83887=CARTESIAN_POINT('Ctrl Pts',(0.417813971737475,-1.10947363824431,
5.49673866417285)) ;
#83888=CARTESIAN_POINT('Ctrl Pts',(0.689147490984914,-0.964028909960287,
5.51855718356141)) ;
#83889=CARTESIAN_POINT('Ctrl Pts',(0.807898497105404,-0.866942506731837,
5.52929148241646)) ;
#83890=CARTESIAN_POINT('Ctrl Pts',(1.00126331908508,-0.633622414306119,
5.5494376355253)) ;
#83891=CARTESIAN_POINT('Ctrl Pts',(1.07430845771922,-0.499868779088293,
5.55830556753948)) ;
#83892=CARTESIAN_POINT('Ctrl Pts',(1.16732151556813,-0.207153881912603,
5.57906124150266)) ;
#83893=CARTESIAN_POINT('Ctrl Pts',(1.18448062330524,-0.0504791232455658,
5.59017065288052)) ;
#83894=CARTESIAN_POINT('Ctrl Pts',(1.15713436045325,0.254524452443586,5.61179768599597)) ;
#83895=CARTESIAN_POINT('Ctrl Pts',(1.11517443295985,0.400187610684816,5.62212629260286)) ;
#83896=CARTESIAN_POINT('Ctrl Pts',(0.975960647319752,0.673101398981301,
5.64147791995286)) ;
#83897=CARTESIAN_POINT('Ctrl Pts',(0.878001633002891,0.796685571300439,
5.65141277616985)) ;
#83898=CARTESIAN_POINT('Ctrl Pts',(0.640998731844676,0.997026504127541,
5.67306940775951)) ;
#83899=CARTESIAN_POINT('Ctrl Pts',(0.504870832789386,1.07240301387313,5.68410108433379)) ;
#83900=CARTESIAN_POINT('Ctrl Pts',(0.216201394429409,1.16474743402637,5.70510155782909)) ;
#83901=CARTESIAN_POINT('Ctrl Pts',(0.0670433973381126,1.18273596616217,
5.71436727770251)) ;
#83902=CARTESIAN_POINT('Ctrl Pts',(-0.237077617719062,1.16159741992614,
5.73379208225248)) ;
#83903=CARTESIAN_POINT('Ctrl Pts',(-0.388928202532001,1.11992285024332,
5.74459439266565)) ;
#83904=CARTESIAN_POINT('Ctrl Pts',(-0.664259586879038,0.981402662111225,
5.76641291082476)) ;
#83905=CARTESIAN_POINT('Ctrl Pts',(-0.785749458649678,0.887130828527359,
5.7772156100363)) ;
#83906=CARTESIAN_POINT('Ctrl Pts',(-0.984673026824418,0.658950965260441,
5.79752087248553)) ;
#83907=CARTESIAN_POINT('Ctrl Pts',(-1.06079452208989,0.527742519535345,
5.80632911101323)) ;
#83908=CARTESIAN_POINT('Ctrl Pts',(-1.15329706571952,0.261507134193389,
5.82520718967931)) ;
#83909=CARTESIAN_POINT('Ctrl Pts',(-1.17524047358084,0.131114627104794,
5.83445299298652)) ;
#83910=CARTESIAN_POINT('Ctrl Pts',(-1.17524047358084,-1.04083408558608E-16,
5.84374999999999)) ;
#83911=CARTESIAN_POINT('Origin',(0.,0.,0.)) ;
#83912=CARTESIAN_POINT('',(-1.17524047358084,-2.72175283376453E-15,6.40624999999999)) ;
#83913=CARTESIAN_POINT('',(-1.17524047358084,4.94679191084167E-17,6.34374999999999)) ;
#83914=CARTESIAN_POINT('',(-1.17524047358084,-1.4392544841992E-16,0.)) ;
#83915=CARTESIAN_POINT('Ctrl Pts',(-1.17524047358084,1.90683135537553E-30,
6.40624999999999)) ;
#83916=CARTESIAN_POINT('Ctrl Pts',(-1.17524047358084,0.0972130928115972,
6.39935686514824)) ;
#83917=CARTESIAN_POINT('Ctrl Pts',(-1.16317811940475,0.194278275973553,
6.39247421819613)) ;
#83918=CARTESIAN_POINT('Ctrl Pts',(-1.10153824254022,0.437298694669516,
6.37524225417408)) ;
#83919=CARTESIAN_POINT('Ctrl Pts',(-1.03531235227418,0.576832605858214,
6.36604191838211)) ;
#83920=CARTESIAN_POINT('Ctrl Pts',(-0.854181441061047,0.82122938275905,
6.34625431141678)) ;
#83921=CARTESIAN_POINT('Ctrl Pts',(-0.74159230416404,0.924157550836251,
6.33569128622248)) ;
#83922=CARTESIAN_POINT('Ctrl Pts',(-0.478579939800903,1.08481631082732,
6.31384435531985)) ;
#83923=CARTESIAN_POINT('Ctrl Pts',(-0.329439848447114,1.13901287968353,
6.30276453833942)) ;
#83924=CARTESIAN_POINT('Ctrl Pts',(-0.0261324283789686,1.18442992169236,
6.28252893136117)) ;
#83925=CARTESIAN_POINT('Ctrl Pts',(0.124605997283236,1.17814861438563,6.27370134002346)) ;
#83926=CARTESIAN_POINT('Ctrl Pts',(0.419011611408069,1.10860715347419,6.25315707143774)) ;
#83927=CARTESIAN_POINT('Ctrl Pts',(0.559556434964203,1.04473390860149,6.24226199553197)) ;
#83928=CARTESIAN_POINT('Ctrl Pts',(0.810650286515072,0.865057396938094,
6.22047270241022)) ;
#83929=CARTESIAN_POINT('Ctrl Pts',(0.918126580154595,0.750031227263427,
6.20979472566)) ;
#83930=CARTESIAN_POINT('Ctrl Pts',(1.07831776895032,0.490540515161358,6.19075784192955)) ;
#83931=CARTESIAN_POINT('Ctrl Pts',(1.1318031266677,0.349942297815048,6.18106352438655)) ;
#83932=CARTESIAN_POINT('Ctrl Pts',(1.18430248810267,0.0506155938961819,
6.15983902390858)) ;
#83933=CARTESIAN_POINT('Ctrl Pts',(1.18067233732404,-0.105589764350431,
6.14876289652883)) ;
#83934=CARTESIAN_POINT('Ctrl Pts',(1.11321071305007,-0.407110440650127,
6.1273828270113)) ;
#83935=CARTESIAN_POINT('Ctrl Pts',(1.05025894768157,-0.549470383003391,
6.11792984709037)) ;
#83936=CARTESIAN_POINT('Ctrl Pts',(0.874933559125881,-0.799012447392118,
6.09831632409727)) ;
#83937=CARTESIAN_POINT('Ctrl Pts',(0.765320654280662,-0.904541234041102,
6.0878438607431)) ;
#83938=CARTESIAN_POINT('Ctrl Pts',(0.507300872470456,-1.07162431480738,
6.06607574654216)) ;
#83939=CARTESIAN_POINT('Ctrl Pts',(0.360076243292598,-1.12964209827539,
6.05497807730034)) ;
#83940=CARTESIAN_POINT('Ctrl Pts',(0.0580496940573428,-1.18335930321019,
6.03452685382692)) ;
#83941=CARTESIAN_POINT('Ctrl Pts',(-0.0933211913583464,-1.18110174006449,
6.02572716652203)) ;
#83942=CARTESIAN_POINT('Ctrl Pts',(-0.389544578689132,-1.11924768487494,
6.00534381997293)) ;
#83943=CARTESIAN_POINT('Ctrl Pts',(-0.531362360870357,-1.05929413324628,
5.99450954241255)) ;
#83944=CARTESIAN_POINT('Ctrl Pts',(-0.78692880581635,-0.886696722849366,
5.97269657832903)) ;
#83945=CARTESIAN_POINT('Ctrl Pts',(-0.897499306377748,-0.774600571175226,
5.96193247361706)) ;
#83946=CARTESIAN_POINT('Ctrl Pts',(-1.06459217294446,-0.519620206308922,
5.94263168257401)) ;
#83947=CARTESIAN_POINT('Ctrl Pts',(-1.1218151619999,-0.380680717852885,
5.93324310810642)) ;
#83948=CARTESIAN_POINT('Ctrl Pts',(-1.16734732758849,-0.157270511476844,
5.91740165470473)) ;
#83949=CARTESIAN_POINT('Ctrl Pts',(-1.17524047358084,-0.0786397277081866,
5.91182614444844)) ;
#83950=CARTESIAN_POINT('Ctrl Pts',(-1.17524047358084,-7.58582575310211E-15,
5.90624999999999)) ;
#83951=CARTESIAN_POINT('Ctrl Pts',(-1.17524047358084,0.,5.84374999999999)) ;
#83952=CARTESIAN_POINT('Ctrl Pts',(-1.17524047358084,-0.0249351682621398,
5.84551808979542)) ;
#83953=CARTESIAN_POINT('Ctrl Pts',(-1.17444690966321,-0.049896454030164,
5.84728803151721)) ;
#83954=CARTESIAN_POINT('Ctrl Pts',(-1.16326691459726,-0.225088989663869,
5.85971049168401)) ;
#83955=CARTESIAN_POINT('Ctrl Pts',(-1.12489655565861,-0.372132512664032,
5.87013697646916)) ;
#83956=CARTESIAN_POINT('Ctrl Pts',(-0.992898546841716,-0.647535079178023,
5.88966507679593)) ;
#83957=CARTESIAN_POINT('Ctrl Pts',(-0.899082365125593,-0.772540989574306,
5.89926224179742)) ;
#83958=CARTESIAN_POINT('Ctrl Pts',(-0.668523936196988,-0.978850247286171,
5.92073473275935)) ;
#83959=CARTESIAN_POINT('Ctrl Pts',(-0.534159183145627,-1.05818012315957,
5.93179830024191)) ;
#83960=CARTESIAN_POINT('Ctrl Pts',(-0.247619332292761,-1.15848698536751,
5.95295029904875)) ;
#83961=CARTESIAN_POINT('Ctrl Pts',(-0.0989124286993728,-1.18050496089781,
5.96248937209396)) ;
#83962=CARTESIAN_POINT('Ctrl Pts',(0.205699478839078,-1.16755936647318,
5.98165385045049)) ;
#83963=CARTESIAN_POINT('Ctrl Pts',(0.358591230794876,-1.12999795665931,
5.9923742696277)) ;
#83964=CARTESIAN_POINT('Ctrl Pts',(0.637893753861499,-0.998801759709271,
6.01417698332077)) ;
#83965=CARTESIAN_POINT('Ctrl Pts',(0.762164334503225,-0.907539621260408,
6.02504373445584)) ;
#83966=CARTESIAN_POINT('Ctrl Pts',(0.966831430978108,-0.684736450733742,
6.04551106976708)) ;
#83967=CARTESIAN_POINT('Ctrl Pts',(1.04611887486588,-0.556111465096944,
6.05431754074319)) ;
#83968=CARTESIAN_POINT('Ctrl Pts',(1.15469189529256,-0.269263414025172,
6.07465721146874)) ;
#83969=CARTESIAN_POINT('Ctrl Pts',(1.18028032062798,-0.112871287684847,
6.08574658210224)) ;
#83970=CARTESIAN_POINT('Ctrl Pts',(1.16878242538718,0.194726490535913,6.10755756356628)) ;
#83971=CARTESIAN_POINT('Ctrl Pts',(1.13414049508146,0.343095127788057,6.11807800885581)) ;
#83972=CARTESIAN_POINT('Ctrl Pts',(1.00952700365956,0.620988342124133,6.13778271472828)) ;
#83973=CARTESIAN_POINT('Ctrl Pts',(0.919855079768746,0.74742876887245,6.14709631564413)) ;
#83974=CARTESIAN_POINT('Ctrl Pts',(0.695871898043459,0.959670786413457,
6.16837537447728)) ;
#83975=CARTESIAN_POINT('Ctrl Pts',(0.563407357950225,1.04296430140369,6.17946278012117)) ;
#83976=CARTESIAN_POINT('Ctrl Pts',(0.279096880839658,1.15134179026669,6.20076401214732)) ;
#83977=CARTESIAN_POINT('Ctrl Pts',(0.130797737839273,1.1774241662368,6.21064059511467)) ;
#83978=CARTESIAN_POINT('Ctrl Pts',(-0.174226850731518,1.17266526439425,
6.22954016640769)) ;
#83979=CARTESIAN_POINT('Ctrl Pts',(-0.328043409459078,1.13923669513064,
6.24017085117553)) ;
#83980=CARTESIAN_POINT('Ctrl Pts',(-0.611114743371182,1.0154674591827,6.26194168525353)) ;
#83981=CARTESIAN_POINT('Ctrl Pts',(-0.738088625482068,0.927290495646206,
6.27286505886348)) ;
#83982=CARTESIAN_POINT('Ctrl Pts',(-0.948448644284149,0.709892127722752,
6.29349036284195)) ;
#83983=CARTESIAN_POINT('Ctrl Pts',(-1.0308750732841,0.583774691885055,6.30235601120873)) ;
#83984=CARTESIAN_POINT('Ctrl Pts',(-1.14546161092712,0.304105800060345,
6.32218662588658)) ;
#83985=CARTESIAN_POINT('Ctrl Pts',(-1.17524047358084,0.152744487257788,
6.33291927423992)) ;
#83986=CARTESIAN_POINT('Ctrl Pts',(-1.17524047358084,-7.28583859910259E-15,
6.34374999999999)) ;
#83987=CARTESIAN_POINT('Origin',(0.,0.,0.)) ;
#83988=CARTESIAN_POINT('',(-1.17524047358084,-4.25264630131406E-15,6.90624999999999)) ;
#83989=CARTESIAN_POINT('',(-1.17524047358084,3.5883038101011E-15,6.84374999999999)) ;
#83990=CARTESIAN_POINT('',(-1.17524047358084,-1.4392544841992E-16,0.)) ;
#83991=CARTESIAN_POINT('Ctrl Pts',(-1.17524047358084,-5.759281940243E-15,
6.90624999999999)) ;
#83992=CARTESIAN_POINT('Ctrl Pts',(-1.17524047358084,0.119521171290162,
6.89777505565335)) ;
#83993=CARTESIAN_POINT('Ctrl Pts',(-1.15700615440808,0.238572139687923,
6.8893334522061)) ;
#83994=CARTESIAN_POINT('Ctrl Pts',(-1.07558381670212,0.497141372528847,
6.87099896104922)) ;
#83995=CARTESIAN_POINT('Ctrl Pts',(-1.0028380249261,0.631144921015609,6.8621221709435)) ;
#83996=CARTESIAN_POINT('Ctrl Pts',(-0.810013135609759,0.864960701822275,
6.84199159983804)) ;
#83997=CARTESIAN_POINT('Ctrl Pts',(-0.691530387648851,0.962315200348783,
6.83126426911237)) ;
#83998=CARTESIAN_POINT('Ctrl Pts',(-0.420592817665239,1.10842350505255,
6.80944653778318)) ;
#83999=CARTESIAN_POINT('Ctrl Pts',(-0.269962987074766,1.15440059797669,
6.79856665051965)) ;
#84000=CARTESIAN_POINT('Ctrl Pts',(0.0335533958635028,1.18417163324696,
6.7788729210257)) ;
#84001=CARTESIAN_POINT('Ctrl Pts',(0.183234004924584,1.17039552724657,6.76982625454176)) ;
#84002=CARTESIAN_POINT('Ctrl Pts',(0.474044454137496,1.08632053978066,6.74898748884204)) ;
#84003=CARTESIAN_POINT('Ctrl Pts',(0.611883678841635,1.01508856981479,6.7379976631639)) ;
#84004=CARTESIAN_POINT('Ctrl Pts',(0.854113308250065,0.822197143610017,
6.71628418319936)) ;
#84005=CARTESIAN_POINT('Ctrl Pts',(0.955508006956892,0.701765744281576,
6.70601043627221)) ;
#84006=CARTESIAN_POINT('Ctrl Pts',(1.10247440168677,0.433798141151207,6.68700953041831)) ;
#84007=CARTESIAN_POINT('Ctrl Pts',(1.14871791834261,0.289921392349667,6.67680759359234)) ;
#84008=CARTESIAN_POINT('Ctrl Pts',(1.18541864386451,-0.0131519852271414,
6.65531742594936)) ;
#84009=CARTESIAN_POINT('Ctrl Pts',(1.17327314348846,-0.169786209996843,
6.64421088872777)) ;
#84010=CARTESIAN_POINT('Ctrl Pts',(1.0896308401728,-0.465854103473383,6.62321746226654)) ;
#84011=CARTESIAN_POINT('Ctrl Pts',(1.02030279684906,-0.60273754292522,6.61420178967267)) ;
#84012=CARTESIAN_POINT('Ctrl Pts',(0.833626125081446,-0.842152937460216,
6.5942502390725)) ;
#84013=CARTESIAN_POINT('Ctrl Pts',(0.718223192197296,-0.942493500016631,
6.58360616549766)) ;
#84014=CARTESIAN_POINT('Ctrl Pts',(0.45054154591066,-1.09681661498434,6.56169712714617)) ;
#84015=CARTESIAN_POINT('Ctrl Pts',(0.299643662535163,-1.1472690025159,6.55064211346663)) ;
#84016=CARTESIAN_POINT('Ctrl Pts',(-0.0048197825588484,-1.18466352171105,
6.53061994609462)) ;
#84017=CARTESIAN_POINT('Ctrl Pts',(-0.154989297907911,-1.17449411767808,
6.52170600664431)) ;
#84018=CARTESIAN_POINT('Ctrl Pts',(-0.447563953364002,-1.09744493981908,
6.50100799634912)) ;
#84019=CARTESIAN_POINT('Ctrl Pts',(-0.586759631694064,-1.02976014462743,
6.49006063461073)) ;
#84020=CARTESIAN_POINT('Ctrl Pts',(-0.83328528339986,-0.843269327369928,
6.46831027141656)) ;
#84021=CARTESIAN_POINT('Ctrl Pts',(-0.937656650770386,-0.725461595602201,
6.45772434419496)) ;
#84022=CARTESIAN_POINT('Ctrl Pts',(-1.09104926102747,-0.46161743045704,
6.43895059917853)) ;
#84023=CARTESIAN_POINT('Ctrl Pts',(-1.14085869704814,-0.319337980171836,
6.42889344952874)) ;
#84024=CARTESIAN_POINT('Ctrl Pts',(-1.17105675703185,-0.114558877463233,
6.41437308062609)) ;
#84025=CARTESIAN_POINT('Ctrl Pts',(-1.17524047358084,-0.0572537864841875,
6.41030972137697)) ;
#84026=CARTESIAN_POINT('Ctrl Pts',(-1.17524047358084,1.90683135537553E-30,
6.40624999999999)) ;
#84027=CARTESIAN_POINT('Ctrl Pts',(-1.17524047358084,-7.58582575310211E-15,
6.34374999999999)) ;
#84028=CARTESIAN_POINT('Ctrl Pts',(-1.17524047358084,-0.0044678076702123,
6.34406680095624)) ;
#84029=CARTESIAN_POINT('Ctrl Pts',(-1.17521499629935,-0.008936798749249,
6.344383685825)) ;
#84030=CARTESIAN_POINT('Ctrl Pts',(-1.17343789132738,-0.164708197103276,
6.35542904220494)) ;
#84031=CARTESIAN_POINT('Ctrl Pts',(-1.14250769285491,-0.314289406667729,
6.36603546793419)) ;
#84032=CARTESIAN_POINT('Ctrl Pts',(-1.02514738656922,-0.594574402112479,
6.38590976896346)) ;
#84033=CARTESIAN_POINT('Ctrl Pts',(-0.939454328608444,-0.722411403523905,
6.39500581227288)) ;
#84034=CARTESIAN_POINT('Ctrl Pts',(-0.721904121579447,-0.940314378340289,
6.41609053918469)) ;
#84035=CARTESIAN_POINT('Ctrl Pts',(-0.591394401613091,-1.02741597556096,
6.42719291461776)) ;
#84036=CARTESIAN_POINT('Ctrl Pts',(-0.309471063041387,-1.14358288483808,
6.44862372208196)) ;
#84037=CARTESIAN_POINT('Ctrl Pts',(-0.161553478030403,-1.17366037958495,
6.45877335648141)) ;
#84038=CARTESIAN_POINT('Ctrl Pts',(0.143839569063921,-1.17676187995031,
6.47763679287917)) ;
#84039=CARTESIAN_POINT('Ctrl Pts',(0.298477955528415,-1.14735543048462,
6.4880674659165)) ;
#84040=CARTESIAN_POINT('Ctrl Pts',(0.58511831199092,-1.03072270487193,6.50980444940654)) ;
#84041=CARTESIAN_POINT('Ctrl Pts',(0.714605246437693,-0.945567060310018,
6.52077502666626)) ;
#84042=CARTESIAN_POINT('Ctrl Pts',(0.930370235619318,-0.733371830307261,
6.54154776661931)) ;
#84043=CARTESIAN_POINT('Ctrl Pts',(1.0157831583268,-0.609588394125534,6.55052562678806)) ;
#84044=CARTESIAN_POINT('Ctrl Pts',(1.13859585747244,-0.330336899820532,
6.57032664486213)) ;
#84045=CARTESIAN_POINT('Ctrl Pts',(1.1723287213559,-0.176492281748416,6.58123537811932)) ;
#84046=CARTESIAN_POINT('Ctrl Pts',(1.17771809657695,0.131124527411696,6.6030477090192)) ;
#84047=CARTESIAN_POINT('Ctrl Pts',(1.15097044421376,0.281948420449146,6.61374225029451)) ;
#84048=CARTESIAN_POINT('Ctrl Pts',(1.04168170028128,0.564832157819538,6.63380082154932)) ;
#84049=CARTESIAN_POINT('Ctrl Pts',(0.960313145035741,0.694217503492424,
6.64272534176084)) ;
#84050=CARTESIAN_POINT('Ctrl Pts',(0.749885964309827,0.918233666595859,
6.66358939556668)) ;
#84051=CARTESIAN_POINT('Ctrl Pts',(0.621647266996083,1.00946928529428,6.67469887929173)) ;
#84052=CARTESIAN_POINT('Ctrl Pts',(0.34244034865538,1.13420282045342,6.69626659660949)) ;
#84053=CARTESIAN_POINT('Ctrl Pts',(0.195026152245701,1.1686182415064,6.70653911478431)) ;
#84054=CARTESIAN_POINT('Ctrl Pts',(-0.111706431977466,1.18039552467786,
6.72579239796304)) ;
#84055=CARTESIAN_POINT('Ctrl Pts',(-0.268183346404951,1.154957615284,6.73593761858074)) ;
#84056=CARTESIAN_POINT('Ctrl Pts',(-0.5590576673299,1.04514304650888,6.75769287084004)) ;
#84057=CARTESIAN_POINT('Ctrl Pts',(-0.690958549416792,0.963041337460044,
6.76870340958252)) ;
#84058=CARTESIAN_POINT('Ctrl Pts',(-0.912033611663407,0.756028455339652,
6.78961849517136)) ;
#84059=CARTESIAN_POINT('Ctrl Pts',(-1.00039140029523,0.634496461721281,
6.79875945863243)) ;
#84060=CARTESIAN_POINT('Ctrl Pts',(-1.13003204407789,0.358532398497774,
6.81832737327253)) ;
#84061=CARTESIAN_POINT('Ctrl Pts',(-1.16757371714912,0.205593473793426,
6.82917188610079)) ;
#84062=CARTESIAN_POINT('Ctrl Pts',(-1.17488878285825,0.0332123672961974,
6.84139499492917)) ;
#84063=CARTESIAN_POINT('Ctrl Pts',(-1.17524047358084,0.0165996920375581,
6.8425729577683)) ;
#84064=CARTESIAN_POINT('Ctrl Pts',(-1.17524047358084,1.51344660858459E-14,
6.84374999999999)) ;
#84065=CARTESIAN_POINT('Origin',(0.,0.,0.)) ;
#84066=CARTESIAN_POINT('',(-1.17524047358084,1.18856858147489E-16,7.40624999999999)) ;
#84067=CARTESIAN_POINT('',(-1.17524047358084,2.22940266706097E-16,7.34374999999999)) ;
#84068=CARTESIAN_POINT('',(-1.17524047358084,-1.4392544841992E-16,0.)) ;
#84069=CARTESIAN_POINT('Ctrl Pts',(-1.17524047358084,-7.52869988573934E-15,
7.40624999999999)) ;
#84070=CARTESIAN_POINT('Ctrl Pts',(-1.17524047358084,0.140900390422391,
7.39625910922843)) ;
#84071=CARTESIAN_POINT('Ctrl Pts',(-1.14989965594148,0.280812784794329,
7.38633827476116)) ;
#84072=CARTESIAN_POINT('Ctrl Pts',(-1.04762920185557,0.553274912443593,
7.36701867352676)) ;
#84073=CARTESIAN_POINT('Ctrl Pts',(-0.968660523144742,0.682157590236431,
7.35821482030409)) ;
#84074=CARTESIAN_POINT('Ctrl Pts',(-0.764571824481488,0.905505645411124,
7.33776368485999)) ;
#84075=CARTESIAN_POINT('Ctrl Pts',(-0.64057893563885,0.997075584412772,
7.32690307345249)) ;
#84076=CARTESIAN_POINT('Ctrl Pts',(-0.361668809505296,1.12901714389102,
7.30509803005525)) ;
#84077=CARTESIAN_POINT('Ctrl Pts',(-0.208877053390522,1.16699541834544,
7.29436897198069)) ;
#84078=CARTESIAN_POINT('Ctrl Pts',(0.0956888238037573,1.18076909072001,
7.27517796178267)) ;
#84079=CARTESIAN_POINT('Ctrl Pts',(0.244439347390227,1.15915998788396,7.26566943497862)) ;
#84080=CARTESIAN_POINT('Ctrl Pts',(0.531198935603337,1.05966305353421,7.24453265758091)) ;
#84081=CARTESIAN_POINT('Ctrl Pts',(0.665748146250717,0.980733454568991,
7.2334719542987)) ;
#84082=CARTESIAN_POINT('Ctrl Pts',(0.896964111186548,0.775026017070139,
7.21198042235567)) ;
#84083=CARTESIAN_POINT('Ctrl Pts',(0.991199233222183,0.65016430083957,7.20235150826259)) ;
#84084=CARTESIAN_POINT('Ctrl Pts',(1.12393435326191,0.375013456795158,7.18284125694029)) ;
#84085=CARTESIAN_POINT('Ctrl Pts',(1.16267390068334,0.228107113413445,7.17242449921537)) ;
#84086=CARTESIAN_POINT('Ctrl Pts',(1.18302576086515,-0.0781448611877374,
7.1507089452865)) ;
#84087=CARTESIAN_POINT('Ctrl Pts',(1.1621366215204,-0.234748686209369,7.13960456363426)) ;
#84088=CARTESIAN_POINT('Ctrl Pts',(1.06221252552216,-0.52490121083084,7.11903058103637)) ;
#84089=CARTESIAN_POINT('Ctrl Pts',(0.986405785060841,-0.656369039599867,
7.11021881605146)) ;
#84090=CARTESIAN_POINT('Ctrl Pts',(0.788052581691994,-0.88507891389793,
7.08992978750648)) ;
#84091=CARTESIAN_POINT('Ctrl Pts',(0.66684160771477,-0.979643959324821,
7.0791338193041)) ;
#84092=CARTESIAN_POINT('Ctrl Pts',(0.391913510093961,-1.11888203078298,
7.05731461439808)) ;
#84093=CARTESIAN_POINT('Ctrl Pts',(0.240172112542563,-1.16096183035088,
7.04650464200688)) ;
#84094=CARTESIAN_POINT('Ctrl Pts',(-0.063896025711483,-1.18291047801106,
7.02705436337555)) ;
#84095=CARTESIAN_POINT('Ctrl Pts',(-0.213100997195953,-1.16531857614416,
7.01781219513354)) ;
#84096=CARTESIAN_POINT('Ctrl Pts',(-0.501975738719509,-1.07375536950523,
6.99682681138702)) ;
#84097=CARTESIAN_POINT('Ctrl Pts',(-0.638270561450102,-0.998768809012039,
6.98579870957638)) ;
#84098=CARTESIAN_POINT('Ctrl Pts',(-0.875903269288135,-0.799019702673039,
6.96412438548422)) ;
#84099=CARTESIAN_POINT('Ctrl Pts',(-0.974271645666074,-0.675575654491047,
6.95415336316112)) ;
#84100=CARTESIAN_POINT('Ctrl Pts',(-1.11418971784618,-0.402907736973438,
6.93481916988699)) ;
#84101=CARTESIAN_POINT('Ctrl Pts',(-1.15649700435257,-0.257383727073601,
6.92450042993751)) ;
#84102=CARTESIAN_POINT('Ctrl Pts',(-1.17359052160968,-0.0719524690405092,
6.9113519678283)) ;
#84103=CARTESIAN_POINT('Ctrl Pts',(-1.17524047358084,-0.0359549588519092,
6.90879947531023)) ;
#84104=CARTESIAN_POINT('Ctrl Pts',(-1.17524047358084,-7.58582575310211E-15,
6.90624999999999)) ;
#84105=CARTESIAN_POINT('Ctrl Pts',(-1.17524047358084,1.57512891618694E-14,
6.84374999999999)) ;
#84106=CARTESIAN_POINT('Ctrl Pts',(-1.17524047358084,-0.135226891452661,
6.85333859729082)) ;
#84107=CARTESIAN_POINT('Ctrl Pts',(-1.15189944472838,-0.26959217728986,
6.86286610030385)) ;
#84108=CARTESIAN_POINT('Ctrl Pts',(-1.05517274840351,-0.539002344572276,
6.88196929473786)) ;
#84109=CARTESIAN_POINT('Ctrl Pts',(-0.977439522827835,-0.669720851075183,
6.89080515286758)) ;
#84110=CARTESIAN_POINT('Ctrl Pts',(-0.773103081343997,-0.898842717747965,
6.91147620481635)) ;
#84111=CARTESIAN_POINT('Ctrl Pts',(-0.646891687261351,-0.993542643945497,
6.92258401921284)) ;
#84112=CARTESIAN_POINT('Ctrl Pts',(-0.370190709228593,-1.12549930666603,
6.94425393943049)) ;
#84113=CARTESIAN_POINT('Ctrl Pts',(-0.223303099307756,-1.16359203364959,
6.95462449539132)) ;
#84114=CARTESIAN_POINT('Ctrl Pts',(0.0820479794397184,-1.18264625779152,
6.97405093828379)) ;
#84115=CARTESIAN_POINT('Ctrl Pts',(0.237697446954262,-1.16142548556799,
6.98383624023947)) ;
#84116=CARTESIAN_POINT('Ctrl Pts',(0.530536422283173,-1.05996578566071,
7.00541592603201)) ;
#84117=CARTESIAN_POINT('Ctrl Pts',(0.664963206627907,-0.981234344893288,
7.01646208595114)) ;
#84118=CARTESIAN_POINT('Ctrl Pts',(0.891737710114681,-0.779865074238771,
7.03752707385189)) ;
#84119=CARTESIAN_POINT('Ctrl Pts',(0.983273371875511,-0.660707460643659,
7.04690090290762)) ;
#84120=CARTESIAN_POINT('Ctrl Pts',(1.12014572345183,-0.388310441098143,
7.06621588749084)) ;
#84121=CARTESIAN_POINT('Ctrl Pts',(1.16171568906366,-0.236442774008544,
7.07698444014762)) ;
#84122=CARTESIAN_POINT('Ctrl Pts',(1.18295170444811,0.0711945256250565,
7.09879822397522)) ;
#84123=CARTESIAN_POINT('Ctrl Pts',(1.16374607860161,0.223939531610267,7.10962898651693)) ;
#84124=CARTESIAN_POINT('Ctrl Pts',(1.06879077063093,0.511278658467174,7.13000347818596)) ;
#84125=CARTESIAN_POINT('Ctrl Pts',(0.994851762372556,0.643419387816601,
7.13880342258014)) ;
#84126=CARTESIAN_POINT('Ctrl Pts',(0.796961154022966,0.87783355824789,7.15926628285598)) ;
#84127=CARTESIAN_POINT('Ctrl Pts',(0.672978156071706,0.976128090143578,
7.17036469883477)) ;
#84128=CARTESIAN_POINT('Ctrl Pts',(0.399108068044064,1.11562402974253,7.19212807622204)) ;
#84129=CARTESIAN_POINT('Ctrl Pts',(0.252872132475181,1.15757465457084,7.20259539127241)) ;
#84130=CARTESIAN_POINT('Ctrl Pts',(-0.0509840568487462,1.18422250573345,
7.22219925893808)) ;
#84131=CARTESIAN_POINT('Ctrl Pts',(-0.2057926830757,1.167324956904,7.23166788460105)) ;
#84132=CARTESIAN_POINT('Ctrl Pts',(-0.500546672836903,1.07451481806782,
7.25305850771178)) ;
#84133=CARTESIAN_POINT('Ctrl Pts',(-0.637503666397729,0.999357909769225,
7.26413331135905)) ;
#84134=CARTESIAN_POINT('Ctrl Pts',(-0.870157429570499,0.803902957339546,
7.28534964623793)) ;
#84135=CARTESIAN_POINT('Ctrl Pts',(-0.9649952259348,0.687153725923925,7.29502566503965)) ;
#84136=CARTESIAN_POINT('Ctrl Pts',(-1.10922617325092,0.418474621077651,
7.31407702168297)) ;
#84137=CARTESIAN_POINT('Ctrl Pts',(-1.15488253080609,0.267815401325705,
7.32475988639157)) ;
#84138=CARTESIAN_POINT('Ctrl Pts',(-1.17343972786484,0.0751669931566532,
7.33842009838646)) ;
#84139=CARTESIAN_POINT('Ctrl Pts',(-1.17524047358084,0.037562040414441,
7.34108657059562)) ;
#84140=CARTESIAN_POINT('Ctrl Pts',(-1.17524047358084,7.69738201417715E-15,
7.34374999999999)) ;
#84141=CARTESIAN_POINT('Origin',(0.,0.,0.)) ;
#84142=CARTESIAN_POINT('',(-1.17524047358084,-7.09759280191603E-15,7.90624999999999)) ;
#84143=CARTESIAN_POINT('',(-1.17524047358084,1.08596519600456E-15,7.84374999999999)) ;
#84144=CARTESIAN_POINT('',(-1.17524047358084,-1.4392544841992E-16,0.)) ;
#84145=CARTESIAN_POINT('Ctrl Pts',(-1.17524047358084,-7.58582575310211E-15,
7.90624999999999)) ;
#84146=CARTESIAN_POINT('Ctrl Pts',(-1.17524047358084,0.0058948731809242,
7.90583200943313)) ;
#84147=CARTESIAN_POINT('Ctrl Pts',(-1.17519612161567,0.0117916867983566,
7.90541388127487)) ;
#84148=CARTESIAN_POINT('Ctrl Pts',(-1.17276021783936,0.173603808745751,
7.89394019244374)) ;
#84149=CARTESIAN_POINT('Ctrl Pts',(-1.13940585452016,0.32753281696594,7.88302547529432)) ;
#84150=CARTESIAN_POINT('Ctrl Pts',(-1.01727153832607,0.607106605361429,
7.86320160416041)) ;
#84151=CARTESIAN_POINT('Ctrl Pts',(-0.932148461486229,0.731114324393812,
7.85423700035429)) ;
#84152=CARTESIAN_POINT('Ctrl Pts',(-0.716907295609362,0.9438169432025,7.83347843834259)) ;
#84153=CARTESIAN_POINT('Ctrl Pts',(-0.587661508996336,1.0292692781813,7.82251215062637)) ;
#84154=CARTESIAN_POINT('Ctrl Pts',(-0.301350693636575,1.14660392666468,
7.80077051770002)) ;
#84155=CARTESIAN_POINT('Ctrl Pts',(-0.146790779180812,1.17639625830996,
7.79030505717394)) ;
#84156=CARTESIAN_POINT('Ctrl Pts',(0.158563243857567,1.17406334471649,7.77147126642596)) ;
#84157=CARTESIAN_POINT('Ctrl Pts',(0.306519541774214,1.14437258126579,7.76133296582669)) ;
#84158=CARTESIAN_POINT('Ctrl Pts',(0.588672505983702,1.02897180053752,7.7399152197063)) ;
#84159=CARTESIAN_POINT('Ctrl Pts',(0.719378386679859,0.942241237046807,
7.72881395303141)) ;
#84160=CARTESIAN_POINT('Ctrl Pts',(0.937560621433912,0.724888409377175,
7.70770991953948)) ;
#84161=CARTESIAN_POINT('Ctrl Pts',(1.0236414217451,0.597188552307871,7.69859513175054)) ;
#84162=CARTESIAN_POINT('Ctrl Pts',(1.14171576494173,0.317136633283916,7.67873735758152)) ;
#84163=CARTESIAN_POINT('Ctrl Pts',(1.1730134137733,0.167670809135427,7.66813911354066)) ;
#84164=CARTESIAN_POINT('Ctrl Pts',(1.17732189197484,-0.140829977811578,
7.64626410200883)) ;
#84165=CARTESIAN_POINT('Ctrl Pts',(1.14793575214488,-0.296951504562182,
7.63519391890871)) ;
#84166=CARTESIAN_POINT('Ctrl Pts',(1.0324120929391,-0.581061428499252,7.61504840186178)) ;
#84167=CARTESIAN_POINT('Ctrl Pts',(0.950296156040182,-0.707424436632612,
7.60619130311218)) ;
#84168=CARTESIAN_POINT('Ctrl Pts',(0.740498868551504,-0.925360465755667,
7.58558149305588)) ;
#84169=CARTESIAN_POINT('Ctrl Pts',(0.613789705347934,-1.01384686019507,
7.57466340473639)) ;
#84170=CARTESIAN_POINT('Ctrl Pts',(0.331083216715362,-1.13835745748783,
7.55288869092816)) ;
#84171=CARTESIAN_POINT('Ctrl Pts',(0.177353214776067,-1.17219688281456,
7.54224875502853)) ;
#84172=CARTESIAN_POINT('Ctrl Pts',(-0.127633834305618,-1.17776796833596,
7.52332269400168)) ;
#84173=CARTESIAN_POINT('Ctrl Pts',(-0.275971546063842,-1.1520907162658,
7.51348248391123)) ;
#84174=CARTESIAN_POINT('Ctrl Pts',(-0.560507923634067,-1.0445190806793,
7.49219595037346)) ;
#84175=CARTESIAN_POINT('Ctrl Pts',(-0.693167236998827,-0.961619211029062,
7.48111054035441)) ;
#84176=CARTESIAN_POINT('Ctrl Pts',(-0.917808778987186,-0.749964388364812,
7.45981187140171)) ;
#84177=CARTESIAN_POINT('Ctrl Pts',(-1.0078920433783,-0.623667128528289,
7.45047266070564)) ;
#84178=CARTESIAN_POINT('Ctrl Pts',(-1.13324613899673,-0.346021163261254,
7.43078548664011)) ;
#84179=CARTESIAN_POINT('Ctrl Pts',(-1.16826437655785,-0.197781345255079,
7.42027417559792)) ;
#84180=CARTESIAN_POINT('Ctrl Pts',(-1.1749274611804,-0.0313328213326564,
7.40847173121425)) ;
#84181=CARTESIAN_POINT('Ctrl Pts',(-1.17524047358084,-0.0156603082556396,
7.40736043290058)) ;
#84182=CARTESIAN_POINT('Ctrl Pts',(-1.17524047358084,-7.58582575310211E-15,
7.40624999999999)) ;
#84183=CARTESIAN_POINT('Ctrl Pts',(-1.17524047358084,7.25114412958305E-15,
7.34374999999999)) ;
#84184=CARTESIAN_POINT('Ctrl Pts',(-1.17524047358084,-0.114800540624639,
7.35189021635041)) ;
#84185=CARTESIAN_POINT('Ctrl Pts',(-1.15841823069317,-0.229200240755181,
7.36000201011389)) ;
#84186=CARTESIAN_POINT('Ctrl Pts',(-1.08191912485661,-0.48272018550954,
7.37797846900701)) ;
#84187=CARTESIAN_POINT('Ctrl Pts',(-1.01178498089613,-0.616324113861105,
7.38680296430364)) ;
#84188=CARTESIAN_POINT('Ctrl Pts',(-0.82044410185443,-0.856005323624095,
7.40705035716586)) ;
#84189=CARTESIAN_POINT('Ctrl Pts',(-0.698808940480666,-0.957874766339547,
7.41813134190996)) ;
#84190=CARTESIAN_POINT('Ctrl Pts',(-0.427997399400052,-1.10491551108798,
7.4399743925815)) ;
#84191=CARTESIAN_POINT('Ctrl Pts',(-0.282520564355878,-1.15074740822359,
7.45053269864208)) ;
#84192=CARTESIAN_POINT('Ctrl Pts',(0.019783699303596,-1.18500381086977,
7.47031101774605)) ;
#84193=CARTESIAN_POINT('Ctrl Pts',(0.173779326513984,-1.17236324487432,
7.47952339270713)) ;
#84194=CARTESIAN_POINT('Ctrl Pts',(0.470320579500165,-1.08814557758605,
7.50071913226851)) ;
#84195=CARTESIAN_POINT('Ctrl Pts',(0.609702319781948,-1.0166223215586,7.51181400741951)) ;
#84196=CARTESIAN_POINT('Ctrl Pts',(0.848175488757153,-0.827119850559174,
7.53317666076052)) ;
#84197=CARTESIAN_POINT('Ctrl Pts',(0.946311269830303,-0.712719278720804,
7.54321287626921)) ;
#84198=CARTESIAN_POINT('Ctrl Pts',(1.09772935000642,-0.447755836558663,
7.56200076465733)) ;
#84199=CARTESIAN_POINT('Ctrl Pts',(1.14735802281595,-0.298391829379991,
7.57259178911405)) ;
#84200=CARTESIAN_POINT('Ctrl Pts',(1.18516499220896,0.00838585772460532,
7.59434461998859)) ;
#84201=CARTESIAN_POINT('Ctrl Pts',(1.17397135458397,0.162738510214385,7.60528937668304)) ;
#84202=CARTESIAN_POINT('Ctrl Pts',(1.09401493221283,0.454525951531374,7.62597928709402)) ;
#84203=CARTESIAN_POINT('Ctrl Pts',(1.02754412146254,0.589583406649628,7.63488717413944)) ;
#84204=CARTESIAN_POINT('Ctrl Pts',(0.842589314505928,0.834295352560546,
7.65492077156646)) ;
#84205=CARTESIAN_POINT('Ctrl Pts',(0.723319896849969,0.939572148399538,
7.66597728489355)) ;
#84206=CARTESIAN_POINT('Ctrl Pts',(0.455659765401045,1.09384952159629,7.68788338035219)) ;
#84207=CARTESIAN_POINT('Ctrl Pts',(0.31101429630278,1.14342395280021,7.69852332098254)) ;
#84208=CARTESIAN_POINT('Ctrl Pts',(0.0102535189430444,1.18499783305075,
7.7184662901098)) ;
#84209=CARTESIAN_POINT('Ctrl Pts',(-0.142993451744908,1.17638561620861,
7.72749029565596)) ;
#84210=CARTESIAN_POINT('Ctrl Pts',(-0.441135736426058,1.1003589123575,7.74849395058592)) ;
#84211=CARTESIAN_POINT('Ctrl Pts',(-0.582743444374524,1.03237289144522,
7.75960010902981)) ;
#84212=CARTESIAN_POINT('Ctrl Pts',(-0.826579541055378,0.848744728621272,
7.7810838211089)) ;
#84213=CARTESIAN_POINT('Ctrl Pts',(-0.927895337597086,0.73663765641396,
7.79128000314893)) ;
#84214=CARTESIAN_POINT('Ctrl Pts',(-1.08612342439241,0.475189699535579,
7.81026572899363)) ;
#84215=CARTESIAN_POINT('Ctrl Pts',(-1.13952856720092,0.327096064670921,
7.82055644429624)) ;
#84216=CARTESIAN_POINT('Ctrl Pts',(-1.17098904386158,0.115479407808046,
7.83556164689236)) ;
#84217=CARTESIAN_POINT('Ctrl Pts',(-1.17524047358084,0.0577152052619275,
7.83965756058302)) ;
#84218=CARTESIAN_POINT('Ctrl Pts',(-1.17524047358084,7.69738201417715E-15,
7.84374999999999)) ;
#84219=CARTESIAN_POINT('Origin',(0.,0.,3.17500000000003)) ;
#84220=CARTESIAN_POINT('',(-1.39316924099002,5.26377606127364E-10,0.217928767409175)) ;
#84221=CARTESIAN_POINT('',(-1.17524047358084,-1.4392544841992E-16,-2.77555756156289E-15)) ;
#84222=CARTESIAN_POINT('',(-4.35024047358084,-5.32750807149204E-16,3.17500000000003)) ;
#84223=CARTESIAN_POINT('',(0.,1.31392241650299,0.138681942922155)) ;
#84224=CARTESIAN_POINT('Ctrl Pts',(1.74721348500384E-12,1.31392241650293,
0.138681942922092)) ;
#84225=CARTESIAN_POINT('Ctrl Pts',(-0.167266855118978,1.31974695353597,
0.144506479954901)) ;
#84226=CARTESIAN_POINT('Ctrl Pts',(-0.334124488002528,1.29418388150016,
0.150878326562875)) ;
#84227=CARTESIAN_POINT('Ctrl Pts',(-0.652060491102024,1.18211772827159,
0.164090894186344)) ;
#84228=CARTESIAN_POINT('Ctrl Pts',(-0.799989205130994,1.09575091156118,
0.170816999489089)) ;
#84229=CARTESIAN_POINT('Ctrl Pts',(-1.06340473087861,0.865641363708454,
0.184102644672758)) ;
#84230=CARTESIAN_POINT('Ctrl Pts',(-1.1726050878534,0.721855450662107,0.190024438180476)) ;
#84231=CARTESIAN_POINT('Ctrl Pts',(-1.3335089728491,0.394133514358114,0.202849944858133)) ;
#84232=CARTESIAN_POINT('Ctrl Pts',(-1.38118306540828,0.212723127559774,
0.209850714302632)) ;
#84233=CARTESIAN_POINT('Ctrl Pts',(-1.39238912395266,0.0182111698154136,
0.217237913870716)) ;
#84234=CARTESIAN_POINT('Ctrl Pts',(-1.39282395373248,0.00910529163896913,
0.217583480158522)) ;
#84235=CARTESIAN_POINT('Ctrl Pts',(-1.39316924099002,1.05275545825681E-9,
0.217928767409175)) ;
#84236=CARTESIAN_POINT('Ctrl Pts',(3.46944695195361E-17,1.313922416503,
0.138681942922154)) ;
#84237=CARTESIAN_POINT('Ctrl Pts',(0.121098558534658,1.30970554378009,0.134465070199245)) ;
#84238=CARTESIAN_POINT('Ctrl Pts',(0.240975723217191,1.2884142130355,0.129912989605975)) ;
#84239=CARTESIAN_POINT('Ctrl Pts',(0.468004205836076,1.21399303966281,0.120506510970423)) ;
#84240=CARTESIAN_POINT('Ctrl Pts',(0.574338680072799,1.16212197232517,0.115708518042526)) ;
#84241=CARTESIAN_POINT('Ctrl Pts',(0.810645309221597,1.0035800682715,0.104033084804398)) ;
#84242=CARTESIAN_POINT('Ctrl Pts',(0.929777469010434,0.884582495704132,
0.0972302038558343)) ;
#84243=CARTESIAN_POINT('Ctrl Pts',(1.10705252184507,0.621012134582888,0.0851203819684317)) ;
#84244=CARTESIAN_POINT('Ctrl Pts',(1.17642194056122,0.470512057886478,0.0792919584706692)) ;
#84245=CARTESIAN_POINT('Ctrl Pts',(1.24281530973834,0.140961942944052,0.0654717101243752)) ;
#84246=CARTESIAN_POINT('Ctrl Pts',(1.24387622027251,-0.0190346630085623,
0.0586570394766492)) ;
#84247=CARTESIAN_POINT('Ctrl Pts',(1.1998121485432,-0.253773770858911,0.0484886700811816)) ;
#84248=CARTESIAN_POINT('Ctrl Pts',(1.17732416720795,-0.331067562529302,
0.045111449811975)) ;
#84249=CARTESIAN_POINT('Ctrl Pts',(1.10851242855053,-0.503006066466911,
0.0375382749190259)) ;
#84250=CARTESIAN_POINT('Ctrl Pts',(1.03395653270362,-0.656327700634369,
0.031502652974492)) ;
#84251=CARTESIAN_POINT('Ctrl Pts',(0.826032359412923,-0.866968095167022,
0.0190841208660029)) ;
#84252=CARTESIAN_POINT('Ctrl Pts',(0.758282491098308,-0.921926165773169,
0.0153019770602942)) ;
#84253=CARTESIAN_POINT('Ctrl Pts',(0.613046880469622,-1.01525486110679,
0.00765611751817106)) ;
#84254=CARTESIAN_POINT('Ctrl Pts',(0.536151617816848,-1.05358542078566,
0.00381702273341533)) ;
#84255=CARTESIAN_POINT('Ctrl Pts',(0.455787866251496,-1.08325786021632,
-1.07414819494005E-15)) ;
#84256=CARTESIAN_POINT('Origin',(0.,0.,1.91347191551875E-17)) ;
#84257=CARTESIAN_POINT('Origin',(0.,0.,3.17500000000003)) ;
#84258=CARTESIAN_POINT('Origin',(0.,0.,1.91347191551875E-17)) ;
#84259=CARTESIAN_POINT('Ctrl Pts',(-0.455787866251585,-1.08325786021629,
7.45931094670027E-15)) ;
#84260=CARTESIAN_POINT('Ctrl Pts',(-0.339450345579036,-1.15671718194011,
0.0225912551073548)) ;
#84261=CARTESIAN_POINT('Ctrl Pts',(-0.210569648303892,-1.20857442445214,
0.0439022454998153)) ;
#84262=CARTESIAN_POINT('Ctrl Pts',(0.0513954888457053,-1.26231602057434,
0.0816139151640012)) ;
#84263=CARTESIAN_POINT('Ctrl Pts',(0.206168368761232,-1.27168280828374,
0.102415923974052)) ;
#84264=CARTESIAN_POINT('Ctrl Pts',(0.54006497178572,-1.22359742953493,0.151575420771421)) ;
#84265=CARTESIAN_POINT('Ctrl Pts',(0.702493852367329,-1.16720785633507,
0.176560474021524)) ;
#84266=CARTESIAN_POINT('Ctrl Pts',(0.986274961170952,-1.00279284711702,
0.222626794633426)) ;
#84267=CARTESIAN_POINT('Ctrl Pts',(1.10763761296648,-0.900326883506944,
0.243527666641757)) ;
#84268=CARTESIAN_POINT('Ctrl Pts',(1.29324613200729,-0.677217027216316,
0.278664266693318)) ;
#84269=CARTESIAN_POINT('Ctrl Pts',(1.39030020188671,-0.53001090787689,0.299259900155697)) ;
#84270=CARTESIAN_POINT('Ctrl Pts',(1.46053184144303,-0.341828524454995,
0.324759526419172)) ;
#84271=CARTESIAN_POINT('Ctrl Pts',(-1.39316924099002,1.05275552164663E-9,
0.217928767409175)) ;
#84272=CARTESIAN_POINT('Ctrl Pts',(-1.39980350682736,-0.174946849597754,
0.224563033114318)) ;
#84273=CARTESIAN_POINT('Ctrl Pts',(-1.37337989354183,-0.349676949483546,
0.231091430108109)) ;
#84274=CARTESIAN_POINT('Ctrl Pts',(-1.24575263556661,-0.71231580729705,
0.244473225311046)) ;
#84275=CARTESIAN_POINT('Ctrl Pts',(-1.13982635511045,-0.871321905508161,
0.250346387180502)) ;
#84276=CARTESIAN_POINT('Ctrl Pts',(-0.909270559414451,-1.1289009029262,
0.262595703399922)) ;
#84277=CARTESIAN_POINT('Ctrl Pts',(-0.761488569708769,-1.24131052195541,
0.269371248043327)) ;
#84278=CARTESIAN_POINT('Ctrl Pts',(-0.425577664861815,-1.40767484606303,
0.28294008110021)) ;
#84279=CARTESIAN_POINT('Ctrl Pts',(-0.239452270725757,-1.45766729711709,
0.289592176453111)) ;
#84280=CARTESIAN_POINT('Ctrl Pts',(0.0747747453737359,-1.47811532752047,
0.299565085727837)) ;
#84281=CARTESIAN_POINT('Ctrl Pts',(0.226155217538108,-1.47209514011507,
0.304325733785537)) ;
#84282=CARTESIAN_POINT('Ctrl Pts',(0.527358450674983,-1.40067277358841,
0.314969262175127)) ;
#84283=CARTESIAN_POINT('Ctrl Pts',(0.657371735221159,-1.34999571672739,
0.319872264403233)) ;
#84284=CARTESIAN_POINT('Ctrl Pts',(0.778543926945339,-1.28213468630119,
0.324759526419204)) ;
#84285=CARTESIAN_POINT('Origin',(0.,0.,0.)) ;
#84286=CARTESIAN_POINT('',(0.455787866252619,-1.08325786021584,8.00000000000007)) ;
#84287=CARTESIAN_POINT('Ctrl Pts',(-1.17524047358084,7.69738201417715E-15,
7.84374999999999)) ;
#84288=CARTESIAN_POINT('Ctrl Pts',(-1.17524047358084,-0.0952625616493213,
7.85050482761405)) ;
#84289=CARTESIAN_POINT('Ctrl Pts',(-1.16365735659741,-0.190391637202836,
7.8572501900662)) ;
#84290=CARTESIAN_POINT('Ctrl Pts',(-1.10467059844949,-0.427908134816351,
7.87409188494714)) ;
#84291=CARTESIAN_POINT('Ctrl Pts',(-1.04158501620156,-0.56435038347386,
7.88313035048783)) ;
#84292=CARTESIAN_POINT('Ctrl Pts',(-0.863722948037223,-0.812098320702218,
7.9028360365624)) ;
#84293=CARTESIAN_POINT('Ctrl Pts',(-0.748452859552877,-0.919412673019757,
7.91371919937978)) ;
#84294=CARTESIAN_POINT('Ctrl Pts',(-0.486259227192268,-1.08065308415695,
7.93553647556142)) ;
#84295=CARTESIAN_POINT('Ctrl Pts',(-0.342656760736266,-1.13439809447822,
7.94626023044091)) ;
#84296=CARTESIAN_POINT('Ctrl Pts',(-0.085547857400007,-1.17715319798042,
7.96356451830549)) ;
#84297=CARTESIAN_POINT('Ctrl Pts',(0.0235942810878135,-1.18002040743108,
7.97002940339912)) ;
#84298=CARTESIAN_POINT('Ctrl Pts',(0.243174285763268,-1.15527572473979,
7.98439059217357)) ;
#84299=CARTESIAN_POINT('Ctrl Pts',(0.352337269914904,-1.12678537873124,
7.99210412633095)) ;
#84300=CARTESIAN_POINT('Ctrl Pts',(0.455787866253993,-1.08325786021526,
8.00000000000017)) ;
#84301=CARTESIAN_POINT('',(-0.455787866251364,-1.08325786021637,8.)) ;
#84302=CARTESIAN_POINT('Origin',(0.,0.,8.)) ;
#84303=CARTESIAN_POINT('Ctrl Pts',(-0.455787866250356,-1.08325786021679,
8.00000000000008)) ;
#84304=CARTESIAN_POINT('Ctrl Pts',(-0.531256398246912,-1.0515039792333,
7.99423985925915)) ;
#84305=CARTESIAN_POINT('Ctrl Pts',(-0.603190980473794,-1.01195569703915,
7.98842038950236)) ;
#84306=CARTESIAN_POINT('Ctrl Pts',(-0.737096443487214,-0.918948446823796,
7.9769001119198)) ;
#84307=CARTESIAN_POINT('Ctrl Pts',(-0.798787320119198,-0.865862967133268,
7.97122974005493)) ;
#84308=CARTESIAN_POINT('Ctrl Pts',(-0.958575679625279,-0.696632226777244,
7.95541764643436)) ;
#84309=CARTESIAN_POINT('Ctrl Pts',(-1.04030848497531,-0.567378753684563,
7.94648139422948)) ;
#84310=CARTESIAN_POINT('Ctrl Pts',(-1.14814522391219,-0.290213046141342,
7.92682827402602)) ;
#84311=CARTESIAN_POINT('Ctrl Pts',(-1.17524047358084,-0.145699223142899,
7.91658116387795)) ;
#84312=CARTESIAN_POINT('Ctrl Pts',(-1.17524047358084,-8.50014503228635E-15,
7.90624999999999)) ;
#84313=CARTESIAN_POINT('Origin',(0.,0.,0.)) ;
#84314=CARTESIAN_POINT('',(-0.581737793027629,1.38259941420621,8.)) ;
#84315=CARTESIAN_POINT('Ctrl Pts',(-1.5,1.00028780763944E-14,7.59374999999998)) ;
#84316=CARTESIAN_POINT('Ctrl Pts',(-1.5,-0.0509437253219826,7.59658020696231)) ;
#84317=CARTESIAN_POINT('Ctrl Pts',(-1.49740480695262,-0.101948126880478,
7.59941378482669)) ;
#84318=CARTESIAN_POINT('Ctrl Pts',(-1.4727084914817,-0.343100689898983,
7.61281114943883)) ;
#84319=CARTESIAN_POINT('Ctrl Pts',(-1.41699909629399,-0.527943361805503,
7.62308018676697)) ;
#84320=CARTESIAN_POINT('Ctrl Pts',(-1.23503998147008,-0.874470527776589,
7.64233169598759)) ;
#84321=CARTESIAN_POINT('Ctrl Pts',(-1.10751742534909,-1.03124396290167,
7.65244354199804)) ;
#84322=CARTESIAN_POINT('Ctrl Pts',(-0.80137955361333,-1.2830869061876,7.67416824453285)) ;
#84323=CARTESIAN_POINT('Ctrl Pts',(-0.626796522977761,-1.37682605537175,
7.68517173976574)) ;
#84324=CARTESIAN_POINT('Ctrl Pts',(-0.257489486781775,-1.4898930142487,
7.70608078168688)) ;
#84325=CARTESIAN_POINT('Ctrl Pts',(-0.0669875740693966,-1.51048940633529,
7.71523568644169)) ;
#84326=CARTESIAN_POINT('Ctrl Pts',(0.32051462680166,-1.47879221828775,7.73475987221949)) ;
#84327=CARTESIAN_POINT('Ctrl Pts',(0.513520886644871,-1.42331700179412,
7.74558686846174)) ;
#84328=CARTESIAN_POINT('Ctrl Pts',(0.862330105706918,-1.24258946154641,
7.76738916928984)) ;
#84329=CARTESIAN_POINT('Ctrl Pts',(1.01566751877847,-1.12074684324605,7.77815113619099)) ;
#84330=CARTESIAN_POINT('Ctrl Pts',(1.2661792463292,-0.826861703363028,7.79836736341024)) ;
#84331=CARTESIAN_POINT('Ctrl Pts',(1.3615516870939,-0.658094117149608,7.80718921571392)) ;
#84332=CARTESIAN_POINT('Ctrl Pts',(1.48575203610995,-0.286847017644384,
7.82781405457532)) ;
#84333=CARTESIAN_POINT('Ctrl Pts',(1.51067710287673,-0.0870855361917978,
7.83891191465601)) ;
#84334=CARTESIAN_POINT('Ctrl Pts',(1.48155691646122,0.302938128189284,7.86057989601052)) ;
#84335=CARTESIAN_POINT('Ctrl Pts',(1.43072661101655,0.489718620170333,7.87095659000947)) ;
#84336=CARTESIAN_POINT('Ctrl Pts',(1.25865525265882,0.8396664471157,7.89039813595088)) ;
#84337=CARTESIAN_POINT('Ctrl Pts',(1.13686882978925,0.998401435207855,7.90011907945755)) ;
#84338=CARTESIAN_POINT('Ctrl Pts',(0.839566688676397,1.25852222601811,7.92164861291357)) ;
#84339=CARTESIAN_POINT('Ctrl Pts',(0.667338761300122,1.35772216803583,7.93269048687789)) ;
#84340=CARTESIAN_POINT('Ctrl Pts',(0.309739960677104,1.47875080212639,7.95325737369721)) ;
#84341=CARTESIAN_POINT('Ctrl Pts',(0.129593969136037,1.50526254987928,7.96236872531174)) ;
#84342=CARTESIAN_POINT('Ctrl Pts',(-0.2334837963999,1.49293881233257,7.98017963849379)) ;
#84343=CARTESIAN_POINT('Ctrl Pts',(-0.413384241403028,1.45343527784404,
7.98993242309205)) ;
#84344=CARTESIAN_POINT('Ctrl Pts',(-0.581737793027622,1.38259941420621,
8.)) ;
#84345=CARTESIAN_POINT('',(0.581737793027052,1.38259941420645,8.)) ;
#84346=CARTESIAN_POINT('Origin',(0.,0.,8.)) ;
#84347=CARTESIAN_POINT('Ctrl Pts',(0.581737793026286,1.38259941420677,8.00000000000004)) ;
#84348=CARTESIAN_POINT('Ctrl Pts',(0.67475850150618,1.34346033957619,7.99443734255911)) ;
#84349=CARTESIAN_POINT('Ctrl Pts',(0.763582990950793,1.29503877601366,7.98881872888587)) ;
#84350=CARTESIAN_POINT('Ctrl Pts',(0.929533949930955,1.18152247381298,7.97768117903257)) ;
#84351=CARTESIAN_POINT('Ctrl Pts',(1.00632475086677,1.11684435455,7.97218996547596)) ;
#84352=CARTESIAN_POINT('Ctrl Pts',(1.21089201470299,0.906188142783699,7.95649615696774)) ;
#84353=CARTESIAN_POINT('Ctrl Pts',(1.31753983147867,0.742644036694035,7.94750800203856)) ;
#84354=CARTESIAN_POINT('Ctrl Pts',(1.46276050636553,0.384267716790858,7.92759820648838)) ;
#84355=CARTESIAN_POINT('Ctrl Pts',(1.50003763254766,0.19287700920056,7.91696538940003)) ;
#84356=CARTESIAN_POINT('Ctrl Pts',(1.49996080802917,-0.201167980378509,
7.89507400109008)) ;
#84357=CARTESIAN_POINT('Ctrl Pts',(1.45957105504829,-0.400026721363593,
7.88402629325758)) ;
#84358=CARTESIAN_POINT('Ctrl Pts',(1.306992989412,-0.760247630347313,7.86401402053627)) ;
#84359=CARTESIAN_POINT('Ctrl Pts',(1.20013180168387,-0.919727078186579,
7.85511006050304)) ;
#84360=CARTESIAN_POINT('Ctrl Pts',(0.928798149448953,-1.19396261027086,
7.83443786040419)) ;
#84361=CARTESIAN_POINT('Ctrl Pts',(0.765468514485824,-1.30470859053651,
7.82350338244853)) ;
#84362=CARTESIAN_POINT('Ctrl Pts',(0.402536691306379,-1.4585819400554,7.8017675572555)) ;
#84363=CARTESIAN_POINT('Ctrl Pts',(0.20592642872561,-1.49903910617981,7.7911843314165)) ;
#84364=CARTESIAN_POINT('Ctrl Pts',(-0.183266169425525,-1.50088711532144,
7.77240796022013)) ;
#84365=CARTESIAN_POINT('Ctrl Pts',(-0.37217407632198,-1.46553401384534,
7.76238637789988)) ;
#84366=CARTESIAN_POINT('Ctrl Pts',(-0.733536341658091,-1.32327533097475,
7.74104869772291)) ;
#84367=CARTESIAN_POINT('Ctrl Pts',(-0.901472357833655,-1.21510701387381,
7.72996419690242)) ;
#84368=CARTESIAN_POINT('Ctrl Pts',(-1.18389796843274,-0.941565603956125,
7.70877761587926)) ;
#84369=CARTESIAN_POINT('Ctrl Pts',(-1.2962998624187,-0.779587835417801,
7.69956043530099)) ;
#84370=CARTESIAN_POINT('Ctrl Pts',(-1.45166388269414,-0.424032599075321,
7.6798073666153)) ;
#84371=CARTESIAN_POINT('Ctrl Pts',(-1.49406770049158,-0.234256040953705,
7.66926422449743)) ;
#84372=CARTESIAN_POINT('Ctrl Pts',(-1.49980716686,-0.0277811177528503,7.65779339543071)) ;
#84373=CARTESIAN_POINT('Ctrl Pts',(-1.5,-0.0138864685015336,7.65702147047229)) ;
#84374=CARTESIAN_POINT('Ctrl Pts',(-1.5,-9.66814085323955E-15,7.65624999999999)) ;
#84375=CARTESIAN_POINT('Origin',(2.07158391530995E-14,-2.18372685607914E-14,
10.5)) ;
#84376=CARTESIAN_POINT('',(-0.214086590007418,-0.905647899858313,8.375)) ;
#84377=CARTESIAN_POINT('',(0.214086590007422,-0.905647899858319,8.375)) ;
#84378=CARTESIAN_POINT('Origin',(1.33147826576248E-14,-2.18372685607914E-14,
8.375)) ;
#84379=CARTESIAN_POINT('',(-0.378092453297405,-1.38212190130695,10.249595595364)) ;
#84380=CARTESIAN_POINT('Ctrl Pts',(-0.214086590007057,-0.905647899857255,
8.37499999999588)) ;
#84381=CARTESIAN_POINT('Ctrl Pts',(-0.279010764447842,-1.09462213691599,
9.11708670956764)) ;
#84382=CARTESIAN_POINT('Ctrl Pts',(-0.378092453294835,-1.38212190129948,
10.2495955953347)) ;
#84383=CARTESIAN_POINT('',(0.378092453297409,-1.38212190130694,10.249595595364)) ;
#84384=CARTESIAN_POINT('Origin',(-5.47577883755165E-29,-2.39231904255907E-14,
10.2495955953641)) ;
#84385=CARTESIAN_POINT('Ctrl Pts',(0.214086590007062,-0.90564789985724,
8.37499999999589)) ;
#84386=CARTESIAN_POINT('Ctrl Pts',(0.279010764452302,-1.09462213692897,
9.11708670961856)) ;
#84387=CARTESIAN_POINT('Ctrl Pts',(0.378092453297408,-1.38212190130698,
10.249595595364)) ;
#84388=CARTESIAN_POINT('Origin',(0.,0.,10.5)) ;
#84389=CARTESIAN_POINT('',(0.905647899858292,-0.214086590007431,8.375)) ;
#84390=CARTESIAN_POINT('',(0.905647899858297,0.214086590007409,8.375)) ;
#84391=CARTESIAN_POINT('Origin',(0.,0.,8.375)) ;
#84392=CARTESIAN_POINT('',(1.38212190130692,-0.378092453297421,10.2495955953641)) ;
#84393=CARTESIAN_POINT('Ctrl Pts',(0.905647899857241,-0.21408659000707,
8.37499999999588)) ;
#84394=CARTESIAN_POINT('Ctrl Pts',(1.09462213691615,-0.279010764447917,
9.11708670956834)) ;
#84395=CARTESIAN_POINT('Ctrl Pts',(1.38212190129946,-0.37809245329485,10.2495955953347)) ;
#84396=CARTESIAN_POINT('',(1.38212190130692,0.378092453297394,10.2495955953641)) ;
#84397=CARTESIAN_POINT('Origin',(0.,-8.23993651088983E-15,10.2495955953641)) ;
#84398=CARTESIAN_POINT('Ctrl Pts',(0.905647899857261,0.214086590007048,
8.37499999999588)) ;
#84399=CARTESIAN_POINT('Ctrl Pts',(1.09462213691212,0.279010764446507,9.11708670955249)) ;
#84400=CARTESIAN_POINT('Ctrl Pts',(1.38212190130691,0.378092453297394,10.2495955953641)) ;
#84401=CARTESIAN_POINT('Origin',(0.,-5.20417042793042E-15,9.0585454011027)) ;
#84402=CARTESIAN_POINT('',(-3.49510952379173E-16,2.85397350993377,9.39035876017455)) ;
#84403=CARTESIAN_POINT('Origin',(0.,-5.89341654657538E-15,9.39035876017455)) ;
#84404=CARTESIAN_POINT('',(-3.67394039744206E-16,3.,9.05854540110271)) ;
#84405=CARTESIAN_POINT('Origin',(-3.12284933782575E-16,2.54999999999999,
9.05854540110271)) ;
#84406=CARTESIAN_POINT('',(2.99999999999999,-3.67394039744205E-16,9.05854540110271)) ;
#84407=CARTESIAN_POINT('Origin',(0.,-5.23876967272948E-15,9.0585454011027)) ;
#84408=CARTESIAN_POINT('Origin',(0.,-5.23876967272948E-15,9.0585454011027)) ;
#84409=CARTESIAN_POINT('Origin',(0.,-8.23993651088983E-15,6.275)) ;
#84410=CARTESIAN_POINT('',(0.378092453297396,1.38212190130692,10.2495955953641)) ;
#84411=CARTESIAN_POINT('',(-0.378092453297399,1.38212190130692,10.2495955953641)) ;
#84412=CARTESIAN_POINT('Origin',(0.,-8.23993651088983E-15,10.2495955953641)) ;
#84413=CARTESIAN_POINT('',(0.39252831458563,0.748513789365911,10.414598244924)) ;
#84414=CARTESIAN_POINT('Origin',(0.0301297752810506,-8.23524087264071E-15,
6.27236398622833)) ;
#84415=CARTESIAN_POINT('',(0.498545645256686,0.498545645256685,10.4407567714872)) ;
#84416=CARTESIAN_POINT('Origin',(0.263070324890146,0.108967296427384,6.25008801707577)) ;
#84417=CARTESIAN_POINT('',(0.748513789365912,0.392528314585628,10.414598244924)) ;
#84418=CARTESIAN_POINT('Origin',(0.108967296427394,0.263070324890141,6.25008801707577)) ;
#84419=CARTESIAN_POINT('Origin',(0.,0.0301297752810484,6.27236398622833)) ;
#84420=CARTESIAN_POINT('',(0.748513789365931,-0.392528314585653,10.414598244924)) ;
#84421=CARTESIAN_POINT('Origin',(-1.05702599154822E-16,-0.0301297752810628,
6.27236398622833)) ;
#84422=CARTESIAN_POINT('',(0.498545645256703,-0.498545645256708,10.4407567714872)) ;
#84423=CARTESIAN_POINT('Origin',(0.108967296427393,-0.263070324890159,6.25008801707577)) ;
#84424=CARTESIAN_POINT('',(0.392528314585646,-0.748513789365934,10.414598244924)) ;
#84425=CARTESIAN_POINT('Origin',(0.263070324890154,-0.108967296427406,6.25008801707577)) ;
#84426=CARTESIAN_POINT('Origin',(0.0301297752810606,-8.33993336976058E-15,
6.27236398622833)) ;
#84427=CARTESIAN_POINT('',(-0.392528314585635,-0.74851378936595,10.414598244924)) ;
#84428=CARTESIAN_POINT('Origin',(-0.0301297752810506,-8.02383567433109E-15,
6.27236398622833)) ;
#84429=CARTESIAN_POINT('',(-0.49854564525669,-0.498545645256722,10.4407567714872)) ;
#84430=CARTESIAN_POINT('Origin',(-0.26307032489015,-0.1089672964274,6.25008801707577)) ;
#84431=CARTESIAN_POINT('',(-0.748513789365915,-0.392528314585664,10.414598244924)) ;
#84432=CARTESIAN_POINT('Origin',(-0.108967296427399,-0.263070324890164,
6.25008801707577)) ;
#84433=CARTESIAN_POINT('',(-1.38212190130693,-0.378092453297424,10.249595595364)) ;
#84434=CARTESIAN_POINT('Origin',(-2.1039509627475E-16,-0.0301297752810731,
6.27236398622833)) ;
#84435=CARTESIAN_POINT('',(-1.38212190130693,0.37809245329739,10.249595595364)) ;
#84436=CARTESIAN_POINT('Origin',(-7.84162695735042E-15,-1.60815634682402E-14,
10.2495955953641)) ;
#84437=CARTESIAN_POINT('',(-0.748513789365927,0.392528314585617,10.414598244924)) ;
#84438=CARTESIAN_POINT('Origin',(3.16097695429417E-16,0.0301297752810384,
6.27236398622833)) ;
#84439=CARTESIAN_POINT('',(-0.4985456452567,0.498545645256671,10.4407567714872)) ;
#84440=CARTESIAN_POINT('Origin',(-0.108967296427388,0.263070324890137,6.25008801707577)) ;
#84441=CARTESIAN_POINT('',(-0.392528314585641,0.748513789365896,10.414598244924)) ;
#84442=CARTESIAN_POINT('Origin',(-0.26307032489015,0.10896729642739,6.25008801707577)) ;
#84443=CARTESIAN_POINT('Origin',(-0.0301297752810606,-7.91914317721115E-15,
6.27236398622833)) ;
#84444=CARTESIAN_POINT('Origin',(0.,0.,0.)) ;
#84445=CARTESIAN_POINT('',(-3.67394039744206E-16,2.99999999999999,8.45)) ;
#84446=CARTESIAN_POINT('',(2.99999999999999,-3.67394039744205E-16,8.44999999999999)) ;
#84447=CARTESIAN_POINT('Origin',(0.,-4.0381478968626E-15,8.44999999999999)) ;
#84448=CARTESIAN_POINT('',(2.99999999999999,-3.67394039744205E-16,0.)) ;
#84449=CARTESIAN_POINT('Origin',(0.,-4.0381478968626E-15,8.44999999999999)) ;
#84450=CARTESIAN_POINT('Origin',(0.,-4.33680868994202E-15,8.44999999999999)) ;
#84451=CARTESIAN_POINT('',(-3.12284933782575E-16,2.54999999999999,8.)) ;
#84452=CARTESIAN_POINT('Origin',(-3.12284933782575E-16,2.55,8.45)) ;
#84453=CARTESIAN_POINT('Origin',(0.,-3.15032621887263E-15,7.99999999999999)) ;
#84454=CARTESIAN_POINT('Origin',(0.,-8.094915342364E-15,8.)) ;
#84455=CARTESIAN_POINT('Ctrl Pts',(-0.581737793027625,1.38259941420621,
8.)) ;
#84456=CARTESIAN_POINT('Ctrl Pts',(-0.729864874634484,1.3029320087127,8.)) ;
#84457=CARTESIAN_POINT('Ctrl Pts',(-0.863262176577335,1.19854179063676,
7.99999999999998)) ;
#84458=CARTESIAN_POINT('Ctrl Pts',(-1.11135289090838,0.924723635099756,
7.99999999999998)) ;
#84459=CARTESIAN_POINT('Ctrl Pts',(-1.19622518509719,0.769719328397424,
7.9999999998933)) ;
#84460=CARTESIAN_POINT('Ctrl Pts',(-1.3131079977207,0.4825998456181,7.9999999998933)) ;
#84461=CARTESIAN_POINT('Ctrl Pts',(-1.34659883481402,0.308343046285069,
8.)) ;
#84462=CARTESIAN_POINT('Ctrl Pts',(-1.3439581077645,-0.0381523603338236,
8.)) ;
#84463=CARTESIAN_POINT('Ctrl Pts',(-1.30980794379433,-0.207008363331256,
8.)) ;
#84464=CARTESIAN_POINT('Ctrl Pts',(-1.1949082548263,-0.485324594498909,
8.)) ;
#84465=CARTESIAN_POINT('Ctrl Pts',(-1.11064003044993,-0.640909763593095,
7.99999999998602)) ;
#84466=CARTESIAN_POINT('Ctrl Pts',(-0.89560004435886,-0.855220230784529,
7.99999999998602)) ;
#84467=CARTESIAN_POINT('Ctrl Pts',(-0.813300635214957,-0.91826563598073,
8.)) ;
#84468=CARTESIAN_POINT('Ctrl Pts',(-0.639506338952977,-1.01853200109966,
8.)) ;
#84469=CARTESIAN_POINT('Ctrl Pts',(-0.549475089174124,-1.0566200499526,
8.)) ;
#84470=CARTESIAN_POINT('Ctrl Pts',(-0.455787866251369,-1.08325786021637,
8.)) ;
#84471=CARTESIAN_POINT('Ctrl Pts',(0.455787866252654,-1.08325786021595,
8.)) ;
#84472=CARTESIAN_POINT('Ctrl Pts',(0.572824329435331,-1.0499812297112,8.)) ;
#84473=CARTESIAN_POINT('Ctrl Pts',(0.684011935637464,-0.998876628478368,
8.)) ;
#84474=CARTESIAN_POINT('Ctrl Pts',(0.903757997974771,-0.853530202235782,
8.)) ;
#84475=CARTESIAN_POINT('Ctrl Pts',(1.00703055401931,-0.754755114613078,
7.99999999999225)) ;
#84476=CARTESIAN_POINT('Ctrl Pts',(1.15763806880758,-0.548083195129258,
7.99999999999225)) ;
#84477=CARTESIAN_POINT('Ctrl Pts',(1.25545705153481,-0.389463905034916,
8.00000000003248)) ;
#84478=CARTESIAN_POINT('Ctrl Pts',(1.34993353979521,0.00500026766052222,
8.00000000003248)) ;
#84479=CARTESIAN_POINT('Ctrl Pts',(1.35637890633501,0.183538835590366,8.)) ;
#84480=CARTESIAN_POINT('Ctrl Pts',(1.29407820061595,0.563580295571493,8.)) ;
#84481=CARTESIAN_POINT('Ctrl Pts',(1.21679738901834,0.732819558362854,7.99999999999994)) ;
#84482=CARTESIAN_POINT('Ctrl Pts',(1.06567098606457,0.974403116538763,7.99999999999994)) ;
#84483=CARTESIAN_POINT('Ctrl Pts',(0.983776834865333,1.07380659930599,8.)) ;
#84484=CARTESIAN_POINT('Ctrl Pts',(0.797226824491547,1.24808435953097,8.)) ;
#84485=CARTESIAN_POINT('Ctrl Pts',(0.693609148877066,1.32243147885714,8.)) ;
#84486=CARTESIAN_POINT('Ctrl Pts',(0.581737793027051,1.38259941420645,8.)) ;
#84487=CARTESIAN_POINT('Ctrl Pts',(0.00408156060463945,1.5000051209297,
0.0310476188649207)) ;
#84488=CARTESIAN_POINT('Ctrl Pts',(-0.864669974149657,1.50236902088577,
0.0727794857188941)) ;
#84489=CARTESIAN_POINT('Ctrl Pts',(-1.29904734958516,0.750005336973063,
0.114577170727664)) ;
#84490=CARTESIAN_POINT('Ctrl Pts',(-1.73206313278021,1.06058278574021E-16,
0.15624383739433)) ;
#84491=CARTESIAN_POINT('Ctrl Pts',(-1.29904734958516,-0.750005336973063,
0.197910504060997)) ;
#84492=CARTESIAN_POINT('Ctrl Pts',(-0.866031566390109,-1.50001067394612,
0.239577170727664)) ;
#84493=CARTESIAN_POINT('Ctrl Pts',(-1.83698327053499E-16,-1.50001067394612,
0.28124383739433)) ;
#84494=CARTESIAN_POINT('Ctrl Pts',(0.866031566390108,-1.50001067394612,
0.322910504060997)) ;
#84495=CARTESIAN_POINT('Ctrl Pts',(1.29904734958516,-0.750005336973063,
0.364577170727663)) ;
#84496=CARTESIAN_POINT('Ctrl Pts',(1.73206313278021,-3.18174835722064E-16,
0.40624383739433)) ;
#84497=CARTESIAN_POINT('Ctrl Pts',(1.29904734958516,0.750005336973062,0.447910504060997)) ;
#84498=CARTESIAN_POINT('Ctrl Pts',(0.866031566390109,1.50001067394612,0.489577170727663)) ;
#84499=CARTESIAN_POINT('Ctrl Pts',(0.,1.50001067394612,0.53124383739433)) ;
#84500=CARTESIAN_POINT('Ctrl Pts',(-0.866031566390108,1.50001067394612,
0.572910504060996)) ;
#84501=CARTESIAN_POINT('Ctrl Pts',(-1.29904734958516,0.750005336973063,
0.614577170727663)) ;
#84502=CARTESIAN_POINT('Ctrl Pts',(-1.73206313278021,1.06058278574021E-16,
0.656243837394329)) ;
#84503=CARTESIAN_POINT('Ctrl Pts',(-1.29904734958516,-0.750005336973063,
0.697910504060997)) ;
#84504=CARTESIAN_POINT('Ctrl Pts',(-0.866031566390109,-1.50001067394612,
0.739577170727663)) ;
#84505=CARTESIAN_POINT('Ctrl Pts',(-1.83698327053499E-16,-1.50001067394612,
0.78124383739433)) ;
#84506=CARTESIAN_POINT('Ctrl Pts',(0.866031566390108,-1.50001067394612,
0.822910504060996)) ;
#84507=CARTESIAN_POINT('Ctrl Pts',(1.29904734958516,-0.750005336973063,
0.864577170727663)) ;
#84508=CARTESIAN_POINT('Ctrl Pts',(1.73206313278021,-3.18174835722064E-16,
0.906243837394329)) ;
#84509=CARTESIAN_POINT('Ctrl Pts',(1.29904734958516,0.750005336973062,0.947910504060997)) ;
#84510=CARTESIAN_POINT('Ctrl Pts',(0.866031566390109,1.50001067394612,0.989577170727662)) ;
#84511=CARTESIAN_POINT('Ctrl Pts',(0.,1.50001067394612,1.03124383739434)) ;
#84512=CARTESIAN_POINT('Ctrl Pts',(-0.866031566390108,1.50001067394612,
1.072910504061)) ;
#84513=CARTESIAN_POINT('Ctrl Pts',(-1.29904734958516,0.750005336973063,
1.11457717072767)) ;
#84514=CARTESIAN_POINT('Ctrl Pts',(-1.73206313278021,1.06058278574021E-16,
1.15624383739434)) ;
#84515=CARTESIAN_POINT('Ctrl Pts',(-1.29904734958516,-0.750005336973063,
1.197910504061)) ;
#84516=CARTESIAN_POINT('Ctrl Pts',(-0.866031566390109,-1.50001067394612,
1.23957717072767)) ;
#84517=CARTESIAN_POINT('Ctrl Pts',(-1.83698327053499E-16,-1.50001067394612,
1.28124383739434)) ;
#84518=CARTESIAN_POINT('Ctrl Pts',(0.866031566390108,-1.50001067394612,
1.322910504061)) ;
#84519=CARTESIAN_POINT('Ctrl Pts',(1.29904734958516,-0.750005336973063,
1.36457717072767)) ;
#84520=CARTESIAN_POINT('Ctrl Pts',(1.73206313278021,-3.18174835722064E-16,
1.40624383739433)) ;
#84521=CARTESIAN_POINT('Ctrl Pts',(1.29904734958516,0.750005336973062,1.447910504061)) ;
#84522=CARTESIAN_POINT('Ctrl Pts',(0.866031566390109,1.50001067394612,1.48957717072767)) ;
#84523=CARTESIAN_POINT('Ctrl Pts',(0.,1.50001067394612,1.53124383739433)) ;
#84524=CARTESIAN_POINT('Ctrl Pts',(-0.866031566390108,1.50001067394612,
1.572910504061)) ;
#84525=CARTESIAN_POINT('Ctrl Pts',(-1.29904734958516,0.750005336973063,
1.61457717072767)) ;
#84526=CARTESIAN_POINT('Ctrl Pts',(-1.73206313278021,1.06058278574021E-16,
1.65624383739433)) ;
#84527=CARTESIAN_POINT('Ctrl Pts',(-1.29904734958516,-0.750005336973063,
1.697910504061)) ;
#84528=CARTESIAN_POINT('Ctrl Pts',(-0.866031566390109,-1.50001067394612,
1.73957717072767)) ;
#84529=CARTESIAN_POINT('Ctrl Pts',(-1.83698327053499E-16,-1.50001067394612,
1.78124383739433)) ;
#84530=CARTESIAN_POINT('Ctrl Pts',(0.866031566390108,-1.50001067394612,
1.822910504061)) ;
#84531=CARTESIAN_POINT('Ctrl Pts',(1.29904734958516,-0.750005336973063,
1.86457717072767)) ;
#84532=CARTESIAN_POINT('Ctrl Pts',(1.73206313278021,-3.18174835722064E-16,
1.90624383739433)) ;
#84533=CARTESIAN_POINT('Ctrl Pts',(1.29904734958516,0.750005336973062,1.947910504061)) ;
#84534=CARTESIAN_POINT('Ctrl Pts',(0.866031566390109,1.50001067394612,1.98957717072767)) ;
#84535=CARTESIAN_POINT('Ctrl Pts',(0.,1.50001067394612,2.03124383739433)) ;
#84536=CARTESIAN_POINT('Ctrl Pts',(-0.866031566390108,1.50001067394612,
2.072910504061)) ;
#84537=CARTESIAN_POINT('Ctrl Pts',(-1.29904734958516,0.750005336973063,
2.11457717072767)) ;
#84538=CARTESIAN_POINT('Ctrl Pts',(-1.73206313278021,1.06058278574021E-16,
2.15624383739433)) ;
#84539=CARTESIAN_POINT('Ctrl Pts',(-1.29904734958516,-0.750005336973063,
2.197910504061)) ;
#84540=CARTESIAN_POINT('Ctrl Pts',(-0.866031566390109,-1.50001067394612,
2.23957717072767)) ;
#84541=CARTESIAN_POINT('Ctrl Pts',(-1.83698327053499E-16,-1.50001067394612,
2.28124383739433)) ;
#84542=CARTESIAN_POINT('Ctrl Pts',(0.866031566390108,-1.50001067394612,
2.322910504061)) ;
#84543=CARTESIAN_POINT('Ctrl Pts',(1.29904734958516,-0.750005336973063,
2.36457717072767)) ;
#84544=CARTESIAN_POINT('Ctrl Pts',(1.73206313278021,-3.18174835722064E-16,
2.40624383739433)) ;
#84545=CARTESIAN_POINT('Ctrl Pts',(1.29904734958516,0.750005336973062,2.447910504061)) ;
#84546=CARTESIAN_POINT('Ctrl Pts',(0.866031566390109,1.50001067394612,2.48957717072767)) ;
#84547=CARTESIAN_POINT('Ctrl Pts',(0.,1.50001067394612,2.53124383739433)) ;
#84548=CARTESIAN_POINT('Ctrl Pts',(-0.866031566390108,1.50001067394612,
2.572910504061)) ;
#84549=CARTESIAN_POINT('Ctrl Pts',(-1.29904734958516,0.750005336973063,
2.61457717072767)) ;
#84550=CARTESIAN_POINT('Ctrl Pts',(-1.73206313278021,1.06058278574021E-16,
2.65624383739433)) ;
#84551=CARTESIAN_POINT('Ctrl Pts',(-1.29904734958516,-0.750005336973063,
2.697910504061)) ;
#84552=CARTESIAN_POINT('Ctrl Pts',(-0.866031566390109,-1.50001067394612,
2.73957717072767)) ;
#84553=CARTESIAN_POINT('Ctrl Pts',(-1.83698327053499E-16,-1.50001067394612,
2.78124383739433)) ;
#84554=CARTESIAN_POINT('Ctrl Pts',(0.866031566390108,-1.50001067394612,
2.822910504061)) ;
#84555=CARTESIAN_POINT('Ctrl Pts',(1.29904734958516,-0.750005336973063,
2.86457717072767)) ;
#84556=CARTESIAN_POINT('Ctrl Pts',(1.73206313278021,-3.18174835722064E-16,
2.90624383739433)) ;
#84557=CARTESIAN_POINT('Ctrl Pts',(1.29904734958516,0.750005336973062,2.947910504061)) ;
#84558=CARTESIAN_POINT('Ctrl Pts',(0.866031566390109,1.50001067394612,2.98957717072767)) ;
#84559=CARTESIAN_POINT('Ctrl Pts',(0.,1.50001067394612,3.03124383739433)) ;
#84560=CARTESIAN_POINT('Ctrl Pts',(-0.866031566390108,1.50001067394612,
3.072910504061)) ;
#84561=CARTESIAN_POINT('Ctrl Pts',(-1.29904734958516,0.750005336973063,
3.11457717072766)) ;
#84562=CARTESIAN_POINT('Ctrl Pts',(-1.73206313278021,1.06058278574021E-16,
3.15624383739433)) ;
#84563=CARTESIAN_POINT('Ctrl Pts',(-1.29904734958516,-0.750005336973063,
3.197910504061)) ;
#84564=CARTESIAN_POINT('Ctrl Pts',(-0.866031566390109,-1.50001067394612,
3.23957717072767)) ;
#84565=CARTESIAN_POINT('Ctrl Pts',(-1.83698327053499E-16,-1.50001067394612,
3.28124383739433)) ;
#84566=CARTESIAN_POINT('Ctrl Pts',(0.866031566390108,-1.50001067394612,
3.32291050406099)) ;
#84567=CARTESIAN_POINT('Ctrl Pts',(1.29904734958516,-0.750005336973063,
3.36457717072766)) ;
#84568=CARTESIAN_POINT('Ctrl Pts',(1.73206313278021,-3.18174835722064E-16,
3.40624383739432)) ;
#84569=CARTESIAN_POINT('Ctrl Pts',(1.29904734958516,0.750005336973062,3.447910504061)) ;
#84570=CARTESIAN_POINT('Ctrl Pts',(0.866031566390109,1.50001067394612,3.48957717072766)) ;
#84571=CARTESIAN_POINT('Ctrl Pts',(0.,1.50001067394612,3.53124383739433)) ;
#84572=CARTESIAN_POINT('Ctrl Pts',(-0.866031566390108,1.50001067394612,
3.572910504061)) ;
#84573=CARTESIAN_POINT('Ctrl Pts',(-1.29904734958516,0.750005336973063,
3.61457717072766)) ;
#84574=CARTESIAN_POINT('Ctrl Pts',(-1.73206313278021,1.06058278574021E-16,
3.65624383739433)) ;
#84575=CARTESIAN_POINT('Ctrl Pts',(-1.29904734958516,-0.750005336973063,
3.697910504061)) ;
#84576=CARTESIAN_POINT('Ctrl Pts',(-0.866031566390109,-1.50001067394612,
3.73957717072766)) ;
#84577=CARTESIAN_POINT('Ctrl Pts',(-1.83698327053499E-16,-1.50001067394612,
3.78124383739433)) ;
#84578=CARTESIAN_POINT('Ctrl Pts',(0.866031566390108,-1.50001067394612,
3.822910504061)) ;
#84579=CARTESIAN_POINT('Ctrl Pts',(1.29904734958516,-0.750005336973063,
3.86457717072766)) ;
#84580=CARTESIAN_POINT('Ctrl Pts',(1.73206313278021,-3.18174835722064E-16,
3.90624383739433)) ;
#84581=CARTESIAN_POINT('Ctrl Pts',(1.29904734958516,0.750005336973062,3.947910504061)) ;
#84582=CARTESIAN_POINT('Ctrl Pts',(0.866031566390109,1.50001067394612,3.98957717072766)) ;
#84583=CARTESIAN_POINT('Ctrl Pts',(0.,1.50001067394612,4.03124383739433)) ;
#84584=CARTESIAN_POINT('Ctrl Pts',(-0.866031566390108,1.50001067394612,
4.07291050406099)) ;
#84585=CARTESIAN_POINT('Ctrl Pts',(-1.29904734958516,0.750005336973063,
4.11457717072766)) ;
#84586=CARTESIAN_POINT('Ctrl Pts',(-1.73206313278021,1.06058278574021E-16,
4.15624383739433)) ;
#84587=CARTESIAN_POINT('Ctrl Pts',(-1.29904734958516,-0.750005336973063,
4.197910504061)) ;
#84588=CARTESIAN_POINT('Ctrl Pts',(-0.866031566390109,-1.50001067394612,
4.23957717072765)) ;
#84589=CARTESIAN_POINT('Ctrl Pts',(-1.83698327053499E-16,-1.50001067394612,
4.28124383739433)) ;
#84590=CARTESIAN_POINT('Ctrl Pts',(0.866031566390108,-1.50001067394612,
4.322910504061)) ;
#84591=CARTESIAN_POINT('Ctrl Pts',(1.29904734958516,-0.750005336973063,
4.36457717072766)) ;
#84592=CARTESIAN_POINT('Ctrl Pts',(1.73206313278021,-3.18174835722064E-16,
4.40624383739433)) ;
#84593=CARTESIAN_POINT('Ctrl Pts',(1.29904734958516,0.750005336973062,4.447910504061)) ;
#84594=CARTESIAN_POINT('Ctrl Pts',(0.866031566390109,1.50001067394612,4.48957717072766)) ;
#84595=CARTESIAN_POINT('Ctrl Pts',(0.,1.50001067394612,4.53124383739433)) ;
#84596=CARTESIAN_POINT('Ctrl Pts',(-0.866031566390108,1.50001067394612,
4.572910504061)) ;
#84597=CARTESIAN_POINT('Ctrl Pts',(-1.29904734958516,0.750005336973063,
4.61457717072766)) ;
#84598=CARTESIAN_POINT('Ctrl Pts',(-1.73206313278021,1.06058278574021E-16,
4.65624383739433)) ;
#84599=CARTESIAN_POINT('Ctrl Pts',(-1.29904734958516,-0.750005336973063,
4.69791050406099)) ;
#84600=CARTESIAN_POINT('Ctrl Pts',(-0.866031566390109,-1.50001067394612,
4.73957717072766)) ;
#84601=CARTESIAN_POINT('Ctrl Pts',(-1.83698327053499E-16,-1.50001067394612,
4.78124383739433)) ;
#84602=CARTESIAN_POINT('Ctrl Pts',(0.866031566390108,-1.50001067394612,
4.822910504061)) ;
#84603=CARTESIAN_POINT('Ctrl Pts',(1.29904734958516,-0.750005336973063,
4.86457717072765)) ;
#84604=CARTESIAN_POINT('Ctrl Pts',(1.73206313278021,-3.18174835722064E-16,
4.90624383739433)) ;
#84605=CARTESIAN_POINT('Ctrl Pts',(1.29904734958516,0.750005336973062,4.94791050406099)) ;
#84606=CARTESIAN_POINT('Ctrl Pts',(0.866031566390109,1.50001067394612,4.98957717072766)) ;
#84607=CARTESIAN_POINT('Ctrl Pts',(0.,1.50001067394612,5.03124383739433)) ;
#84608=CARTESIAN_POINT('Ctrl Pts',(-0.866031566390108,1.50001067394612,
5.07291050406099)) ;
#84609=CARTESIAN_POINT('Ctrl Pts',(-1.29904734958516,0.750005336973063,
5.11457717072766)) ;
#84610=CARTESIAN_POINT('Ctrl Pts',(-1.73206313278021,1.06058278574021E-16,
5.15624383739433)) ;
#84611=CARTESIAN_POINT('Ctrl Pts',(-1.29904734958516,-0.750005336973063,
5.19791050406099)) ;
#84612=CARTESIAN_POINT('Ctrl Pts',(-0.866031566390109,-1.50001067394612,
5.23957717072765)) ;
#84613=CARTESIAN_POINT('Ctrl Pts',(-1.83698327053499E-16,-1.50001067394612,
5.28124383739433)) ;
#84614=CARTESIAN_POINT('Ctrl Pts',(0.866031566390108,-1.50001067394612,
5.32291050406099)) ;
#84615=CARTESIAN_POINT('Ctrl Pts',(1.29904734958516,-0.750005336973063,
5.36457717072766)) ;
#84616=CARTESIAN_POINT('Ctrl Pts',(1.73206313278021,-3.18174835722064E-16,
5.40624383739433)) ;
#84617=CARTESIAN_POINT('Ctrl Pts',(1.29904734958516,0.750005336973062,5.44791050406099)) ;
#84618=CARTESIAN_POINT('Ctrl Pts',(0.866031566390109,1.50001067394612,5.48957717072765)) ;
#84619=CARTESIAN_POINT('Ctrl Pts',(0.,1.50001067394612,5.53124383739433)) ;
#84620=CARTESIAN_POINT('Ctrl Pts',(-0.866031566390108,1.50001067394612,
5.57291050406099)) ;
#84621=CARTESIAN_POINT('Ctrl Pts',(-1.29904734958516,0.750005336973063,
5.61457717072766)) ;
#84622=CARTESIAN_POINT('Ctrl Pts',(-1.73206313278021,1.06058278574021E-16,
5.65624383739433)) ;
#84623=CARTESIAN_POINT('Ctrl Pts',(-1.29904734958516,-0.750005336973063,
5.69791050406099)) ;
#84624=CARTESIAN_POINT('Ctrl Pts',(-0.866031566390109,-1.50001067394612,
5.73957717072766)) ;
#84625=CARTESIAN_POINT('Ctrl Pts',(-1.83698327053499E-16,-1.50001067394612,
5.78124383739433)) ;
#84626=CARTESIAN_POINT('Ctrl Pts',(0.866031566390108,-1.50001067394612,
5.82291050406099)) ;
#84627=CARTESIAN_POINT('Ctrl Pts',(1.29904734958516,-0.750005336973063,
5.86457717072765)) ;
#84628=CARTESIAN_POINT('Ctrl Pts',(1.73206313278021,-3.18174835722064E-16,
5.90624383739431)) ;
#84629=CARTESIAN_POINT('Ctrl Pts',(1.29904734958516,0.750005336973062,5.94791050406099)) ;
#84630=CARTESIAN_POINT('Ctrl Pts',(0.866031566390109,1.50001067394612,5.98957717072766)) ;
#84631=CARTESIAN_POINT('Ctrl Pts',(0.,1.50001067394612,6.03124383739433)) ;
#84632=CARTESIAN_POINT('Ctrl Pts',(-0.866031566390108,1.50001067394612,
6.07291050406099)) ;
#84633=CARTESIAN_POINT('Ctrl Pts',(-1.29904734958516,0.750005336973063,
6.11457717072765)) ;
#84634=CARTESIAN_POINT('Ctrl Pts',(-1.73206313278021,1.06058278574021E-16,
6.15624383739433)) ;
#84635=CARTESIAN_POINT('Ctrl Pts',(-1.29904734958516,-0.750005336973063,
6.19791050406099)) ;
#84636=CARTESIAN_POINT('Ctrl Pts',(-0.866031566390109,-1.50001067394612,
6.23957717072766)) ;
#84637=CARTESIAN_POINT('Ctrl Pts',(-1.83698327053499E-16,-1.50001067394612,
6.28124383739432)) ;
#84638=CARTESIAN_POINT('Ctrl Pts',(0.866031566390108,-1.50001067394612,
6.32291050406099)) ;
#84639=CARTESIAN_POINT('Ctrl Pts',(1.29904734958516,-0.750005336973063,
6.36457717072766)) ;
#84640=CARTESIAN_POINT('Ctrl Pts',(1.73206313278021,-3.18174835722064E-16,
6.40624383739432)) ;
#84641=CARTESIAN_POINT('Ctrl Pts',(1.29904734958516,0.750005336973062,6.44791050406099)) ;
#84642=CARTESIAN_POINT('Ctrl Pts',(0.866031566390109,1.50001067394612,6.48957717072766)) ;
#84643=CARTESIAN_POINT('Ctrl Pts',(0.,1.50001067394612,6.53124383739432)) ;
#84644=CARTESIAN_POINT('Ctrl Pts',(-0.866031566390108,1.50001067394612,
6.57291050406099)) ;
#84645=CARTESIAN_POINT('Ctrl Pts',(-1.29904734958516,0.750005336973063,
6.61457717072766)) ;
#84646=CARTESIAN_POINT('Ctrl Pts',(-1.73206313278021,1.06058278574021E-16,
6.65624383739432)) ;
#84647=CARTESIAN_POINT('Ctrl Pts',(-1.29904734958516,-0.750005336973063,
6.69791050406099)) ;
#84648=CARTESIAN_POINT('Ctrl Pts',(-0.866031566390109,-1.50001067394612,
6.73957717072765)) ;
#84649=CARTESIAN_POINT('Ctrl Pts',(-1.83698327053499E-16,-1.50001067394612,
6.78124383739432)) ;
#84650=CARTESIAN_POINT('Ctrl Pts',(0.866031566390108,-1.50001067394612,
6.82291050406099)) ;
#84651=CARTESIAN_POINT('Ctrl Pts',(1.29904734958516,-0.750005336973063,
6.86457717072766)) ;
#84652=CARTESIAN_POINT('Ctrl Pts',(1.73206313278021,-3.18174835722064E-16,
6.90624383739432)) ;
#84653=CARTESIAN_POINT('Ctrl Pts',(1.29904734958516,0.750005336973062,6.94791050406099)) ;
#84654=CARTESIAN_POINT('Ctrl Pts',(0.866031566390109,1.50001067394612,6.98957717072766)) ;
#84655=CARTESIAN_POINT('Ctrl Pts',(0.,1.50001067394612,7.03124383739432)) ;
#84656=CARTESIAN_POINT('Ctrl Pts',(-0.866031566390108,1.50001067394612,
7.07291050406099)) ;
#84657=CARTESIAN_POINT('Ctrl Pts',(-1.29904734958516,0.750005336973063,
7.11457717072766)) ;
#84658=CARTESIAN_POINT('Ctrl Pts',(-1.73206313278021,1.06058278574021E-16,
7.15624383739432)) ;
#84659=CARTESIAN_POINT('Ctrl Pts',(-1.29904734958516,-0.750005336973063,
7.19791050406099)) ;
#84660=CARTESIAN_POINT('Ctrl Pts',(-0.866031566390109,-1.50001067394612,
7.23957717072766)) ;
#84661=CARTESIAN_POINT('Ctrl Pts',(-1.83698327053499E-16,-1.50001067394612,
7.28124383739432)) ;
#84662=CARTESIAN_POINT('Ctrl Pts',(0.866031566390108,-1.50001067394612,
7.32291050406099)) ;
#84663=CARTESIAN_POINT('Ctrl Pts',(1.29904734958516,-0.750005336973063,
7.36457717072765)) ;
#84664=CARTESIAN_POINT('Ctrl Pts',(1.73206313278021,-3.18174835722064E-16,
7.40624383739432)) ;
#84665=CARTESIAN_POINT('Ctrl Pts',(1.29904734958516,0.750005336973062,7.44791050406099)) ;
#84666=CARTESIAN_POINT('Ctrl Pts',(0.866031566390109,1.50001067394612,7.48957717072766)) ;
#84667=CARTESIAN_POINT('Ctrl Pts',(0.,1.50001067394612,7.53124383739432)) ;
#84668=CARTESIAN_POINT('Ctrl Pts',(-0.866031566390108,1.50001067394612,
7.57291050406099)) ;
#84669=CARTESIAN_POINT('Ctrl Pts',(-1.29904734958516,0.750005336973063,
7.61457717072766)) ;
#84670=CARTESIAN_POINT('Ctrl Pts',(-1.73206313278021,1.06058278574021E-16,
7.65624383739432)) ;
#84671=CARTESIAN_POINT('Ctrl Pts',(-1.29904734958516,-0.750005336973063,
7.69791050406099)) ;
#84672=CARTESIAN_POINT('Ctrl Pts',(-0.866031566390109,-1.50001067394612,
7.73957717072766)) ;
#84673=CARTESIAN_POINT('Ctrl Pts',(-1.83698327053499E-16,-1.50001067394612,
7.78124383739432)) ;
#84674=CARTESIAN_POINT('Ctrl Pts',(0.866031566390108,-1.50001067394612,
7.82291050406099)) ;
#84675=CARTESIAN_POINT('Ctrl Pts',(1.29904734958516,-0.750005336973063,
7.86457717072766)) ;
#84676=CARTESIAN_POINT('Ctrl Pts',(1.73206313278021,-3.18174835722064E-16,
7.90624383739432)) ;
#84677=CARTESIAN_POINT('Ctrl Pts',(1.29904734958516,0.750005336973062,7.94791050406099)) ;
#84678=CARTESIAN_POINT('Ctrl Pts',(0.866031566390109,1.50001067394612,7.98957717072765)) ;
#84679=CARTESIAN_POINT('Ctrl Pts',(0.,1.50001067394612,8.03124383739432)) ;
#84680=CARTESIAN_POINT('Ctrl Pts',(-0.866031566390108,1.50001067394612,
8.07291050406099)) ;
#84681=CARTESIAN_POINT('Ctrl Pts',(-1.29904734958516,0.750005336973063,
8.11457717072765)) ;
#84682=CARTESIAN_POINT('Ctrl Pts',(-1.73206313278021,1.06058278574021E-16,
8.15624383739432)) ;
#84683=CARTESIAN_POINT('Ctrl Pts',(-1.29904734958516,-0.750005336973063,
8.19791050406099)) ;
#84684=CARTESIAN_POINT('Ctrl Pts',(-0.866031566390109,-1.50001067394612,
8.23957717072765)) ;
#84685=CARTESIAN_POINT('Ctrl Pts',(-1.83698327053499E-16,-1.50001067394612,
8.28124383739432)) ;
#84686=CARTESIAN_POINT('Ctrl Pts',(0.866031566390108,-1.50001067394612,
8.32291050406099)) ;
#84687=CARTESIAN_POINT('Ctrl Pts',(1.29904734958516,-0.750005336973063,
8.36457717072766)) ;
#84688=CARTESIAN_POINT('Ctrl Pts',(1.73206313278021,-3.18174835722064E-16,
8.40624383739432)) ;
#84689=CARTESIAN_POINT('Ctrl Pts',(1.29904734958516,0.750005336973062,8.44791050406099)) ;
#84690=CARTESIAN_POINT('Ctrl Pts',(0.866031566390109,1.50001067394612,8.48957717072766)) ;
#84691=CARTESIAN_POINT('Ctrl Pts',(0.,1.50001067394612,8.53124383739432)) ;
#84692=CARTESIAN_POINT('Ctrl Pts',(-0.866031566390108,1.50001067394612,
8.57291050406099)) ;
#84693=CARTESIAN_POINT('Ctrl Pts',(-1.29904734958516,0.750005336973063,
8.61457717072765)) ;
#84694=CARTESIAN_POINT('Ctrl Pts',(-1.73206313278021,1.06058278574021E-16,
8.65624383739432)) ;
#84695=CARTESIAN_POINT('Ctrl Pts',(-1.29904734958516,-0.750005336973063,
8.69791050406099)) ;
#84696=CARTESIAN_POINT('Ctrl Pts',(-0.866031566390109,-1.50001067394612,
8.73957717072765)) ;
#84697=CARTESIAN_POINT('Ctrl Pts',(-1.83698327053499E-16,-1.50001067394612,
8.78124383739432)) ;
#84698=CARTESIAN_POINT('Ctrl Pts',(0.866031566390108,-1.50001067394612,
8.82291050406099)) ;
#84699=CARTESIAN_POINT('Ctrl Pts',(1.29904734958516,-0.750005336973063,
8.86457717072765)) ;
#84700=CARTESIAN_POINT('Ctrl Pts',(1.73206313278021,-3.18174835722064E-16,
8.90624383739432)) ;
#84701=CARTESIAN_POINT('Ctrl Pts',(1.29904734958516,0.750005336973062,8.94791050406099)) ;
#84702=CARTESIAN_POINT('Ctrl Pts',(0.866031566390109,1.50001067394612,8.98957717072765)) ;
#84703=CARTESIAN_POINT('Ctrl Pts',(0.,1.50001067394612,9.03124383739432)) ;
#84704=CARTESIAN_POINT('Ctrl Pts',(0.00319785405614896,1.1752361228587,
0.218553781470594)) ;
#84705=CARTESIAN_POINT('Ctrl Pts',(-0.677458612502694,1.17708821028189,
0.260285648324568)) ;
#84706=CARTESIAN_POINT('Ctrl Pts',(-1.01778810567666,0.587620236790419,
0.302083333333337)) ;
#84707=CARTESIAN_POINT('Ctrl Pts',(-1.35705080756888,8.30953963884779E-17,
0.343750000000004)) ;
#84708=CARTESIAN_POINT('Ctrl Pts',(-1.01778810567666,-0.587620236790419,
0.38541666666667)) ;
#84709=CARTESIAN_POINT('Ctrl Pts',(-0.67852540378444,-1.17524047358084,
0.427083333333337)) ;
#84710=CARTESIAN_POINT('Ctrl Pts',(-1.43925448419919E-16,-1.17524047358084,
0.468750000000003)) ;
#84711=CARTESIAN_POINT('Ctrl Pts',(0.678525403784439,-1.17524047358084,
0.51041666666667)) ;
#84712=CARTESIAN_POINT('Ctrl Pts',(1.01778810567666,-0.587620236790419,
0.552083333333337)) ;
#84713=CARTESIAN_POINT('Ctrl Pts',(1.35705080756888,-2.49286189165434E-16,
0.593750000000003)) ;
#84714=CARTESIAN_POINT('Ctrl Pts',(1.01778810567666,0.587620236790418,0.63541666666667)) ;
#84715=CARTESIAN_POINT('Ctrl Pts',(0.67852540378444,1.17524047358084,0.677083333333336)) ;
#84716=CARTESIAN_POINT('Ctrl Pts',(0.,1.17524047358084,0.718750000000003)) ;
#84717=CARTESIAN_POINT('Ctrl Pts',(-0.67852540378444,1.17524047358084,0.76041666666667)) ;
#84718=CARTESIAN_POINT('Ctrl Pts',(-1.01778810567666,0.587620236790419,
0.802083333333336)) ;
#84719=CARTESIAN_POINT('Ctrl Pts',(-1.35705080756888,8.30953963884779E-17,
0.843750000000003)) ;
#84720=CARTESIAN_POINT('Ctrl Pts',(-1.01778810567666,-0.587620236790419,
0.885416666666669)) ;
#84721=CARTESIAN_POINT('Ctrl Pts',(-0.67852540378444,-1.17524047358084,
0.927083333333336)) ;
#84722=CARTESIAN_POINT('Ctrl Pts',(-1.43925448419919E-16,-1.17524047358084,
0.968750000000002)) ;
#84723=CARTESIAN_POINT('Ctrl Pts',(0.678525403784439,-1.17524047358084,
1.01041666666667)) ;
#84724=CARTESIAN_POINT('Ctrl Pts',(1.01778810567666,-0.587620236790419,
1.05208333333334)) ;
#84725=CARTESIAN_POINT('Ctrl Pts',(1.35705080756888,-2.49286189165434E-16,
1.09375)) ;
#84726=CARTESIAN_POINT('Ctrl Pts',(1.01778810567666,0.587620236790418,1.13541666666667)) ;
#84727=CARTESIAN_POINT('Ctrl Pts',(0.67852540378444,1.17524047358084,1.17708333333334)) ;
#84728=CARTESIAN_POINT('Ctrl Pts',(0.,1.17524047358084,1.21875)) ;
#84729=CARTESIAN_POINT('Ctrl Pts',(-0.67852540378444,1.17524047358084,1.26041666666667)) ;
#84730=CARTESIAN_POINT('Ctrl Pts',(-1.01778810567666,0.587620236790419,
1.30208333333334)) ;
#84731=CARTESIAN_POINT('Ctrl Pts',(-1.35705080756888,8.30953963884779E-17,
1.34375)) ;
#84732=CARTESIAN_POINT('Ctrl Pts',(-1.01778810567666,-0.587620236790419,
1.38541666666667)) ;
#84733=CARTESIAN_POINT('Ctrl Pts',(-0.67852540378444,-1.17524047358084,
1.42708333333334)) ;
#84734=CARTESIAN_POINT('Ctrl Pts',(-1.43925448419919E-16,-1.17524047358084,
1.46875)) ;
#84735=CARTESIAN_POINT('Ctrl Pts',(0.678525403784439,-1.17524047358084,
1.51041666666667)) ;
#84736=CARTESIAN_POINT('Ctrl Pts',(1.01778810567666,-0.587620236790419,
1.55208333333333)) ;
#84737=CARTESIAN_POINT('Ctrl Pts',(1.35705080756888,-2.49286189165434E-16,
1.59375)) ;
#84738=CARTESIAN_POINT('Ctrl Pts',(1.01778810567666,0.587620236790418,1.63541666666667)) ;
#84739=CARTESIAN_POINT('Ctrl Pts',(0.67852540378444,1.17524047358084,1.67708333333333)) ;
#84740=CARTESIAN_POINT('Ctrl Pts',(0.,1.17524047358084,1.71875)) ;
#84741=CARTESIAN_POINT('Ctrl Pts',(-0.67852540378444,1.17524047358084,1.76041666666667)) ;
#84742=CARTESIAN_POINT('Ctrl Pts',(-1.01778810567666,0.587620236790419,
1.80208333333333)) ;
#84743=CARTESIAN_POINT('Ctrl Pts',(-1.35705080756888,8.30953963884779E-17,
1.84375)) ;
#84744=CARTESIAN_POINT('Ctrl Pts',(-1.01778810567666,-0.587620236790419,
1.88541666666667)) ;
#84745=CARTESIAN_POINT('Ctrl Pts',(-0.67852540378444,-1.17524047358084,
1.92708333333333)) ;
#84746=CARTESIAN_POINT('Ctrl Pts',(-1.43925448419919E-16,-1.17524047358084,
1.96875)) ;
#84747=CARTESIAN_POINT('Ctrl Pts',(0.678525403784439,-1.17524047358084,
2.01041666666667)) ;
#84748=CARTESIAN_POINT('Ctrl Pts',(1.01778810567666,-0.587620236790419,
2.05208333333333)) ;
#84749=CARTESIAN_POINT('Ctrl Pts',(1.35705080756888,-2.49286189165434E-16,
2.09375)) ;
#84750=CARTESIAN_POINT('Ctrl Pts',(1.01778810567666,0.587620236790418,2.13541666666667)) ;
#84751=CARTESIAN_POINT('Ctrl Pts',(0.67852540378444,1.17524047358084,2.17708333333333)) ;
#84752=CARTESIAN_POINT('Ctrl Pts',(0.,1.17524047358084,2.21875)) ;
#84753=CARTESIAN_POINT('Ctrl Pts',(-0.67852540378444,1.17524047358084,2.26041666666667)) ;
#84754=CARTESIAN_POINT('Ctrl Pts',(-1.01778810567666,0.587620236790419,
2.30208333333333)) ;
#84755=CARTESIAN_POINT('Ctrl Pts',(-1.35705080756888,8.30953963884779E-17,
2.34375)) ;
#84756=CARTESIAN_POINT('Ctrl Pts',(-1.01778810567666,-0.587620236790419,
2.38541666666667)) ;
#84757=CARTESIAN_POINT('Ctrl Pts',(-0.67852540378444,-1.17524047358084,
2.42708333333333)) ;
#84758=CARTESIAN_POINT('Ctrl Pts',(-1.43925448419919E-16,-1.17524047358084,
2.46875)) ;
#84759=CARTESIAN_POINT('Ctrl Pts',(0.678525403784439,-1.17524047358084,
2.51041666666667)) ;
#84760=CARTESIAN_POINT('Ctrl Pts',(1.01778810567666,-0.587620236790419,
2.55208333333333)) ;
#84761=CARTESIAN_POINT('Ctrl Pts',(1.35705080756888,-2.49286189165434E-16,
2.59375)) ;
#84762=CARTESIAN_POINT('Ctrl Pts',(1.01778810567666,0.587620236790418,2.63541666666667)) ;
#84763=CARTESIAN_POINT('Ctrl Pts',(0.67852540378444,1.17524047358084,2.67708333333333)) ;
#84764=CARTESIAN_POINT('Ctrl Pts',(0.,1.17524047358084,2.71875)) ;
#84765=CARTESIAN_POINT('Ctrl Pts',(-0.67852540378444,1.17524047358084,2.76041666666667)) ;
#84766=CARTESIAN_POINT('Ctrl Pts',(-1.01778810567666,0.587620236790419,
2.80208333333333)) ;
#84767=CARTESIAN_POINT('Ctrl Pts',(-1.35705080756888,8.30953963884779E-17,
2.84375)) ;
#84768=CARTESIAN_POINT('Ctrl Pts',(-1.01778810567666,-0.587620236790419,
2.88541666666667)) ;
#84769=CARTESIAN_POINT('Ctrl Pts',(-0.67852540378444,-1.17524047358084,
2.92708333333333)) ;
#84770=CARTESIAN_POINT('Ctrl Pts',(-1.43925448419919E-16,-1.17524047358084,
2.96875)) ;
#84771=CARTESIAN_POINT('Ctrl Pts',(0.678525403784439,-1.17524047358084,
3.01041666666666)) ;
#84772=CARTESIAN_POINT('Ctrl Pts',(1.01778810567666,-0.587620236790419,
3.05208333333333)) ;
#84773=CARTESIAN_POINT('Ctrl Pts',(1.35705080756888,-2.49286189165434E-16,
3.09375)) ;
#84774=CARTESIAN_POINT('Ctrl Pts',(1.01778810567666,0.587620236790418,3.13541666666666)) ;
#84775=CARTESIAN_POINT('Ctrl Pts',(0.67852540378444,1.17524047358084,3.17708333333333)) ;
#84776=CARTESIAN_POINT('Ctrl Pts',(0.,1.17524047358084,3.21875)) ;
#84777=CARTESIAN_POINT('Ctrl Pts',(-0.67852540378444,1.17524047358084,3.26041666666666)) ;
#84778=CARTESIAN_POINT('Ctrl Pts',(-1.01778810567666,0.587620236790419,
3.30208333333333)) ;
#84779=CARTESIAN_POINT('Ctrl Pts',(-1.35705080756888,8.30953963884779E-17,
3.34375)) ;
#84780=CARTESIAN_POINT('Ctrl Pts',(-1.01778810567666,-0.587620236790419,
3.38541666666666)) ;
#84781=CARTESIAN_POINT('Ctrl Pts',(-0.67852540378444,-1.17524047358084,
3.42708333333333)) ;
#84782=CARTESIAN_POINT('Ctrl Pts',(-1.43925448419919E-16,-1.17524047358084,
3.46875)) ;
#84783=CARTESIAN_POINT('Ctrl Pts',(0.678525403784439,-1.17524047358084,
3.51041666666666)) ;
#84784=CARTESIAN_POINT('Ctrl Pts',(1.01778810567666,-0.587620236790419,
3.55208333333333)) ;
#84785=CARTESIAN_POINT('Ctrl Pts',(1.35705080756888,-2.49286189165434E-16,
3.59375)) ;
#84786=CARTESIAN_POINT('Ctrl Pts',(1.01778810567666,0.587620236790418,3.63541666666666)) ;
#84787=CARTESIAN_POINT('Ctrl Pts',(0.67852540378444,1.17524047358084,3.67708333333333)) ;
#84788=CARTESIAN_POINT('Ctrl Pts',(0.,1.17524047358084,3.71875)) ;
#84789=CARTESIAN_POINT('Ctrl Pts',(-0.67852540378444,1.17524047358084,3.76041666666666)) ;
#84790=CARTESIAN_POINT('Ctrl Pts',(-1.01778810567666,0.587620236790419,
3.80208333333333)) ;
#84791=CARTESIAN_POINT('Ctrl Pts',(-1.35705080756888,8.30953963884779E-17,
3.84375)) ;
#84792=CARTESIAN_POINT('Ctrl Pts',(-1.01778810567666,-0.587620236790419,
3.88541666666666)) ;
#84793=CARTESIAN_POINT('Ctrl Pts',(-0.67852540378444,-1.17524047358084,
3.92708333333333)) ;
#84794=CARTESIAN_POINT('Ctrl Pts',(-1.43925448419919E-16,-1.17524047358084,
3.96875)) ;
#84795=CARTESIAN_POINT('Ctrl Pts',(0.678525403784439,-1.17524047358084,
4.01041666666666)) ;
#84796=CARTESIAN_POINT('Ctrl Pts',(1.01778810567666,-0.587620236790419,
4.05208333333333)) ;
#84797=CARTESIAN_POINT('Ctrl Pts',(1.35705080756888,-2.49286189165434E-16,
4.09375)) ;
#84798=CARTESIAN_POINT('Ctrl Pts',(1.01778810567666,0.587620236790418,4.13541666666666)) ;
#84799=CARTESIAN_POINT('Ctrl Pts',(0.67852540378444,1.17524047358084,4.17708333333333)) ;
#84800=CARTESIAN_POINT('Ctrl Pts',(0.,1.17524047358084,4.21874999999999)) ;
#84801=CARTESIAN_POINT('Ctrl Pts',(-0.67852540378444,1.17524047358084,4.26041666666666)) ;
#84802=CARTESIAN_POINT('Ctrl Pts',(-1.01778810567666,0.587620236790419,
4.30208333333333)) ;
#84803=CARTESIAN_POINT('Ctrl Pts',(-1.35705080756888,8.30953963884779E-17,
4.34374999999999)) ;
#84804=CARTESIAN_POINT('Ctrl Pts',(-1.01778810567666,-0.587620236790419,
4.38541666666666)) ;
#84805=CARTESIAN_POINT('Ctrl Pts',(-0.67852540378444,-1.17524047358084,
4.42708333333333)) ;
#84806=CARTESIAN_POINT('Ctrl Pts',(-1.43925448419919E-16,-1.17524047358084,
4.46874999999999)) ;
#84807=CARTESIAN_POINT('Ctrl Pts',(0.678525403784439,-1.17524047358084,
4.51041666666666)) ;
#84808=CARTESIAN_POINT('Ctrl Pts',(1.01778810567666,-0.587620236790419,
4.55208333333333)) ;
#84809=CARTESIAN_POINT('Ctrl Pts',(1.35705080756888,-2.49286189165434E-16,
4.59374999999999)) ;
#84810=CARTESIAN_POINT('Ctrl Pts',(1.01778810567666,0.587620236790418,4.63541666666666)) ;
#84811=CARTESIAN_POINT('Ctrl Pts',(0.67852540378444,1.17524047358084,4.67708333333333)) ;
#84812=CARTESIAN_POINT('Ctrl Pts',(0.,1.17524047358084,4.71874999999999)) ;
#84813=CARTESIAN_POINT('Ctrl Pts',(-0.67852540378444,1.17524047358084,4.76041666666666)) ;
#84814=CARTESIAN_POINT('Ctrl Pts',(-1.01778810567666,0.587620236790419,
4.80208333333333)) ;
#84815=CARTESIAN_POINT('Ctrl Pts',(-1.35705080756888,8.30953963884779E-17,
4.84374999999999)) ;
#84816=CARTESIAN_POINT('Ctrl Pts',(-1.01778810567666,-0.587620236790419,
4.88541666666666)) ;
#84817=CARTESIAN_POINT('Ctrl Pts',(-0.67852540378444,-1.17524047358084,
4.92708333333333)) ;
#84818=CARTESIAN_POINT('Ctrl Pts',(-1.43925448419919E-16,-1.17524047358084,
4.96874999999999)) ;
#84819=CARTESIAN_POINT('Ctrl Pts',(0.678525403784439,-1.17524047358084,
5.01041666666666)) ;
#84820=CARTESIAN_POINT('Ctrl Pts',(1.01778810567666,-0.587620236790419,
5.05208333333333)) ;
#84821=CARTESIAN_POINT('Ctrl Pts',(1.35705080756888,-2.49286189165434E-16,
5.09374999999999)) ;
#84822=CARTESIAN_POINT('Ctrl Pts',(1.01778810567666,0.587620236790418,5.13541666666666)) ;
#84823=CARTESIAN_POINT('Ctrl Pts',(0.67852540378444,1.17524047358084,5.17708333333333)) ;
#84824=CARTESIAN_POINT('Ctrl Pts',(0.,1.17524047358084,5.21874999999999)) ;
#84825=CARTESIAN_POINT('Ctrl Pts',(-0.67852540378444,1.17524047358084,5.26041666666666)) ;
#84826=CARTESIAN_POINT('Ctrl Pts',(-1.01778810567666,0.587620236790419,
5.30208333333333)) ;
#84827=CARTESIAN_POINT('Ctrl Pts',(-1.35705080756888,8.30953963884779E-17,
5.34374999999999)) ;
#84828=CARTESIAN_POINT('Ctrl Pts',(-1.01778810567666,-0.587620236790419,
5.38541666666666)) ;
#84829=CARTESIAN_POINT('Ctrl Pts',(-0.67852540378444,-1.17524047358084,
5.42708333333333)) ;
#84830=CARTESIAN_POINT('Ctrl Pts',(-1.43925448419919E-16,-1.17524047358084,
5.46874999999999)) ;
#84831=CARTESIAN_POINT('Ctrl Pts',(0.678525403784439,-1.17524047358084,
5.51041666666666)) ;
#84832=CARTESIAN_POINT('Ctrl Pts',(1.01778810567666,-0.587620236790419,
5.55208333333333)) ;
#84833=CARTESIAN_POINT('Ctrl Pts',(1.35705080756888,-2.49286189165434E-16,
5.59374999999999)) ;
#84834=CARTESIAN_POINT('Ctrl Pts',(1.01778810567666,0.587620236790418,5.63541666666666)) ;
#84835=CARTESIAN_POINT('Ctrl Pts',(0.67852540378444,1.17524047358084,5.67708333333333)) ;
#84836=CARTESIAN_POINT('Ctrl Pts',(0.,1.17524047358084,5.71874999999999)) ;
#84837=CARTESIAN_POINT('Ctrl Pts',(-0.67852540378444,1.17524047358084,5.76041666666666)) ;
#84838=CARTESIAN_POINT('Ctrl Pts',(-1.01778810567666,0.587620236790419,
5.80208333333333)) ;
#84839=CARTESIAN_POINT('Ctrl Pts',(-1.35705080756888,8.30953963884779E-17,
5.84374999999999)) ;
#84840=CARTESIAN_POINT('Ctrl Pts',(-1.01778810567666,-0.587620236790419,
5.88541666666666)) ;
#84841=CARTESIAN_POINT('Ctrl Pts',(-0.67852540378444,-1.17524047358084,
5.92708333333333)) ;
#84842=CARTESIAN_POINT('Ctrl Pts',(-1.43925448419919E-16,-1.17524047358084,
5.96874999999999)) ;
#84843=CARTESIAN_POINT('Ctrl Pts',(0.678525403784439,-1.17524047358084,
6.01041666666666)) ;
#84844=CARTESIAN_POINT('Ctrl Pts',(1.01778810567666,-0.587620236790419,
6.05208333333333)) ;
#84845=CARTESIAN_POINT('Ctrl Pts',(1.35705080756888,-2.49286189165434E-16,
6.09374999999999)) ;
#84846=CARTESIAN_POINT('Ctrl Pts',(1.01778810567666,0.587620236790418,6.13541666666666)) ;
#84847=CARTESIAN_POINT('Ctrl Pts',(0.67852540378444,1.17524047358084,6.17708333333332)) ;
#84848=CARTESIAN_POINT('Ctrl Pts',(0.,1.17524047358084,6.21874999999999)) ;
#84849=CARTESIAN_POINT('Ctrl Pts',(-0.67852540378444,1.17524047358084,6.26041666666666)) ;
#84850=CARTESIAN_POINT('Ctrl Pts',(-1.01778810567666,0.587620236790419,
6.30208333333332)) ;
#84851=CARTESIAN_POINT('Ctrl Pts',(-1.35705080756888,8.30953963884779E-17,
6.34374999999999)) ;
#84852=CARTESIAN_POINT('Ctrl Pts',(-1.01778810567666,-0.587620236790419,
6.38541666666666)) ;
#84853=CARTESIAN_POINT('Ctrl Pts',(-0.67852540378444,-1.17524047358084,
6.42708333333332)) ;
#84854=CARTESIAN_POINT('Ctrl Pts',(-1.43925448419919E-16,-1.17524047358084,
6.46874999999999)) ;
#84855=CARTESIAN_POINT('Ctrl Pts',(0.678525403784439,-1.17524047358084,
6.51041666666666)) ;
#84856=CARTESIAN_POINT('Ctrl Pts',(1.01778810567666,-0.587620236790419,
6.55208333333332)) ;
#84857=CARTESIAN_POINT('Ctrl Pts',(1.35705080756888,-2.49286189165434E-16,
6.59374999999999)) ;
#84858=CARTESIAN_POINT('Ctrl Pts',(1.01778810567666,0.587620236790418,6.63541666666666)) ;
#84859=CARTESIAN_POINT('Ctrl Pts',(0.67852540378444,1.17524047358084,6.67708333333332)) ;
#84860=CARTESIAN_POINT('Ctrl Pts',(0.,1.17524047358084,6.71874999999999)) ;
#84861=CARTESIAN_POINT('Ctrl Pts',(-0.67852540378444,1.17524047358084,6.76041666666666)) ;
#84862=CARTESIAN_POINT('Ctrl Pts',(-1.01778810567666,0.587620236790419,
6.80208333333332)) ;
#84863=CARTESIAN_POINT('Ctrl Pts',(-1.35705080756888,8.30953963884779E-17,
6.84374999999999)) ;
#84864=CARTESIAN_POINT('Ctrl Pts',(-1.01778810567666,-0.587620236790419,
6.88541666666666)) ;
#84865=CARTESIAN_POINT('Ctrl Pts',(-0.67852540378444,-1.17524047358084,
6.92708333333332)) ;
#84866=CARTESIAN_POINT('Ctrl Pts',(-1.43925448419919E-16,-1.17524047358084,
6.96874999999999)) ;
#84867=CARTESIAN_POINT('Ctrl Pts',(0.678525403784439,-1.17524047358084,
7.01041666666666)) ;
#84868=CARTESIAN_POINT('Ctrl Pts',(1.01778810567666,-0.587620236790419,
7.05208333333332)) ;
#84869=CARTESIAN_POINT('Ctrl Pts',(1.35705080756888,-2.49286189165434E-16,
7.09374999999999)) ;
#84870=CARTESIAN_POINT('Ctrl Pts',(1.01778810567666,0.587620236790418,7.13541666666666)) ;
#84871=CARTESIAN_POINT('Ctrl Pts',(0.67852540378444,1.17524047358084,7.17708333333332)) ;
#84872=CARTESIAN_POINT('Ctrl Pts',(0.,1.17524047358084,7.21874999999999)) ;
#84873=CARTESIAN_POINT('Ctrl Pts',(-0.67852540378444,1.17524047358084,7.26041666666666)) ;
#84874=CARTESIAN_POINT('Ctrl Pts',(-1.01778810567666,0.587620236790419,
7.30208333333332)) ;
#84875=CARTESIAN_POINT('Ctrl Pts',(-1.35705080756888,8.30953963884779E-17,
7.34374999999999)) ;
#84876=CARTESIAN_POINT('Ctrl Pts',(-1.01778810567666,-0.587620236790419,
7.38541666666666)) ;
#84877=CARTESIAN_POINT('Ctrl Pts',(-0.67852540378444,-1.17524047358084,
7.42708333333332)) ;
#84878=CARTESIAN_POINT('Ctrl Pts',(-1.43925448419919E-16,-1.17524047358084,
7.46874999999999)) ;
#84879=CARTESIAN_POINT('Ctrl Pts',(0.678525403784439,-1.17524047358084,
7.51041666666666)) ;
#84880=CARTESIAN_POINT('Ctrl Pts',(1.01778810567666,-0.587620236790419,
7.55208333333332)) ;
#84881=CARTESIAN_POINT('Ctrl Pts',(1.35705080756888,-2.49286189165434E-16,
7.59374999999999)) ;
#84882=CARTESIAN_POINT('Ctrl Pts',(1.01778810567666,0.587620236790418,7.63541666666665)) ;
#84883=CARTESIAN_POINT('Ctrl Pts',(0.67852540378444,1.17524047358084,7.67708333333332)) ;
#84884=CARTESIAN_POINT('Ctrl Pts',(0.,1.17524047358084,7.71874999999999)) ;
#84885=CARTESIAN_POINT('Ctrl Pts',(-0.67852540378444,1.17524047358084,7.76041666666666)) ;
#84886=CARTESIAN_POINT('Ctrl Pts',(-1.01778810567666,0.587620236790419,
7.80208333333332)) ;
#84887=CARTESIAN_POINT('Ctrl Pts',(-1.35705080756888,8.30953963884779E-17,
7.84374999999999)) ;
#84888=CARTESIAN_POINT('Ctrl Pts',(-1.01778810567666,-0.587620236790419,
7.88541666666665)) ;
#84889=CARTESIAN_POINT('Ctrl Pts',(-0.67852540378444,-1.17524047358084,
7.92708333333332)) ;
#84890=CARTESIAN_POINT('Ctrl Pts',(-1.43925448419919E-16,-1.17524047358084,
7.96874999999999)) ;
#84891=CARTESIAN_POINT('Ctrl Pts',(0.678525403784439,-1.17524047358084,
8.01041666666665)) ;
#84892=CARTESIAN_POINT('Ctrl Pts',(1.01778810567666,-0.587620236790419,
8.05208333333332)) ;
#84893=CARTESIAN_POINT('Ctrl Pts',(1.35705080756888,-2.49286189165434E-16,
8.09374999999999)) ;
#84894=CARTESIAN_POINT('Ctrl Pts',(1.01778810567666,0.587620236790418,8.13541666666665)) ;
#84895=CARTESIAN_POINT('Ctrl Pts',(0.67852540378444,1.17524047358084,8.17708333333332)) ;
#84896=CARTESIAN_POINT('Ctrl Pts',(0.,1.17524047358084,8.21874999999999)) ;
#84897=CARTESIAN_POINT('Ctrl Pts',(-0.67852540378444,1.17524047358084,8.26041666666665)) ;
#84898=CARTESIAN_POINT('Ctrl Pts',(-1.01778810567666,0.587620236790419,
8.30208333333332)) ;
#84899=CARTESIAN_POINT('Ctrl Pts',(-1.35705080756888,8.30953963884779E-17,
8.34374999999999)) ;
#84900=CARTESIAN_POINT('Ctrl Pts',(-1.01778810567666,-0.587620236790419,
8.38541666666665)) ;
#84901=CARTESIAN_POINT('Ctrl Pts',(-0.67852540378444,-1.17524047358084,
8.42708333333332)) ;
#84902=CARTESIAN_POINT('Ctrl Pts',(-1.43925448419919E-16,-1.17524047358084,
8.46874999999999)) ;
#84903=CARTESIAN_POINT('Ctrl Pts',(0.678525403784439,-1.17524047358084,
8.51041666666665)) ;
#84904=CARTESIAN_POINT('Ctrl Pts',(1.01778810567666,-0.587620236790419,
8.55208333333332)) ;
#84905=CARTESIAN_POINT('Ctrl Pts',(1.35705080756888,-2.49286189165434E-16,
8.59374999999999)) ;
#84906=CARTESIAN_POINT('Ctrl Pts',(1.01778810567666,0.587620236790418,8.63541666666665)) ;
#84907=CARTESIAN_POINT('Ctrl Pts',(0.67852540378444,1.17524047358084,8.67708333333332)) ;
#84908=CARTESIAN_POINT('Ctrl Pts',(0.,1.17524047358084,8.71874999999999)) ;
#84909=CARTESIAN_POINT('Ctrl Pts',(-0.67852540378444,1.17524047358084,8.76041666666665)) ;
#84910=CARTESIAN_POINT('Ctrl Pts',(-1.01778810567666,0.587620236790419,
8.80208333333332)) ;
#84911=CARTESIAN_POINT('Ctrl Pts',(-1.35705080756888,8.30953963884779E-17,
8.84374999999998)) ;
#84912=CARTESIAN_POINT('Ctrl Pts',(-1.01778810567666,-0.587620236790419,
8.88541666666665)) ;
#84913=CARTESIAN_POINT('Ctrl Pts',(-0.67852540378444,-1.17524047358084,
8.92708333333332)) ;
#84914=CARTESIAN_POINT('Ctrl Pts',(-1.43925448419919E-16,-1.17524047358084,
8.96874999999999)) ;
#84915=CARTESIAN_POINT('Ctrl Pts',(0.678525403784439,-1.17524047358084,
9.01041666666665)) ;
#84916=CARTESIAN_POINT('Ctrl Pts',(1.01778810567666,-0.587620236790419,
9.05208333333332)) ;
#84917=CARTESIAN_POINT('Ctrl Pts',(1.35705080756888,-2.49286189165434E-16,
9.09374999999999)) ;
#84918=CARTESIAN_POINT('Ctrl Pts',(1.01778810567666,0.587620236790418,9.13541666666665)) ;
#84919=CARTESIAN_POINT('Ctrl Pts',(0.67852540378444,1.17524047358084,9.17708333333332)) ;
#84920=CARTESIAN_POINT('Ctrl Pts',(0.,1.17524047358084,9.21874999999998)) ;
#84921=CARTESIAN_POINT('',(0.,1.5,0.03125)) ;
#84922=CARTESIAN_POINT('Ctrl Pts',(0.,1.17524047358084,-0.218749999999996)) ;
#84923=CARTESIAN_POINT('Ctrl Pts',(-0.67852540378444,1.17524047358084,-0.17708333333333)) ;
#84924=CARTESIAN_POINT('Ctrl Pts',(-1.01778810567666,0.587620236790419,
-0.135416666666663)) ;
#84925=CARTESIAN_POINT('Ctrl Pts',(-1.35705080756888,8.30953963884779E-17,
-0.0937499999999966)) ;
#84926=CARTESIAN_POINT('Ctrl Pts',(-1.01778810567666,-0.587620236790419,
-0.05208333333333)) ;
#84927=CARTESIAN_POINT('Ctrl Pts',(-0.67852540378444,-1.17524047358084,
-0.0104166666666634)) ;
#84928=CARTESIAN_POINT('Ctrl Pts',(-1.43925448419919E-16,-1.17524047358084,
0.0312500000000032)) ;
#84929=CARTESIAN_POINT('Ctrl Pts',(0.678525403784439,-1.17524047358084,
0.0729166666666698)) ;
#84930=CARTESIAN_POINT('Ctrl Pts',(1.01778810567666,-0.587620236790419,
0.114583333333336)) ;
#84931=CARTESIAN_POINT('Ctrl Pts',(1.35705080756888,-2.49286189165434E-16,
0.156250000000003)) ;
#84932=CARTESIAN_POINT('Ctrl Pts',(1.01778810567666,0.587620236790418,0.19791666666667)) ;
#84933=CARTESIAN_POINT('Ctrl Pts',(0.67852540378444,1.17524047358084,0.239583333333336)) ;
#84934=CARTESIAN_POINT('Ctrl Pts',(0.,1.17524047358084,0.281250000000003)) ;
#84935=CARTESIAN_POINT('Ctrl Pts',(-0.67852540378444,1.17524047358084,0.322916666666669)) ;
#84936=CARTESIAN_POINT('Ctrl Pts',(-1.01778810567666,0.587620236790419,
0.364583333333336)) ;
#84937=CARTESIAN_POINT('Ctrl Pts',(-1.35705080756888,8.30953963884779E-17,
0.406250000000002)) ;
#84938=CARTESIAN_POINT('Ctrl Pts',(-1.01778810567666,-0.587620236790419,
0.447916666666669)) ;
#84939=CARTESIAN_POINT('Ctrl Pts',(-0.67852540378444,-1.17524047358084,
0.489583333333336)) ;
#84940=CARTESIAN_POINT('Ctrl Pts',(-1.43925448419919E-16,-1.17524047358084,
0.531250000000002)) ;
#84941=CARTESIAN_POINT('Ctrl Pts',(0.678525403784439,-1.17524047358084,
0.572916666666669)) ;
#84942=CARTESIAN_POINT('Ctrl Pts',(1.01778810567666,-0.587620236790419,
0.614583333333335)) ;
#84943=CARTESIAN_POINT('Ctrl Pts',(1.35705080756888,-2.49286189165434E-16,
0.656250000000002)) ;
#84944=CARTESIAN_POINT('Ctrl Pts',(1.01778810567666,0.587620236790418,0.697916666666669)) ;
#84945=CARTESIAN_POINT('Ctrl Pts',(0.67852540378444,1.17524047358084,0.739583333333335)) ;
#84946=CARTESIAN_POINT('Ctrl Pts',(0.,1.17524047358084,0.781250000000002)) ;
#84947=CARTESIAN_POINT('Ctrl Pts',(-0.67852540378444,1.17524047358084,0.822916666666668)) ;
#84948=CARTESIAN_POINT('Ctrl Pts',(-1.01778810567666,0.587620236790419,
0.864583333333335)) ;
#84949=CARTESIAN_POINT('Ctrl Pts',(-1.35705080756888,8.30953963884779E-17,
0.906250000000001)) ;
#84950=CARTESIAN_POINT('Ctrl Pts',(-1.01778810567666,-0.587620236790419,
0.947916666666668)) ;
#84951=CARTESIAN_POINT('Ctrl Pts',(-0.67852540378444,-1.17524047358084,
0.989583333333335)) ;
#84952=CARTESIAN_POINT('Ctrl Pts',(-1.43925448419919E-16,-1.17524047358084,
1.03125)) ;
#84953=CARTESIAN_POINT('Ctrl Pts',(0.678525403784439,-1.17524047358084,
1.07291666666667)) ;
#84954=CARTESIAN_POINT('Ctrl Pts',(1.01778810567666,-0.587620236790419,
1.11458333333333)) ;
#84955=CARTESIAN_POINT('Ctrl Pts',(1.35705080756888,-2.49286189165434E-16,
1.15625)) ;
#84956=CARTESIAN_POINT('Ctrl Pts',(1.01778810567666,0.587620236790418,1.19791666666667)) ;
#84957=CARTESIAN_POINT('Ctrl Pts',(0.67852540378444,1.17524047358084,1.23958333333333)) ;
#84958=CARTESIAN_POINT('Ctrl Pts',(0.,1.17524047358084,1.28125)) ;
#84959=CARTESIAN_POINT('Ctrl Pts',(-0.67852540378444,1.17524047358084,1.32291666666667)) ;
#84960=CARTESIAN_POINT('Ctrl Pts',(-1.01778810567666,0.587620236790419,
1.36458333333333)) ;
#84961=CARTESIAN_POINT('Ctrl Pts',(-1.35705080756888,8.30953963884779E-17,
1.40625)) ;
#84962=CARTESIAN_POINT('Ctrl Pts',(-1.01778810567666,-0.587620236790419,
1.44791666666667)) ;
#84963=CARTESIAN_POINT('Ctrl Pts',(-0.67852540378444,-1.17524047358084,
1.48958333333333)) ;
#84964=CARTESIAN_POINT('Ctrl Pts',(-1.43925448419919E-16,-1.17524047358084,
1.53125)) ;
#84965=CARTESIAN_POINT('Ctrl Pts',(0.678525403784439,-1.17524047358084,
1.57291666666667)) ;
#84966=CARTESIAN_POINT('Ctrl Pts',(1.01778810567666,-0.587620236790419,
1.61458333333333)) ;
#84967=CARTESIAN_POINT('Ctrl Pts',(1.35705080756888,-2.49286189165434E-16,
1.65625)) ;
#84968=CARTESIAN_POINT('Ctrl Pts',(1.01778810567666,0.587620236790418,1.69791666666667)) ;
#84969=CARTESIAN_POINT('Ctrl Pts',(0.67852540378444,1.17524047358084,1.73958333333333)) ;
#84970=CARTESIAN_POINT('Ctrl Pts',(0.,1.17524047358084,1.78125)) ;
#84971=CARTESIAN_POINT('Ctrl Pts',(-0.67852540378444,1.17524047358084,1.82291666666667)) ;
#84972=CARTESIAN_POINT('Ctrl Pts',(-1.01778810567666,0.587620236790419,
1.86458333333333)) ;
#84973=CARTESIAN_POINT('Ctrl Pts',(-1.35705080756888,8.30953963884779E-17,
1.90625)) ;
#84974=CARTESIAN_POINT('Ctrl Pts',(-1.01778810567666,-0.587620236790419,
1.94791666666667)) ;
#84975=CARTESIAN_POINT('Ctrl Pts',(-0.67852540378444,-1.17524047358084,
1.98958333333333)) ;
#84976=CARTESIAN_POINT('Ctrl Pts',(-1.43925448419919E-16,-1.17524047358084,
2.03125)) ;
#84977=CARTESIAN_POINT('Ctrl Pts',(0.678525403784439,-1.17524047358084,
2.07291666666667)) ;
#84978=CARTESIAN_POINT('Ctrl Pts',(1.01778810567666,-0.587620236790419,
2.11458333333333)) ;
#84979=CARTESIAN_POINT('Ctrl Pts',(1.35705080756888,-2.49286189165434E-16,
2.15625)) ;
#84980=CARTESIAN_POINT('Ctrl Pts',(1.01778810567666,0.587620236790418,2.19791666666667)) ;
#84981=CARTESIAN_POINT('Ctrl Pts',(0.67852540378444,1.17524047358084,2.23958333333333)) ;
#84982=CARTESIAN_POINT('Ctrl Pts',(0.,1.17524047358084,2.28125)) ;
#84983=CARTESIAN_POINT('Ctrl Pts',(-0.67852540378444,1.17524047358084,2.32291666666667)) ;
#84984=CARTESIAN_POINT('Ctrl Pts',(-1.01778810567666,0.587620236790419,
2.36458333333333)) ;
#84985=CARTESIAN_POINT('Ctrl Pts',(-1.35705080756888,8.30953963884779E-17,
2.40625)) ;
#84986=CARTESIAN_POINT('Ctrl Pts',(-1.01778810567666,-0.587620236790419,
2.44791666666666)) ;
#84987=CARTESIAN_POINT('Ctrl Pts',(-0.67852540378444,-1.17524047358084,
2.48958333333333)) ;
#84988=CARTESIAN_POINT('Ctrl Pts',(-1.43925448419919E-16,-1.17524047358084,
2.53125)) ;
#84989=CARTESIAN_POINT('Ctrl Pts',(0.678525403784439,-1.17524047358084,
2.57291666666666)) ;
#84990=CARTESIAN_POINT('Ctrl Pts',(1.01778810567666,-0.587620236790419,
2.61458333333333)) ;
#84991=CARTESIAN_POINT('Ctrl Pts',(1.35705080756888,-2.49286189165434E-16,
2.65625)) ;
#84992=CARTESIAN_POINT('Ctrl Pts',(1.01778810567666,0.587620236790418,2.69791666666666)) ;
#84993=CARTESIAN_POINT('Ctrl Pts',(0.67852540378444,1.17524047358084,2.73958333333333)) ;
#84994=CARTESIAN_POINT('Ctrl Pts',(0.,1.17524047358084,2.78125)) ;
#84995=CARTESIAN_POINT('Ctrl Pts',(-0.67852540378444,1.17524047358084,2.82291666666666)) ;
#84996=CARTESIAN_POINT('Ctrl Pts',(-1.01778810567666,0.587620236790419,
2.86458333333333)) ;
#84997=CARTESIAN_POINT('Ctrl Pts',(-1.35705080756888,8.30953963884779E-17,
2.90625)) ;
#84998=CARTESIAN_POINT('Ctrl Pts',(-1.01778810567666,-0.587620236790419,
2.94791666666666)) ;
#84999=CARTESIAN_POINT('Ctrl Pts',(-0.67852540378444,-1.17524047358084,
2.98958333333333)) ;
#85000=CARTESIAN_POINT('Ctrl Pts',(-1.43925448419919E-16,-1.17524047358084,
3.03125)) ;
#85001=CARTESIAN_POINT('Ctrl Pts',(0.678525403784439,-1.17524047358084,
3.07291666666666)) ;
#85002=CARTESIAN_POINT('Ctrl Pts',(1.01778810567666,-0.587620236790419,
3.11458333333333)) ;
#85003=CARTESIAN_POINT('Ctrl Pts',(1.35705080756888,-2.49286189165434E-16,
3.15625)) ;
#85004=CARTESIAN_POINT('Ctrl Pts',(1.01778810567666,0.587620236790418,3.19791666666666)) ;
#85005=CARTESIAN_POINT('Ctrl Pts',(0.67852540378444,1.17524047358084,3.23958333333333)) ;
#85006=CARTESIAN_POINT('Ctrl Pts',(0.,1.17524047358084,3.28125)) ;
#85007=CARTESIAN_POINT('Ctrl Pts',(-0.67852540378444,1.17524047358084,3.32291666666666)) ;
#85008=CARTESIAN_POINT('Ctrl Pts',(-1.01778810567666,0.587620236790419,
3.36458333333333)) ;
#85009=CARTESIAN_POINT('Ctrl Pts',(-1.35705080756888,8.30953963884779E-17,
3.40625)) ;
#85010=CARTESIAN_POINT('Ctrl Pts',(-1.01778810567666,-0.587620236790419,
3.44791666666666)) ;
#85011=CARTESIAN_POINT('Ctrl Pts',(-0.67852540378444,-1.17524047358084,
3.48958333333333)) ;
#85012=CARTESIAN_POINT('Ctrl Pts',(-1.43925448419919E-16,-1.17524047358084,
3.53125)) ;
#85013=CARTESIAN_POINT('Ctrl Pts',(0.678525403784439,-1.17524047358084,
3.57291666666666)) ;
#85014=CARTESIAN_POINT('Ctrl Pts',(1.01778810567666,-0.587620236790419,
3.61458333333333)) ;
#85015=CARTESIAN_POINT('Ctrl Pts',(1.35705080756888,-2.49286189165434E-16,
3.65625)) ;
#85016=CARTESIAN_POINT('Ctrl Pts',(1.01778810567666,0.587620236790418,3.69791666666666)) ;
#85017=CARTESIAN_POINT('Ctrl Pts',(0.67852540378444,1.17524047358084,3.73958333333333)) ;
#85018=CARTESIAN_POINT('Ctrl Pts',(0.,1.17524047358084,3.78125)) ;
#85019=CARTESIAN_POINT('Ctrl Pts',(-0.67852540378444,1.17524047358084,3.82291666666666)) ;
#85020=CARTESIAN_POINT('Ctrl Pts',(-1.01778810567666,0.587620236790419,
3.86458333333333)) ;
#85021=CARTESIAN_POINT('Ctrl Pts',(-1.35705080756888,8.30953963884779E-17,
3.90625)) ;
#85022=CARTESIAN_POINT('Ctrl Pts',(-1.01778810567666,-0.587620236790419,
3.94791666666666)) ;
#85023=CARTESIAN_POINT('Ctrl Pts',(-0.67852540378444,-1.17524047358084,
3.98958333333333)) ;
#85024=CARTESIAN_POINT('Ctrl Pts',(-1.43925448419919E-16,-1.17524047358084,
4.03124999999999)) ;
#85025=CARTESIAN_POINT('Ctrl Pts',(0.678525403784439,-1.17524047358084,
4.07291666666666)) ;
#85026=CARTESIAN_POINT('Ctrl Pts',(1.01778810567666,-0.587620236790419,
4.11458333333333)) ;
#85027=CARTESIAN_POINT('Ctrl Pts',(1.35705080756888,-2.49286189165434E-16,
4.15624999999999)) ;
#85028=CARTESIAN_POINT('Ctrl Pts',(1.01778810567666,0.587620236790418,4.19791666666666)) ;
#85029=CARTESIAN_POINT('Ctrl Pts',(0.67852540378444,1.17524047358084,4.23958333333333)) ;
#85030=CARTESIAN_POINT('Ctrl Pts',(0.,1.17524047358084,4.28124999999999)) ;
#85031=CARTESIAN_POINT('Ctrl Pts',(-0.67852540378444,1.17524047358084,4.32291666666666)) ;
#85032=CARTESIAN_POINT('Ctrl Pts',(-1.01778810567666,0.587620236790419,
4.36458333333333)) ;
#85033=CARTESIAN_POINT('Ctrl Pts',(-1.35705080756888,8.30953963884779E-17,
4.40624999999999)) ;
#85034=CARTESIAN_POINT('Ctrl Pts',(-1.01778810567666,-0.587620236790419,
4.44791666666666)) ;
#85035=CARTESIAN_POINT('Ctrl Pts',(-0.67852540378444,-1.17524047358084,
4.48958333333333)) ;
#85036=CARTESIAN_POINT('Ctrl Pts',(-1.43925448419919E-16,-1.17524047358084,
4.53124999999999)) ;
#85037=CARTESIAN_POINT('Ctrl Pts',(0.678525403784439,-1.17524047358084,
4.57291666666666)) ;
#85038=CARTESIAN_POINT('Ctrl Pts',(1.01778810567666,-0.587620236790419,
4.61458333333333)) ;
#85039=CARTESIAN_POINT('Ctrl Pts',(1.35705080756888,-2.49286189165434E-16,
4.65624999999999)) ;
#85040=CARTESIAN_POINT('Ctrl Pts',(1.01778810567666,0.587620236790418,4.69791666666666)) ;
#85041=CARTESIAN_POINT('Ctrl Pts',(0.67852540378444,1.17524047358084,4.73958333333333)) ;
#85042=CARTESIAN_POINT('Ctrl Pts',(0.,1.17524047358084,4.78124999999999)) ;
#85043=CARTESIAN_POINT('Ctrl Pts',(-0.67852540378444,1.17524047358084,4.82291666666666)) ;
#85044=CARTESIAN_POINT('Ctrl Pts',(-1.01778810567666,0.587620236790419,
4.86458333333333)) ;
#85045=CARTESIAN_POINT('Ctrl Pts',(-1.35705080756888,8.30953963884779E-17,
4.90624999999999)) ;
#85046=CARTESIAN_POINT('Ctrl Pts',(-1.01778810567666,-0.587620236790419,
4.94791666666666)) ;
#85047=CARTESIAN_POINT('Ctrl Pts',(-0.67852540378444,-1.17524047358084,
4.98958333333333)) ;
#85048=CARTESIAN_POINT('Ctrl Pts',(-1.43925448419919E-16,-1.17524047358084,
5.03124999999999)) ;
#85049=CARTESIAN_POINT('Ctrl Pts',(0.678525403784439,-1.17524047358084,
5.07291666666666)) ;
#85050=CARTESIAN_POINT('Ctrl Pts',(1.01778810567666,-0.587620236790419,
5.11458333333333)) ;
#85051=CARTESIAN_POINT('Ctrl Pts',(1.35705080756888,-2.49286189165434E-16,
5.15624999999999)) ;
#85052=CARTESIAN_POINT('Ctrl Pts',(1.01778810567666,0.587620236790418,5.19791666666666)) ;
#85053=CARTESIAN_POINT('Ctrl Pts',(0.67852540378444,1.17524047358084,5.23958333333332)) ;
#85054=CARTESIAN_POINT('Ctrl Pts',(0.,1.17524047358084,5.28124999999999)) ;
#85055=CARTESIAN_POINT('Ctrl Pts',(-0.67852540378444,1.17524047358084,5.32291666666666)) ;
#85056=CARTESIAN_POINT('Ctrl Pts',(-1.01778810567666,0.587620236790419,
5.36458333333333)) ;
#85057=CARTESIAN_POINT('Ctrl Pts',(-1.35705080756888,8.30953963884779E-17,
5.40624999999999)) ;
#85058=CARTESIAN_POINT('Ctrl Pts',(-1.01778810567666,-0.587620236790419,
5.44791666666666)) ;
#85059=CARTESIAN_POINT('Ctrl Pts',(-0.67852540378444,-1.17524047358084,
5.48958333333333)) ;
#85060=CARTESIAN_POINT('Ctrl Pts',(-1.43925448419919E-16,-1.17524047358084,
5.53124999999999)) ;
#85061=CARTESIAN_POINT('Ctrl Pts',(0.678525403784439,-1.17524047358084,
5.57291666666666)) ;
#85062=CARTESIAN_POINT('Ctrl Pts',(1.01778810567666,-0.587620236790419,
5.61458333333332)) ;
#85063=CARTESIAN_POINT('Ctrl Pts',(1.35705080756888,-2.49286189165434E-16,
5.65624999999999)) ;
#85064=CARTESIAN_POINT('Ctrl Pts',(1.01778810567666,0.587620236790418,5.69791666666666)) ;
#85065=CARTESIAN_POINT('Ctrl Pts',(0.67852540378444,1.17524047358084,5.73958333333333)) ;
#85066=CARTESIAN_POINT('Ctrl Pts',(0.,1.17524047358084,5.78124999999999)) ;
#85067=CARTESIAN_POINT('Ctrl Pts',(-0.67852540378444,1.17524047358084,5.82291666666666)) ;
#85068=CARTESIAN_POINT('Ctrl Pts',(-1.01778810567666,0.587620236790419,
5.86458333333332)) ;
#85069=CARTESIAN_POINT('Ctrl Pts',(-1.35705080756888,8.30953963884779E-17,
5.90624999999999)) ;
#85070=CARTESIAN_POINT('Ctrl Pts',(-1.01778810567666,-0.587620236790419,
5.94791666666666)) ;
#85071=CARTESIAN_POINT('Ctrl Pts',(-0.67852540378444,-1.17524047358084,
5.98958333333333)) ;
#85072=CARTESIAN_POINT('Ctrl Pts',(-1.43925448419919E-16,-1.17524047358084,
6.03124999999999)) ;
#85073=CARTESIAN_POINT('Ctrl Pts',(0.678525403784439,-1.17524047358084,
6.07291666666666)) ;
#85074=CARTESIAN_POINT('Ctrl Pts',(1.01778810567666,-0.587620236790419,
6.11458333333332)) ;
#85075=CARTESIAN_POINT('Ctrl Pts',(1.35705080756888,-2.49286189165434E-16,
6.15624999999999)) ;
#85076=CARTESIAN_POINT('Ctrl Pts',(1.01778810567666,0.587620236790418,6.19791666666666)) ;
#85077=CARTESIAN_POINT('Ctrl Pts',(0.67852540378444,1.17524047358084,6.23958333333332)) ;
#85078=CARTESIAN_POINT('Ctrl Pts',(0.,1.17524047358084,6.28124999999999)) ;
#85079=CARTESIAN_POINT('Ctrl Pts',(-0.67852540378444,1.17524047358084,6.32291666666666)) ;
#85080=CARTESIAN_POINT('Ctrl Pts',(-1.01778810567666,0.587620236790419,
6.36458333333332)) ;
#85081=CARTESIAN_POINT('Ctrl Pts',(-1.35705080756888,8.30953963884779E-17,
6.40624999999999)) ;
#85082=CARTESIAN_POINT('Ctrl Pts',(-1.01778810567666,-0.587620236790419,
6.44791666666666)) ;
#85083=CARTESIAN_POINT('Ctrl Pts',(-0.67852540378444,-1.17524047358084,
6.48958333333332)) ;
#85084=CARTESIAN_POINT('Ctrl Pts',(-1.43925448419919E-16,-1.17524047358084,
6.53124999999999)) ;
#85085=CARTESIAN_POINT('Ctrl Pts',(0.678525403784439,-1.17524047358084,
6.57291666666666)) ;
#85086=CARTESIAN_POINT('Ctrl Pts',(1.01778810567666,-0.587620236790419,
6.61458333333332)) ;
#85087=CARTESIAN_POINT('Ctrl Pts',(1.35705080756888,-2.49286189165434E-16,
6.65624999999999)) ;
#85088=CARTESIAN_POINT('Ctrl Pts',(1.01778810567666,0.587620236790418,6.69791666666666)) ;
#85089=CARTESIAN_POINT('Ctrl Pts',(0.67852540378444,1.17524047358084,6.73958333333332)) ;
#85090=CARTESIAN_POINT('Ctrl Pts',(0.,1.17524047358084,6.78124999999999)) ;
#85091=CARTESIAN_POINT('Ctrl Pts',(-0.67852540378444,1.17524047358084,6.82291666666666)) ;
#85092=CARTESIAN_POINT('Ctrl Pts',(-1.01778810567666,0.587620236790419,
6.86458333333332)) ;
#85093=CARTESIAN_POINT('Ctrl Pts',(-1.35705080756888,8.30953963884779E-17,
6.90624999999999)) ;
#85094=CARTESIAN_POINT('Ctrl Pts',(-1.01778810567666,-0.587620236790419,
6.94791666666665)) ;
#85095=CARTESIAN_POINT('Ctrl Pts',(-0.67852540378444,-1.17524047358084,
6.98958333333332)) ;
#85096=CARTESIAN_POINT('Ctrl Pts',(-1.43925448419919E-16,-1.17524047358084,
7.03124999999999)) ;
#85097=CARTESIAN_POINT('Ctrl Pts',(0.678525403784439,-1.17524047358084,
7.07291666666666)) ;
#85098=CARTESIAN_POINT('Ctrl Pts',(1.01778810567666,-0.587620236790419,
7.11458333333332)) ;
#85099=CARTESIAN_POINT('Ctrl Pts',(1.35705080756888,-2.49286189165434E-16,
7.15624999999999)) ;
#85100=CARTESIAN_POINT('Ctrl Pts',(1.01778810567666,0.587620236790418,7.19791666666666)) ;
#85101=CARTESIAN_POINT('Ctrl Pts',(0.67852540378444,1.17524047358084,7.23958333333332)) ;
#85102=CARTESIAN_POINT('Ctrl Pts',(0.,1.17524047358084,7.28124999999999)) ;
#85103=CARTESIAN_POINT('Ctrl Pts',(-0.67852540378444,1.17524047358084,7.32291666666665)) ;
#85104=CARTESIAN_POINT('Ctrl Pts',(-1.01778810567666,0.587620236790419,
7.36458333333332)) ;
#85105=CARTESIAN_POINT('Ctrl Pts',(-1.35705080756888,8.30953963884779E-17,
7.40624999999999)) ;
#85106=CARTESIAN_POINT('Ctrl Pts',(-1.01778810567666,-0.587620236790419,
7.44791666666665)) ;
#85107=CARTESIAN_POINT('Ctrl Pts',(-0.67852540378444,-1.17524047358084,
7.48958333333332)) ;
#85108=CARTESIAN_POINT('Ctrl Pts',(-1.43925448419919E-16,-1.17524047358084,
7.53124999999999)) ;
#85109=CARTESIAN_POINT('Ctrl Pts',(0.678525403784439,-1.17524047358084,
7.57291666666665)) ;
#85110=CARTESIAN_POINT('Ctrl Pts',(1.01778810567666,-0.587620236790419,
7.61458333333332)) ;
#85111=CARTESIAN_POINT('Ctrl Pts',(1.35705080756888,-2.49286189165434E-16,
7.65624999999999)) ;
#85112=CARTESIAN_POINT('Ctrl Pts',(1.01778810567666,0.587620236790418,7.69791666666665)) ;
#85113=CARTESIAN_POINT('Ctrl Pts',(0.67852540378444,1.17524047358084,7.73958333333332)) ;
#85114=CARTESIAN_POINT('Ctrl Pts',(0.,1.17524047358084,7.78124999999999)) ;
#85115=CARTESIAN_POINT('Ctrl Pts',(-0.67852540378444,1.17524047358084,7.82291666666665)) ;
#85116=CARTESIAN_POINT('Ctrl Pts',(-1.01778810567666,0.587620236790419,
7.86458333333332)) ;
#85117=CARTESIAN_POINT('Ctrl Pts',(-1.35705080756888,8.30953963884779E-17,
7.90624999999999)) ;
#85118=CARTESIAN_POINT('Ctrl Pts',(-1.01778810567666,-0.587620236790419,
7.94791666666665)) ;
#85119=CARTESIAN_POINT('Ctrl Pts',(-0.67852540378444,-1.17524047358084,
7.98958333333332)) ;
#85120=CARTESIAN_POINT('Ctrl Pts',(-1.43925448419919E-16,-1.17524047358084,
8.03124999999999)) ;
#85121=CARTESIAN_POINT('Ctrl Pts',(0.678525403784439,-1.17524047358084,
8.07291666666665)) ;
#85122=CARTESIAN_POINT('Ctrl Pts',(1.01778810567666,-0.587620236790419,
8.11458333333332)) ;
#85123=CARTESIAN_POINT('Ctrl Pts',(1.35705080756888,-2.49286189165434E-16,
8.15624999999999)) ;
#85124=CARTESIAN_POINT('Ctrl Pts',(1.01778810567666,0.587620236790418,8.19791666666665)) ;
#85125=CARTESIAN_POINT('Ctrl Pts',(0.67852540378444,1.17524047358084,8.23958333333332)) ;
#85126=CARTESIAN_POINT('Ctrl Pts',(0.,1.17524047358084,8.28124999999998)) ;
#85127=CARTESIAN_POINT('Ctrl Pts',(-0.67852540378444,1.17524047358084,8.32291666666665)) ;
#85128=CARTESIAN_POINT('Ctrl Pts',(-1.01778810567666,0.587620236790419,
8.36458333333332)) ;
#85129=CARTESIAN_POINT('Ctrl Pts',(-1.35705080756888,8.30953963884779E-17,
8.40624999999999)) ;
#85130=CARTESIAN_POINT('Ctrl Pts',(-1.01778810567666,-0.587620236790419,
8.44791666666665)) ;
#85131=CARTESIAN_POINT('Ctrl Pts',(-0.67852540378444,-1.17524047358084,
8.48958333333332)) ;
#85132=CARTESIAN_POINT('Ctrl Pts',(-1.43925448419919E-16,-1.17524047358084,
8.53124999999999)) ;
#85133=CARTESIAN_POINT('Ctrl Pts',(0.678525403784439,-1.17524047358084,
8.57291666666665)) ;
#85134=CARTESIAN_POINT('Ctrl Pts',(1.01778810567666,-0.587620236790419,
8.61458333333332)) ;
#85135=CARTESIAN_POINT('Ctrl Pts',(1.35705080756888,-2.49286189165434E-16,
8.65624999999998)) ;
#85136=CARTESIAN_POINT('Ctrl Pts',(1.01778810567666,0.587620236790418,8.69791666666665)) ;
#85137=CARTESIAN_POINT('Ctrl Pts',(0.67852540378444,1.17524047358084,8.73958333333332)) ;
#85138=CARTESIAN_POINT('Ctrl Pts',(0.,1.17524047358084,8.78124999999999)) ;
#85139=CARTESIAN_POINT('Ctrl Pts',(0.,1.5,-0.03125)) ;
#85140=CARTESIAN_POINT('Ctrl Pts',(-0.866025403784439,1.5,0.0104166666666666)) ;
#85141=CARTESIAN_POINT('Ctrl Pts',(-1.29903810567666,0.750000000000001,
0.0520833333333332)) ;
#85142=CARTESIAN_POINT('Ctrl Pts',(-1.73205080756888,1.06057523872491E-16,
0.0937499999999997)) ;
#85143=CARTESIAN_POINT('Ctrl Pts',(-1.29903810567666,-0.75,0.135416666666666)) ;
#85144=CARTESIAN_POINT('Ctrl Pts',(-0.866025403784439,-1.5,0.177083333333333)) ;
#85145=CARTESIAN_POINT('Ctrl Pts',(-1.83697019872103E-16,-1.5,0.21875)) ;
#85146=CARTESIAN_POINT('Ctrl Pts',(0.866025403784438,-1.5,0.260416666666666)) ;
#85147=CARTESIAN_POINT('Ctrl Pts',(1.29903810567666,-0.750000000000001,
0.302083333333333)) ;
#85148=CARTESIAN_POINT('Ctrl Pts',(1.73205080756888,-3.18172571617472E-16,
0.343749999999999)) ;
#85149=CARTESIAN_POINT('Ctrl Pts',(1.29903810567666,0.749999999999999,0.385416666666666)) ;
#85150=CARTESIAN_POINT('Ctrl Pts',(0.86602540378444,1.5,0.427083333333332)) ;
#85151=CARTESIAN_POINT('Ctrl Pts',(0.,1.5,0.468749999999999)) ;
#85152=CARTESIAN_POINT('Ctrl Pts',(-0.866025403784439,1.5,0.510416666666666)) ;
#85153=CARTESIAN_POINT('Ctrl Pts',(-1.29903810567666,0.750000000000001,
0.552083333333332)) ;
#85154=CARTESIAN_POINT('Ctrl Pts',(-1.73205080756888,1.06057523872491E-16,
0.593749999999999)) ;
#85155=CARTESIAN_POINT('Ctrl Pts',(-1.29903810567666,-0.75,0.635416666666665)) ;
#85156=CARTESIAN_POINT('Ctrl Pts',(-0.866025403784439,-1.5,0.677083333333332)) ;
#85157=CARTESIAN_POINT('Ctrl Pts',(-1.83697019872103E-16,-1.5,0.718749999999998)) ;
#85158=CARTESIAN_POINT('Ctrl Pts',(0.866025403784438,-1.5,0.760416666666665)) ;
#85159=CARTESIAN_POINT('Ctrl Pts',(1.29903810567666,-0.750000000000001,
0.802083333333332)) ;
#85160=CARTESIAN_POINT('Ctrl Pts',(1.73205080756888,-3.18172571617472E-16,
0.843749999999998)) ;
#85161=CARTESIAN_POINT('Ctrl Pts',(1.29903810567666,0.749999999999999,0.885416666666665)) ;
#85162=CARTESIAN_POINT('Ctrl Pts',(0.86602540378444,1.5,0.927083333333331)) ;
#85163=CARTESIAN_POINT('Ctrl Pts',(0.,1.5,0.968749999999998)) ;
#85164=CARTESIAN_POINT('Ctrl Pts',(-0.866025403784439,1.5,1.01041666666666)) ;
#85165=CARTESIAN_POINT('Ctrl Pts',(-1.29903810567666,0.750000000000001,
1.05208333333333)) ;
#85166=CARTESIAN_POINT('Ctrl Pts',(-1.73205080756888,1.06057523872491E-16,
1.09375)) ;
#85167=CARTESIAN_POINT('Ctrl Pts',(-1.29903810567666,-0.75,1.13541666666666)) ;
#85168=CARTESIAN_POINT('Ctrl Pts',(-0.866025403784439,-1.5,1.17708333333333)) ;
#85169=CARTESIAN_POINT('Ctrl Pts',(-1.83697019872103E-16,-1.5,1.21875)) ;
#85170=CARTESIAN_POINT('Ctrl Pts',(0.866025403784438,-1.5,1.26041666666666)) ;
#85171=CARTESIAN_POINT('Ctrl Pts',(1.29903810567666,-0.750000000000001,
1.30208333333333)) ;
#85172=CARTESIAN_POINT('Ctrl Pts',(1.73205080756888,-3.18172571617472E-16,
1.34375)) ;
#85173=CARTESIAN_POINT('Ctrl Pts',(1.29903810567666,0.749999999999999,1.38541666666666)) ;
#85174=CARTESIAN_POINT('Ctrl Pts',(0.86602540378444,1.5,1.42708333333333)) ;
#85175=CARTESIAN_POINT('Ctrl Pts',(0.,1.5,1.46875)) ;
#85176=CARTESIAN_POINT('Ctrl Pts',(-0.866025403784439,1.5,1.51041666666666)) ;
#85177=CARTESIAN_POINT('Ctrl Pts',(-1.29903810567666,0.750000000000001,
1.55208333333333)) ;
#85178=CARTESIAN_POINT('Ctrl Pts',(-1.73205080756888,1.06057523872491E-16,
1.59375)) ;
#85179=CARTESIAN_POINT('Ctrl Pts',(-1.29903810567666,-0.75,1.63541666666666)) ;
#85180=CARTESIAN_POINT('Ctrl Pts',(-0.866025403784439,-1.5,1.67708333333333)) ;
#85181=CARTESIAN_POINT('Ctrl Pts',(-1.83697019872103E-16,-1.5,1.71875)) ;
#85182=CARTESIAN_POINT('Ctrl Pts',(0.866025403784438,-1.5,1.76041666666666)) ;
#85183=CARTESIAN_POINT('Ctrl Pts',(1.29903810567666,-0.750000000000001,
1.80208333333333)) ;
#85184=CARTESIAN_POINT('Ctrl Pts',(1.73205080756888,-3.18172571617472E-16,
1.84375)) ;
#85185=CARTESIAN_POINT('Ctrl Pts',(1.29903810567666,0.749999999999999,1.88541666666666)) ;
#85186=CARTESIAN_POINT('Ctrl Pts',(0.86602540378444,1.5,1.92708333333333)) ;
#85187=CARTESIAN_POINT('Ctrl Pts',(0.,1.5,1.96875)) ;
#85188=CARTESIAN_POINT('Ctrl Pts',(-0.866025403784439,1.5,2.01041666666666)) ;
#85189=CARTESIAN_POINT('Ctrl Pts',(-1.29903810567666,0.750000000000001,
2.05208333333333)) ;
#85190=CARTESIAN_POINT('Ctrl Pts',(-1.73205080756888,1.06057523872491E-16,
2.09375)) ;
#85191=CARTESIAN_POINT('Ctrl Pts',(-1.29903810567666,-0.75,2.13541666666666)) ;
#85192=CARTESIAN_POINT('Ctrl Pts',(-0.866025403784439,-1.5,2.17708333333333)) ;
#85193=CARTESIAN_POINT('Ctrl Pts',(-1.83697019872103E-16,-1.5,2.21875)) ;
#85194=CARTESIAN_POINT('Ctrl Pts',(0.866025403784438,-1.5,2.26041666666666)) ;
#85195=CARTESIAN_POINT('Ctrl Pts',(1.29903810567666,-0.750000000000001,
2.30208333333333)) ;
#85196=CARTESIAN_POINT('Ctrl Pts',(1.73205080756888,-3.18172571617472E-16,
2.34374999999999)) ;
#85197=CARTESIAN_POINT('Ctrl Pts',(1.29903810567666,0.749999999999999,2.38541666666666)) ;
#85198=CARTESIAN_POINT('Ctrl Pts',(0.86602540378444,1.5,2.42708333333333)) ;
#85199=CARTESIAN_POINT('Ctrl Pts',(0.,1.5,2.46874999999999)) ;
#85200=CARTESIAN_POINT('Ctrl Pts',(-0.866025403784439,1.5,2.51041666666666)) ;
#85201=CARTESIAN_POINT('Ctrl Pts',(-1.29903810567666,0.750000000000001,
2.55208333333333)) ;
#85202=CARTESIAN_POINT('Ctrl Pts',(-1.73205080756888,1.06057523872491E-16,
2.59374999999999)) ;
#85203=CARTESIAN_POINT('Ctrl Pts',(-1.29903810567666,-0.75,2.63541666666666)) ;
#85204=CARTESIAN_POINT('Ctrl Pts',(-0.866025403784439,-1.5,2.67708333333333)) ;
#85205=CARTESIAN_POINT('Ctrl Pts',(-1.83697019872103E-16,-1.5,2.71874999999999)) ;
#85206=CARTESIAN_POINT('Ctrl Pts',(0.866025403784438,-1.5,2.76041666666666)) ;
#85207=CARTESIAN_POINT('Ctrl Pts',(1.29903810567666,-0.750000000000001,
2.80208333333333)) ;
#85208=CARTESIAN_POINT('Ctrl Pts',(1.73205080756888,-3.18172571617472E-16,
2.84374999999999)) ;
#85209=CARTESIAN_POINT('Ctrl Pts',(1.29903810567666,0.749999999999999,2.88541666666666)) ;
#85210=CARTESIAN_POINT('Ctrl Pts',(0.86602540378444,1.5,2.92708333333333)) ;
#85211=CARTESIAN_POINT('Ctrl Pts',(0.,1.5,2.96874999999999)) ;
#85212=CARTESIAN_POINT('Ctrl Pts',(-0.866025403784439,1.5,3.01041666666666)) ;
#85213=CARTESIAN_POINT('Ctrl Pts',(-1.29903810567666,0.750000000000001,
3.05208333333333)) ;
#85214=CARTESIAN_POINT('Ctrl Pts',(-1.73205080756888,1.06057523872491E-16,
3.09374999999999)) ;
#85215=CARTESIAN_POINT('Ctrl Pts',(-1.29903810567666,-0.75,3.13541666666666)) ;
#85216=CARTESIAN_POINT('Ctrl Pts',(-0.866025403784439,-1.5,3.17708333333333)) ;
#85217=CARTESIAN_POINT('Ctrl Pts',(-1.83697019872103E-16,-1.5,3.21874999999999)) ;
#85218=CARTESIAN_POINT('Ctrl Pts',(0.866025403784438,-1.5,3.26041666666666)) ;
#85219=CARTESIAN_POINT('Ctrl Pts',(1.29903810567666,-0.750000000000001,
3.30208333333333)) ;
#85220=CARTESIAN_POINT('Ctrl Pts',(1.73205080756888,-3.18172571617472E-16,
3.34374999999999)) ;
#85221=CARTESIAN_POINT('Ctrl Pts',(1.29903810567666,0.749999999999999,3.38541666666666)) ;
#85222=CARTESIAN_POINT('Ctrl Pts',(0.86602540378444,1.5,3.42708333333333)) ;
#85223=CARTESIAN_POINT('Ctrl Pts',(0.,1.5,3.46874999999999)) ;
#85224=CARTESIAN_POINT('Ctrl Pts',(-0.866025403784439,1.5,3.51041666666666)) ;
#85225=CARTESIAN_POINT('Ctrl Pts',(-1.29903810567666,0.750000000000001,
3.55208333333333)) ;
#85226=CARTESIAN_POINT('Ctrl Pts',(-1.73205080756888,1.06057523872491E-16,
3.59374999999999)) ;
#85227=CARTESIAN_POINT('Ctrl Pts',(-1.29903810567666,-0.75,3.63541666666666)) ;
#85228=CARTESIAN_POINT('Ctrl Pts',(-0.866025403784439,-1.5,3.67708333333333)) ;
#85229=CARTESIAN_POINT('Ctrl Pts',(-1.83697019872103E-16,-1.5,3.71874999999999)) ;
#85230=CARTESIAN_POINT('Ctrl Pts',(0.866025403784438,-1.5,3.76041666666666)) ;
#85231=CARTESIAN_POINT('Ctrl Pts',(1.29903810567666,-0.750000000000001,
3.80208333333333)) ;
#85232=CARTESIAN_POINT('Ctrl Pts',(1.73205080756888,-3.18172571617472E-16,
3.84374999999999)) ;
#85233=CARTESIAN_POINT('Ctrl Pts',(1.29903810567666,0.749999999999999,3.88541666666666)) ;
#85234=CARTESIAN_POINT('Ctrl Pts',(0.86602540378444,1.5,3.92708333333333)) ;
#85235=CARTESIAN_POINT('Ctrl Pts',(0.,1.5,3.96874999999999)) ;
#85236=CARTESIAN_POINT('Ctrl Pts',(-0.866025403784439,1.5,4.01041666666666)) ;
#85237=CARTESIAN_POINT('Ctrl Pts',(-1.29903810567666,0.750000000000001,
4.05208333333332)) ;
#85238=CARTESIAN_POINT('Ctrl Pts',(-1.73205080756888,1.06057523872491E-16,
4.09374999999999)) ;
#85239=CARTESIAN_POINT('Ctrl Pts',(-1.29903810567666,-0.75,4.13541666666666)) ;
#85240=CARTESIAN_POINT('Ctrl Pts',(-0.866025403784439,-1.5,4.17708333333333)) ;
#85241=CARTESIAN_POINT('Ctrl Pts',(-1.83697019872103E-16,-1.5,4.21874999999999)) ;
#85242=CARTESIAN_POINT('Ctrl Pts',(0.866025403784438,-1.5,4.26041666666666)) ;
#85243=CARTESIAN_POINT('Ctrl Pts',(1.29903810567666,-0.750000000000001,
4.30208333333332)) ;
#85244=CARTESIAN_POINT('Ctrl Pts',(1.73205080756888,-3.18172571617472E-16,
4.34374999999999)) ;
#85245=CARTESIAN_POINT('Ctrl Pts',(1.29903810567666,0.749999999999999,4.38541666666666)) ;
#85246=CARTESIAN_POINT('Ctrl Pts',(0.86602540378444,1.5,4.42708333333332)) ;
#85247=CARTESIAN_POINT('Ctrl Pts',(0.,1.5,4.46874999999999)) ;
#85248=CARTESIAN_POINT('Ctrl Pts',(-0.866025403784439,1.5,4.51041666666666)) ;
#85249=CARTESIAN_POINT('Ctrl Pts',(-1.29903810567666,0.750000000000001,
4.55208333333332)) ;
#85250=CARTESIAN_POINT('Ctrl Pts',(-1.73205080756888,1.06057523872491E-16,
4.59374999999999)) ;
#85251=CARTESIAN_POINT('Ctrl Pts',(-1.29903810567666,-0.75,4.63541666666666)) ;
#85252=CARTESIAN_POINT('Ctrl Pts',(-0.866025403784439,-1.5,4.67708333333332)) ;
#85253=CARTESIAN_POINT('Ctrl Pts',(-1.83697019872103E-16,-1.5,4.71874999999999)) ;
#85254=CARTESIAN_POINT('Ctrl Pts',(0.866025403784438,-1.5,4.76041666666666)) ;
#85255=CARTESIAN_POINT('Ctrl Pts',(1.29903810567666,-0.750000000000001,
4.80208333333332)) ;
#85256=CARTESIAN_POINT('Ctrl Pts',(1.73205080756888,-3.18172571617472E-16,
4.84374999999999)) ;
#85257=CARTESIAN_POINT('Ctrl Pts',(1.29903810567666,0.749999999999999,4.88541666666666)) ;
#85258=CARTESIAN_POINT('Ctrl Pts',(0.86602540378444,1.5,4.92708333333332)) ;
#85259=CARTESIAN_POINT('Ctrl Pts',(0.,1.5,4.96874999999999)) ;
#85260=CARTESIAN_POINT('Ctrl Pts',(-0.866025403784439,1.5,5.01041666666666)) ;
#85261=CARTESIAN_POINT('Ctrl Pts',(-1.29903810567666,0.750000000000001,
5.05208333333332)) ;
#85262=CARTESIAN_POINT('Ctrl Pts',(-1.73205080756888,1.06057523872491E-16,
5.09374999999999)) ;
#85263=CARTESIAN_POINT('Ctrl Pts',(-1.29903810567666,-0.75,5.13541666666666)) ;
#85264=CARTESIAN_POINT('Ctrl Pts',(-0.866025403784439,-1.5,5.17708333333332)) ;
#85265=CARTESIAN_POINT('Ctrl Pts',(-1.83697019872103E-16,-1.5,5.21874999999999)) ;
#85266=CARTESIAN_POINT('Ctrl Pts',(0.866025403784438,-1.5,5.26041666666666)) ;
#85267=CARTESIAN_POINT('Ctrl Pts',(1.29903810567666,-0.750000000000001,
5.30208333333332)) ;
#85268=CARTESIAN_POINT('Ctrl Pts',(1.73205080756888,-3.18172571617472E-16,
5.34374999999999)) ;
#85269=CARTESIAN_POINT('Ctrl Pts',(1.29903810567666,0.749999999999999,5.38541666666665)) ;
#85270=CARTESIAN_POINT('Ctrl Pts',(0.86602540378444,1.5,5.42708333333332)) ;
#85271=CARTESIAN_POINT('Ctrl Pts',(0.,1.5,5.46874999999999)) ;
#85272=CARTESIAN_POINT('Ctrl Pts',(-0.866025403784439,1.5,5.51041666666666)) ;
#85273=CARTESIAN_POINT('Ctrl Pts',(-1.29903810567666,0.750000000000001,
5.55208333333332)) ;
#85274=CARTESIAN_POINT('Ctrl Pts',(-1.73205080756888,1.06057523872491E-16,
5.59374999999999)) ;
#85275=CARTESIAN_POINT('Ctrl Pts',(-1.29903810567666,-0.75,5.63541666666666)) ;
#85276=CARTESIAN_POINT('Ctrl Pts',(-0.866025403784439,-1.5,5.67708333333332)) ;
#85277=CARTESIAN_POINT('Ctrl Pts',(-1.83697019872103E-16,-1.5,5.71874999999999)) ;
#85278=CARTESIAN_POINT('Ctrl Pts',(0.866025403784438,-1.5,5.76041666666665)) ;
#85279=CARTESIAN_POINT('Ctrl Pts',(1.29903810567666,-0.750000000000001,
5.80208333333332)) ;
#85280=CARTESIAN_POINT('Ctrl Pts',(1.73205080756888,-3.18172571617472E-16,
5.84374999999999)) ;
#85281=CARTESIAN_POINT('Ctrl Pts',(1.29903810567666,0.749999999999999,5.88541666666666)) ;
#85282=CARTESIAN_POINT('Ctrl Pts',(0.86602540378444,1.5,5.92708333333332)) ;
#85283=CARTESIAN_POINT('Ctrl Pts',(0.,1.5,5.96874999999999)) ;
#85284=CARTESIAN_POINT('Ctrl Pts',(-0.866025403784439,1.5,6.01041666666665)) ;
#85285=CARTESIAN_POINT('Ctrl Pts',(-1.29903810567666,0.750000000000001,
6.05208333333332)) ;
#85286=CARTESIAN_POINT('Ctrl Pts',(-1.73205080756888,1.06057523872491E-16,
6.09374999999999)) ;
#85287=CARTESIAN_POINT('Ctrl Pts',(-1.29903810567666,-0.75,6.13541666666665)) ;
#85288=CARTESIAN_POINT('Ctrl Pts',(-0.866025403784439,-1.5,6.17708333333332)) ;
#85289=CARTESIAN_POINT('Ctrl Pts',(-1.83697019872103E-16,-1.5,6.21874999999999)) ;
#85290=CARTESIAN_POINT('Ctrl Pts',(0.866025403784438,-1.5,6.26041666666665)) ;
#85291=CARTESIAN_POINT('Ctrl Pts',(1.29903810567666,-0.750000000000001,
6.30208333333332)) ;
#85292=CARTESIAN_POINT('Ctrl Pts',(1.73205080756888,-3.18172571617472E-16,
6.34374999999999)) ;
#85293=CARTESIAN_POINT('Ctrl Pts',(1.29903810567666,0.749999999999999,6.38541666666665)) ;
#85294=CARTESIAN_POINT('Ctrl Pts',(0.86602540378444,1.5,6.42708333333332)) ;
#85295=CARTESIAN_POINT('Ctrl Pts',(0.,1.5,6.46874999999999)) ;
#85296=CARTESIAN_POINT('Ctrl Pts',(-0.866025403784439,1.5,6.51041666666665)) ;
#85297=CARTESIAN_POINT('Ctrl Pts',(-1.29903810567666,0.750000000000001,
6.55208333333332)) ;
#85298=CARTESIAN_POINT('Ctrl Pts',(-1.73205080756888,1.06057523872491E-16,
6.59374999999999)) ;
#85299=CARTESIAN_POINT('Ctrl Pts',(-1.29903810567666,-0.75,6.63541666666665)) ;
#85300=CARTESIAN_POINT('Ctrl Pts',(-0.866025403784439,-1.5,6.67708333333332)) ;
#85301=CARTESIAN_POINT('Ctrl Pts',(-1.83697019872103E-16,-1.5,6.71874999999999)) ;
#85302=CARTESIAN_POINT('Ctrl Pts',(0.866025403784438,-1.5,6.76041666666665)) ;
#85303=CARTESIAN_POINT('Ctrl Pts',(1.29903810567666,-0.750000000000001,
6.80208333333332)) ;
#85304=CARTESIAN_POINT('Ctrl Pts',(1.73205080756888,-3.18172571617472E-16,
6.84374999999999)) ;
#85305=CARTESIAN_POINT('Ctrl Pts',(1.29903810567666,0.749999999999999,6.88541666666665)) ;
#85306=CARTESIAN_POINT('Ctrl Pts',(0.86602540378444,1.5,6.92708333333332)) ;
#85307=CARTESIAN_POINT('Ctrl Pts',(0.,1.5,6.96874999999999)) ;
#85308=CARTESIAN_POINT('Ctrl Pts',(-0.866025403784439,1.5,7.01041666666665)) ;
#85309=CARTESIAN_POINT('Ctrl Pts',(-1.29903810567666,0.750000000000001,
7.05208333333332)) ;
#85310=CARTESIAN_POINT('Ctrl Pts',(-1.73205080756888,1.06057523872491E-16,
7.09374999999999)) ;
#85311=CARTESIAN_POINT('Ctrl Pts',(-1.29903810567666,-0.75,7.13541666666665)) ;
#85312=CARTESIAN_POINT('Ctrl Pts',(-0.866025403784439,-1.5,7.17708333333332)) ;
#85313=CARTESIAN_POINT('Ctrl Pts',(-1.83697019872103E-16,-1.5,7.21874999999998)) ;
#85314=CARTESIAN_POINT('Ctrl Pts',(0.866025403784438,-1.5,7.26041666666665)) ;
#85315=CARTESIAN_POINT('Ctrl Pts',(1.29903810567666,-0.750000000000001,
7.30208333333332)) ;
#85316=CARTESIAN_POINT('Ctrl Pts',(1.73205080756888,-3.18172571617472E-16,
7.34374999999998)) ;
#85317=CARTESIAN_POINT('Ctrl Pts',(1.29903810567666,0.749999999999999,7.38541666666665)) ;
#85318=CARTESIAN_POINT('Ctrl Pts',(0.86602540378444,1.5,7.42708333333332)) ;
#85319=CARTESIAN_POINT('Ctrl Pts',(0.,1.5,7.46874999999998)) ;
#85320=CARTESIAN_POINT('Ctrl Pts',(-0.866025403784439,1.5,7.51041666666665)) ;
#85321=CARTESIAN_POINT('Ctrl Pts',(-1.29903810567666,0.750000000000001,
7.55208333333332)) ;
#85322=CARTESIAN_POINT('Ctrl Pts',(-1.73205080756888,1.06057523872491E-16,
7.59374999999998)) ;
#85323=CARTESIAN_POINT('Ctrl Pts',(-1.29903810567666,-0.75,7.63541666666665)) ;
#85324=CARTESIAN_POINT('Ctrl Pts',(-0.866025403784439,-1.5,7.67708333333332)) ;
#85325=CARTESIAN_POINT('Ctrl Pts',(-1.83697019872103E-16,-1.5,7.71874999999998)) ;
#85326=CARTESIAN_POINT('Ctrl Pts',(0.866025403784438,-1.5,7.76041666666665)) ;
#85327=CARTESIAN_POINT('Ctrl Pts',(1.29903810567666,-0.750000000000001,
7.80208333333332)) ;
#85328=CARTESIAN_POINT('Ctrl Pts',(1.73205080756888,-3.18172571617472E-16,
7.84374999999998)) ;
#85329=CARTESIAN_POINT('Ctrl Pts',(1.29903810567666,0.749999999999999,7.88541666666665)) ;
#85330=CARTESIAN_POINT('Ctrl Pts',(0.86602540378444,1.5,7.92708333333332)) ;
#85331=CARTESIAN_POINT('Ctrl Pts',(0.,1.5,7.96874999999998)) ;
#85332=CARTESIAN_POINT('Ctrl Pts',(-0.866025403784439,1.5,8.01041666666665)) ;
#85333=CARTESIAN_POINT('Ctrl Pts',(-1.29903810567666,0.750000000000001,
8.05208333333332)) ;
#85334=CARTESIAN_POINT('Ctrl Pts',(-1.73205080756888,1.06057523872491E-16,
8.09374999999998)) ;
#85335=CARTESIAN_POINT('Ctrl Pts',(-1.29903810567666,-0.75,8.13541666666665)) ;
#85336=CARTESIAN_POINT('Ctrl Pts',(-0.866025403784439,-1.5,8.17708333333332)) ;
#85337=CARTESIAN_POINT('Ctrl Pts',(-1.83697019872103E-16,-1.5,8.21874999999998)) ;
#85338=CARTESIAN_POINT('Ctrl Pts',(0.866025403784438,-1.5,8.26041666666665)) ;
#85339=CARTESIAN_POINT('Ctrl Pts',(1.29903810567666,-0.750000000000001,
8.30208333333332)) ;
#85340=CARTESIAN_POINT('Ctrl Pts',(1.73205080756888,-3.18172571617472E-16,
8.34374999999998)) ;
#85341=CARTESIAN_POINT('Ctrl Pts',(1.29903810567666,0.749999999999999,8.38541666666665)) ;
#85342=CARTESIAN_POINT('Ctrl Pts',(0.86602540378444,1.5,8.42708333333332)) ;
#85343=CARTESIAN_POINT('Ctrl Pts',(0.,1.5,8.46874999999998)) ;
#85344=CARTESIAN_POINT('Ctrl Pts',(-0.866025403784439,1.5,8.51041666666665)) ;
#85345=CARTESIAN_POINT('Ctrl Pts',(-1.29903810567666,0.750000000000001,
8.55208333333331)) ;
#85346=CARTESIAN_POINT('Ctrl Pts',(-1.73205080756888,1.06057523872491E-16,
8.59374999999998)) ;
#85347=CARTESIAN_POINT('Ctrl Pts',(-1.29903810567666,-0.75,8.63541666666665)) ;
#85348=CARTESIAN_POINT('Ctrl Pts',(-0.866025403784439,-1.5,8.67708333333331)) ;
#85349=CARTESIAN_POINT('Ctrl Pts',(-1.83697019872103E-16,-1.5,8.71874999999998)) ;
#85350=CARTESIAN_POINT('Ctrl Pts',(0.866025403784438,-1.5,8.76041666666665)) ;
#85351=CARTESIAN_POINT('Ctrl Pts',(1.29903810567666,-0.750000000000001,
8.80208333333331)) ;
#85352=CARTESIAN_POINT('Ctrl Pts',(1.73205080756888,-3.18172571617472E-16,
8.84374999999998)) ;
#85353=CARTESIAN_POINT('Ctrl Pts',(1.29903810567666,0.749999999999999,8.88541666666665)) ;
#85354=CARTESIAN_POINT('Ctrl Pts',(0.86602540378444,1.5,8.92708333333331)) ;
#85355=CARTESIAN_POINT('Ctrl Pts',(0.,1.5,8.96874999999998)) ;
#85356=CARTESIAN_POINT('Ctrl Pts',(-0.000186377689213934,1.49999998842112,
0.0312589667791176)) ;
#85357=CARTESIAN_POINT('Ctrl Pts',(0.865963275659358,1.50010760906922,-0.0104106883850433)) ;
#85358=CARTESIAN_POINT('Ctrl Pts',(1.29903810567666,0.750000000000001,-0.0520833333333332)) ;
#85359=CARTESIAN_POINT('Ctrl Pts',(1.73205080756888,1.06057523872491E-16,
-0.0937499999999997)) ;
#85360=CARTESIAN_POINT('Ctrl Pts',(1.29903810567666,-0.75,-0.135416666666666)) ;
#85361=CARTESIAN_POINT('Ctrl Pts',(0.866025403784439,-1.5,-0.177083333333333)) ;
#85362=CARTESIAN_POINT('Ctrl Pts',(1.83697019872103E-16,-1.5,-0.21875)) ;
#85363=CARTESIAN_POINT('Ctrl Pts',(-0.866025403784438,-1.5,-0.260416666666666)) ;
#85364=CARTESIAN_POINT('Ctrl Pts',(-1.29903810567666,-0.750000000000001,
-0.302083333333333)) ;
#85365=CARTESIAN_POINT('Ctrl Pts',(-1.73205080756888,-3.18172571617472E-16,
-0.343749999999999)) ;
#85366=CARTESIAN_POINT('Ctrl Pts',(-1.29903810567666,0.749999999999999,
-0.385416666666666)) ;
#85367=CARTESIAN_POINT('Ctrl Pts',(-0.86602540378444,1.5,-0.427083333333332)) ;
#85368=CARTESIAN_POINT('Ctrl Pts',(0.,1.5,-0.468749999999999)) ;
#85369=CARTESIAN_POINT('Ctrl Pts',(-0.000146025735824457,1.17524046450886,
0.218758966779122)) ;
#85370=CARTESIAN_POINT('Ctrl Pts',(0.678476726793011,1.17532478460315,0.177089311614961)) ;
#85371=CARTESIAN_POINT('Ctrl Pts',(1.01778810567666,0.587620236790419,0.135416666666671)) ;
#85372=CARTESIAN_POINT('Ctrl Pts',(1.35705080756888,8.30953963884779E-17,
0.0937500000000043)) ;
#85373=CARTESIAN_POINT('Ctrl Pts',(1.01778810567666,-0.587620236790419,
0.0520833333333377)) ;
#85374=CARTESIAN_POINT('Ctrl Pts',(0.67852540378444,-1.17524047358084,0.0104166666666711)) ;
#85375=CARTESIAN_POINT('Ctrl Pts',(1.43925448419919E-16,-1.17524047358084,
-0.0312499999999955)) ;
#85376=CARTESIAN_POINT('Ctrl Pts',(-0.678525403784439,-1.17524047358084,
-0.0729166666666621)) ;
#85377=CARTESIAN_POINT('Ctrl Pts',(-1.01778810567666,-0.587620236790419,
-0.114583333333329)) ;
#85378=CARTESIAN_POINT('Ctrl Pts',(-1.35705080756888,-2.49286189165434E-16,
-0.156249999999995)) ;
#85379=CARTESIAN_POINT('Ctrl Pts',(-1.01778810567666,0.587620236790418,
-0.197916666666662)) ;
#85380=CARTESIAN_POINT('Ctrl Pts',(-0.67852540378444,1.17524047358084,-0.239583333333328)) ;
#85381=CARTESIAN_POINT('Ctrl Pts',(0.,1.17524047358084,-0.281249999999995)) ;
#85382=CARTESIAN_POINT('Origin',(0.,0.,9.56735957759373E-18)) ;
#85383=CARTESIAN_POINT('Origin',(0.,0.,10.5)) ;
#85384=CARTESIAN_POINT('',(-0.214086590007416,0.905647899858295,8.375)) ;
#85385=CARTESIAN_POINT('Ctrl Pts',(-0.214086590007055,0.905647899857224,
8.37499999999588)) ;
#85386=CARTESIAN_POINT('Ctrl Pts',(-0.27901076445186,1.09462213692769,9.11708670961361)) ;
#85387=CARTESIAN_POINT('Ctrl Pts',(-0.378092453297399,1.38212190130695,
10.249595595364)) ;
#85388=CARTESIAN_POINT('',(0.214086590007411,0.905647899858296,8.375)) ;
#85389=CARTESIAN_POINT('Origin',(0.,0.,8.375)) ;
#85390=CARTESIAN_POINT('Ctrl Pts',(0.21408659000705,0.905647899857235,8.37499999999588)) ;
#85391=CARTESIAN_POINT('Ctrl Pts',(0.279010764449613,1.09462213692116,9.11708670958797)) ;
#85392=CARTESIAN_POINT('Ctrl Pts',(0.378092453294824,1.38212190129948,10.2495955953347)) ;
#85393=CARTESIAN_POINT('Origin',(0.4,6.2338841963792E-17,10.5)) ;
#85394=CARTESIAN_POINT('',(0.214086590007411,0.713019523490749,8.375)) ;
#85395=CARTESIAN_POINT('',(0.214086590007411,3.33647752525978E-17,8.375)) ;
#85396=CARTESIAN_POINT('',(0.398867118306387,0.749774655820362,10.4870511029892)) ;
#85397=CARTESIAN_POINT('Origin',(0.606586399182262,0.251256313292347,10.5)) ;
#85398=CARTESIAN_POINT('',(0.360220662867382,0.360220662867381,8.375)) ;
#85399=CARTESIAN_POINT('',(0.434824804870729,0.180110331433686,8.375)) ;
#85400=CARTESIAN_POINT('',(0.501858559970094,0.501858559970092,10.4902321148732)) ;
#85401=CARTESIAN_POINT('Origin',(0.251256313292348,0.606586399182262,10.5)) ;
#85402=CARTESIAN_POINT('',(0.71301952349075,0.214086590007409,8.375)) ;
#85403=CARTESIAN_POINT('',(0.180110331433687,0.434824804870729,8.375)) ;
#85404=CARTESIAN_POINT('',(0.750162198617137,0.400815427513497,10.5093203791284)) ;
#85405=CARTESIAN_POINT('Origin',(0.,0.399999999999998,10.5)) ;
#85406=CARTESIAN_POINT('',(0.,0.214086590007409,8.375)) ;
#85407=CARTESIAN_POINT('Origin',(0.,0.,8.375)) ;
#85408=CARTESIAN_POINT('',(0.713019523490766,-0.21408659000743,8.375)) ;
#85409=CARTESIAN_POINT('',(-7.51067965057384E-16,-0.214086590007428,8.375)) ;
#85410=CARTESIAN_POINT('',(-0.214086590007418,0.713019523490736,8.375)) ;
#85411=CARTESIAN_POINT('',(-0.214086590007425,2.27939140812495E-15,8.375)) ;
#85412=CARTESIAN_POINT('',(-0.360220662867393,0.360220662867369,8.375)) ;
#85413=CARTESIAN_POINT('',(-0.434824804870735,0.180110331433695,8.375)) ;
#85414=CARTESIAN_POINT('',(-0.713019523490764,0.214086590007402,8.375)) ;
#85415=CARTESIAN_POINT('',(-0.180110331433678,0.434824804870723,8.375)) ;
#85416=CARTESIAN_POINT('',(-0.905647899858292,0.214086590007404,8.375)) ;
#85417=CARTESIAN_POINT('',(2.24602663287203E-15,0.214086590007395,8.375)) ;
#85418=CARTESIAN_POINT('',(-0.905647899858305,-0.214086590007436,8.375)) ;
#85419=CARTESIAN_POINT('Origin',(-4.11190782820327E-15,-4.14316783061991E-14,
8.375)) ;
#85420=CARTESIAN_POINT('',(-0.713019523490751,-0.214086590007437,8.375)) ;
#85421=CARTESIAN_POINT('',(-1.49495866781509E-15,-0.214086590007442,8.375)) ;
#85422=CARTESIAN_POINT('',(-0.360220662867385,-0.360220662867411,8.375)) ;
#85423=CARTESIAN_POINT('',(-0.180110331433702,-0.434824804870756,8.375)) ;
#85424=CARTESIAN_POINT('',(-0.214086590007416,-0.713019523490781,8.375)) ;
#85425=CARTESIAN_POINT('',(-0.434824804870743,-0.180110331433688,8.375)) ;
#85426=CARTESIAN_POINT('',(-0.214086590007411,1.53550070536725E-15,8.375)) ;
#85427=CARTESIAN_POINT('',(0.214086590007423,-0.713019523490768,8.375)) ;
#85428=CARTESIAN_POINT('',(0.214086590007425,-7.10525927504996E-16,8.375)) ;
#85429=CARTESIAN_POINT('',(0.360220662867396,-0.3602206628674,8.375)) ;
#85430=CARTESIAN_POINT('',(0.434824804870748,-0.180110331433697,8.375)) ;
#85431=CARTESIAN_POINT('',(0.180110331433693,-0.43482480487075,8.375)) ;
#85432=CARTESIAN_POINT('Origin',(1.93815854595261E-14,-0.400000000000021,
10.5)) ;
#85433=CARTESIAN_POINT('',(0.749774655820382,-0.398867118306411,10.4870511029892)) ;
#85434=CARTESIAN_POINT('Origin',(0.251256313292365,-0.606586399182284,10.5)) ;
#85435=CARTESIAN_POINT('',(0.501858559970111,-0.501858559970116,10.4902321148732)) ;
#85436=CARTESIAN_POINT('Origin',(0.606586399182282,-0.251256313292371,10.5)) ;
#85437=CARTESIAN_POINT('',(0.400815427513515,-0.75016219861716,10.5093203791284)) ;
#85438=CARTESIAN_POINT('Origin',(0.400000000000019,-2.21124316886369E-14,
10.5)) ;
#85439=CARTESIAN_POINT('Origin',(-0.4,-3.87008320770884E-14,10.5)) ;
#85440=CARTESIAN_POINT('',(-0.398867118306393,-0.749774655820401,10.4870511029892)) ;
#85441=CARTESIAN_POINT('Origin',(-0.606586399182264,-0.251256313292384,
10.5)) ;
#85442=CARTESIAN_POINT('',(-0.501858559970097,-0.50185855997013,10.4902321148732)) ;
#85443=CARTESIAN_POINT('Origin',(-0.251256313292353,-0.606586399182301,
10.5)) ;
#85444=CARTESIAN_POINT('',(-0.75016219861714,-0.400815427513533,10.5093203791284)) ;
#85445=CARTESIAN_POINT('Origin',(-2.79318507107464E-15,-0.400000000000039,
10.5)) ;
#85446=CARTESIAN_POINT('Ctrl Pts',(-0.905647899857242,-0.214086590007075,
8.37499999999588)) ;
#85447=CARTESIAN_POINT('Ctrl Pts',(-1.09462213691718,-0.279010764448275,
9.11708670957237)) ;
#85448=CARTESIAN_POINT('Ctrl Pts',(-1.38212190129947,-0.378092453294853,
10.2495955953347)) ;
#85449=CARTESIAN_POINT('Origin',(1.12142940769163E-15,-4.14316783061991E-14,
10.5)) ;
#85450=CARTESIAN_POINT('Ctrl Pts',(-0.905647899857243,0.214086590007043,
8.37499999999588)) ;
#85451=CARTESIAN_POINT('Ctrl Pts',(-1.09462213691218,0.279010764446527,
9.11708670955277)) ;
#85452=CARTESIAN_POINT('Ctrl Pts',(-1.38212190129944,0.37809245329482,10.2495955953347)) ;
#85453=CARTESIAN_POINT('Origin',(-1.65884003884516E-14,0.399999999999979,
10.5)) ;
#85454=CARTESIAN_POINT('',(-0.749774655820378,0.398867118306375,10.4870511029892)) ;
#85455=CARTESIAN_POINT('Origin',(-0.251256313292361,0.606586399182244,10.5)) ;
#85456=CARTESIAN_POINT('',(-0.501858559970107,0.501858559970078,10.4902321148732)) ;
#85457=CARTESIAN_POINT('Origin',(-0.60658639918228,0.251256313292334,10.5)) ;
#85458=CARTESIAN_POINT('',(-0.400815427513509,0.75016219861712,10.5093203791284)) ;
#85459=CARTESIAN_POINT('Origin',(-0.400000000000019,-1.65260615464876E-14,
10.5)) ;
#86301=UNCERTAINTY_MEASURE_WITH_UNIT(LENGTH_MEASURE(0.01),#86331,
'DISTANCE_ACCURACY_VALUE',
'Maximum model space distance between geometric entities at asserted c
onnectivities') ;
#86304=UNCERTAINTY_MEASURE_WITH_UNIT(LENGTH_MEASURE(0.01),#86331,
'DISTANCE_ACCURACY_VALUE',
'Maximum model space distance between geometric entities at asserted c
onnectivities') ;
#86327=(
GEOMETRIC_REPRESENTATION_CONTEXT(3)
GLOBAL_UNCERTAINTY_ASSIGNED_CONTEXT((#86301))
GLOBAL_UNIT_ASSIGNED_CONTEXT((#86331,#86333,#86334))
REPRESENTATION_CONTEXT('','3D')
) ;
#86330=(
GEOMETRIC_REPRESENTATION_CONTEXT(3)
GLOBAL_UNCERTAINTY_ASSIGNED_CONTEXT((#86304))
GLOBAL_UNIT_ASSIGNED_CONTEXT((#86331,#86333,#86334))
REPRESENTATION_CONTEXT('','3D')
) ;
#86331=(
LENGTH_UNIT()
NAMED_UNIT(*)
SI_UNIT(.MILLI.,.METRE.)
) ;
#86333=(
NAMED_UNIT(*)
PLANE_ANGLE_UNIT()
SI_UNIT($,.RADIAN.)
) ;
#86334=(
NAMED_UNIT(*)
SI_UNIT($,.STERADIAN.)
SOLID_ANGLE_UNIT()
) ;
#86357=SHAPE_DEFINITION_REPRESENTATION(#86428,#86473) ;
#86428=PRODUCT_DEFINITION_SHAPE('',$,#86499) ;
#86473=SHAPE_REPRESENTATION('',(#36381),#86327) ;
#86476=PRODUCT_DEFINITION_CONTEXT('part definition',#86553,'design') ;
#86499=PRODUCT_DEFINITION('Pan_Head_Phillips_Screw',
'Pan_Head_Phillips_Screw',#86524,#86476) ;
#86524=PRODUCT_DEFINITION_FORMATION('',$,#86577) ;
#86553=APPLICATION_CONTEXT(
'Core Data for Automotive Mechanical Design Process') ;
#86554=PRODUCT_CONTEXT('part definition',#86553,'mechanical') ;
#86577=PRODUCT('Pan_Head_Phillips_Screw','Pan_Head_Phillips_Screw',$,(#86554)) ;
#86582=PRESENTATION_STYLE_ASSIGNMENT((#86587)) ;
#86587=SURFACE_STYLE_USAGE(.BOTH.,#86592) ;
#86592=SURFACE_SIDE_STYLE('',(#86597)) ;
#86597=SURFACE_STYLE_FILL_AREA(#86602) ;
#86602=FILL_AREA_STYLE('Opaque(203,203,203)',(#86607)) ;
#86607=FILL_AREA_STYLE_COLOUR('Opaque(203,203,203)',#86612) ;
#86612=COLOUR_RGB('Opaque(203,203,203)', 0.66274510, 0.83137255, 0.94901961) ;
ENDSEC;
END-ISO-10303-21;
